ISO-10303-21;
HEADER;
/* Generated by software containing ST-Developer
 * from STEP Tools, Inc. (www.steptools.com) 
 */

FILE_DESCRIPTION(
/* description */ ('STEP AP214'),
/* implementation_level */ '2;1');

FILE_NAME(
/* name */ 'Countersunk Screw ISO 10642 M4x12 A2.step',
/* time_stamp */ '2026-11-14T05:50:49-08:00',
/* author */ (''),
/* organization */ (''),
/* preprocessor_version */ 'ST-DEVELOPER v20.2',
/* originating_system */ 'Autodesk Translation Framework v15.17.0.0',
/* authorisation */ '');

FILE_SCHEMA (('AUTOMOTIVE_DESIGN { 1 0 10303 214 3 1 1 }'));
ENDSEC;

DATA;
#10=MECHANICAL_DESIGN_GEOMETRIC_PRESENTATION_REPRESENTATION('',(#163),#9903);
#63=(
BOUNDED_SURFACE()
B_SPLINE_SURFACE(1,2,((#4642,#4643,#4644,#4645,#4646,#4647,#4648,#4649,
#4650,#4651,#4652,#4653,#4654,#4655,#4656,#4657,#4658,#4659,#4660,#4661,
#4662,#4663,#4664,#4665,#4666,#4667,#4668,#4669,#4670,#4671,#4672,#4673,
#4674,#4675,#4676,#4677,#4678,#4679,#4680,#4681,#4682,#4683,#4684,#4685,
#4686,#4687,#4688,#4689,#4690,#4691,#4692,#4693,#4694,#4695,#4696,#4697,
#4698,#4699,#4700,#4701,#4702,#4703,#4704,#4705,#4706,#4707,#4708,#4709,
#4710,#4711,#4712,#4713,#4714,#4715,#4716,#4717,#4718,#4719,#4720,#4721,
#4722,#4723,#4724,#4725,#4726,#4727,#4728,#4729,#4730,#4731,#4732,#4733,
#4734,#4735,#4736,#4737,#4738,#4739,#4740,#4741,#4742,#4743,#4744,#4745,
#4746,#4747,#4748,#4749,#4750,#4751,#4752,#4753,#4754,#4755,#4756,#4757,
#4758,#4759,#4760,#4761,#4762,#4763,#4764,#4765,#4766,#4767,#4768,#4769,
#4770,#4771,#4772,#4773,#4774,#4775,#4776,#4777,#4778,#4779,#4780,#4781,
#4782,#4783,#4784,#4785,#4786,#4787,#4788,#4789,#4790,#4791,#4792,#4793,
#4794,#4795,#4796,#4797,#4798,#4799,#4800,#4801,#4802,#4803,#4804,#4805,
#4806,#4807,#4808,#4809,#4810,#4811,#4812,#4813,#4814,#4815,#4816,#4817,
#4818,#4819,#4820,#4821,#4822,#4823,#4824,#4825,#4826,#4827,#4828,#4829,
#4830,#4831,#4832,#4833,#4834,#4835,#4836,#4837,#4838,#4839,#4840,#4841,
#4842,#4843,#4844,#4845,#4846,#4847,#4848,#4849,#4850,#4851,#4852,#4853,
#4854,#4855,#4856,#4857,#4858,#4859,#4860,#4861,#4862,#4863,#4864,#4865,
#4866,#4867,#4868,#4869,#4870,#4871,#4872,#4873,#4874,#4875,#4876,#4877,
#4878,#4879,#4880,#4881,#4882,#4883,#4884,#4885,#4886,#4887,#4888,#4889,
#4890,#4891,#4892,#4893,#4894,#4895,#4896,#4897,#4898,#4899,#4900,#4901,
#4902,#4903,#4904,#4905,#4906,#4907,#4908,#4909,#4910,#4911,#4912,#4913,
#4914,#4915,#4916,#4917,#4918,#4919,#4920,#4921,#4922,#4923,#4924,#4925,
#4926,#4927,#4928,#4929,#4930,#4931,#4932,#4933,#4934,#4935,#4936,#4937,
#4938,#4939,#4940,#4941,#4942,#4943,#4944,#4945,#4946,#4947,#4948,#4949,
#4950,#4951,#4952,#4953,#4954,#4955,#4956,#4957,#4958,#4959,#4960,#4961,
#4962,#4963,#4964,#4965,#4966,#4967,#4968,#4969,#4970,#4971,#4972,#4973,
#4974,#4975,#4976,#4977,#4978,#4979,#4980,#4981,#4982,#4983,#4984,#4985,
#4986,#4987,#4988,#4989,#4990,#4991,#4992,#4993,#4994,#4995,#4996,#4997,
#4998,#4999,#5000,#5001,#5002,#5003,#5004,#5005,#5006,#5007,#5008,#5009,
#5010,#5011,#5012,#5013,#5014,#5015,#5016,#5017,#5018,#5019,#5020,#5021,
#5022,#5023,#5024,#5025,#5026,#5027,#5028,#5029,#5030,#5031,#5032,#5033,
#5034,#5035,#5036,#5037,#5038,#5039,#5040,#5041,#5042,#5043,#5044,#5045,
#5046,#5047,#5048,#5049,#5050,#5051,#5052,#5053,#5054,#5055,#5056,#5057,
#5058,#5059,#5060,#5061,#5062,#5063,#5064,#5065,#5066,#5067,#5068,#5069,
#5070,#5071,#5072,#5073,#5074,#5075,#5076,#5077,#5078,#5079,#5080,#5081,
#5082,#5083,#5084,#5085,#5086,#5087,#5088,#5089,#5090,#5091,#5092,#5093,
#5094,#5095,#5096,#5097,#5098,#5099,#5100,#5101,#5102,#5103,#5104,#5105,
#5106,#5107,#5108,#5109,#5110,#5111,#5112,#5113,#5114,#5115,#5116,#5117,
#5118,#5119,#5120,#5121,#5122,#5123,#5124,#5125,#5126,#5127,#5128,#5129,
#5130,#5131,#5132,#5133,#5134,#5135,#5136,#5137,#5138,#5139,#5140,#5141,
#5142,#5143,#5144,#5145,#5146,#5147,#5148,#5149,#5150,#5151,#5152,#5153,
#5154,#5155,#5156,#5157,#5158,#5159,#5160,#5161,#5162,#5163,#5164,#5165,
#5166,#5167,#5168,#5169,#5170,#5171,#5172,#5173,#5174,#5175,#5176,#5177,
#5178,#5179,#5180,#5181,#5182,#5183,#5184,#5185,#5186,#5187,#5188,#5189,
#5190,#5191,#5192,#5193,#5194,#5195,#5196,#5197,#5198,#5199,#5200,#5201,
#5202,#5203,#5204,#5205,#5206,#5207,#5208,#5209,#5210,#5211,#5212,#5213,
#5214,#5215,#5216,#5217,#5218,#5219,#5220,#5221,#5222,#5223,#5224,#5225,
#5226,#5227,#5228,#5229,#5230,#5231,#5232,#5233,#5234,#5235,#5236,#5237,
#5238,#5239,#5240,#5241,#5242,#5243,#5244,#5245,#5246,#5247,#5248,#5249,
#5250,#5251,#5252,#5253,#5254,#5255,#5256,#5257,#5258,#5259,#5260,#5261,
#5262,#5263,#5264,#5265,#5266,#5267,#5268,#5269,#5270,#5271,#5272,#5273,
#5274,#5275,#5276,#5277,#5278,#5279,#5280,#5281,#5282,#5283,#5284,#5285,
#5286,#5287,#5288,#5289,#5290,#5291,#5292,#5293,#5294,#5295,#5296,#5297,
#5298,#5299,#5300,#5301,#5302,#5303,#5304,#5305,#5306,#5307,#5308,#5309,
#5310,#5311,#5312,#5313,#5314,#5315,#5316,#5317,#5318,#5319,#5320,#5321,
#5322,#5323,#5324,#5325,#5326,#5327,#5328,#5329,#5330,#5331,#5332,#5333,
#5334,#5335,#5336,#5337,#5338,#5339,#5340,#5341,#5342,#5343,#5344,#5345,
#5346,#5347,#5348,#5349,#5350,#5351,#5352,#5353,#5354,#5355,#5356,#5357,
#5358,#5359,#5360,#5361,#5362,#5363,#5364,#5365,#5366,#5367,#5368,#5369,
#5370,#5371,#5372,#5373,#5374,#5375,#5376,#5377,#5378,#5379,#5380,#5381,
#5382,#5383,#5384,#5385,#5386,#5387,#5388,#5389,#5390,#5391,#5392,#5393,
#5394,#5395,#5396,#5397,#5398,#5399,#5400,#5401,#5402,#5403,#5404,#5405,
#5406,#5407,#5408,#5409,#5410,#5411,#5412,#5413,#5414,#5415,#5416,#5417,
#5418,#5419,#5420,#5421,#5422,#5423,#5424,#5425,#5426,#5427,#5428,#5429,
#5430,#5431,#5432,#5433,#5434,#5435,#5436,#5437,#5438,#5439,#5440,#5441,
#5442,#5443,#5444,#5445,#5446,#5447,#5448,#5449,#5450,#5451,#5452,#5453,
#5454,#5455,#5456,#5457,#5458,#5459,#5460,#5461,#5462,#5463,#5464,#5465,
#5466,#5467,#5468,#5469,#5470,#5471,#5472,#5473,#5474,#5475,#5476,#5477,
#5478,#5479,#5480,#5481,#5482,#5483,#5484,#5485,#5486,#5487,#5488,#5489,
#5490,#5491,#5492,#5493,#5494,#5495,#5496,#5497,#5498,#5499,#5500,#5501,
#5502,#5503,#5504,#5505,#5506,#5507,#5508,#5509,#5510,#5511,#5512,#5513,
#5514,#5515,#5516,#5517,#5518,#5519,#5520,#5521,#5522,#5523,#5524,#5525,
#5526,#5527,#5528,#5529,#5530,#5531,#5532,#5533,#5534,#5535,#5536,#5537,
#5538,#5539,#5540,#5541,#5542,#5543,#5544,#5545,#5546,#5547,#5548,#5549,
#5550,#5551,#5552,#5553,#5554,#5555,#5556,#5557,#5558,#5559,#5560,#5561,
#5562,#5563,#5564,#5565,#5566,#5567,#5568,#5569,#5570,#5571,#5572,#5573,
#5574,#5575,#5576,#5577,#5578,#5579,#5580,#5581,#5582,#5583,#5584,#5585,
#5586,#5587,#5588,#5589,#5590,#5591,#5592,#5593,#5594,#5595,#5596,#5597,
#5598,#5599,#5600,#5601,#5602,#5603,#5604,#5605,#5606,#5607,#5608,#5609,
#5610,#5611,#5612,#5613,#5614,#5615,#5616,#5617,#5618,#5619,#5620,#5621,
#5622,#5623,#5624,#5625,#5626,#5627,#5628,#5629,#5630,#5631,#5632,#5633,
#5634,#5635,#5636,#5637,#5638,#5639,#5640,#5641,#5642,#5643,#5644,#5645,
#5646,#5647,#5648,#5649,#5650,#5651,#5652,#5653,#5654,#5655,#5656,#5657,
#5658,#5659,#5660,#5661,#5662,#5663,#5664,#5665,#5666,#5667,#5668,#5669,
#5670,#5671,#5672,#5673,#5674,#5675,#5676,#5677,#5678,#5679,#5680,#5681,
#5682,#5683,#5684,#5685,#5686,#5687,#5688,#5689,#5690,#5691,#5692,#5693,
#5694,#5695,#5696,#5697,#5698,#5699,#5700,#5701,#5702,#5703,#5704,#5705,
#5706,#5707,#5708,#5709,#5710,#5711,#5712,#5713,#5714,#5715,#5716,#5717,
#5718,#5719,#5720,#5721,#5722,#5723,#5724,#5725,#5726,#5727,#5728,#5729,
#5730,#5731,#5732,#5733,#5734,#5735,#5736,#5737,#5738,#5739,#5740,#5741,
#5742,#5743,#5744,#5745,#5746,#5747,#5748,#5749,#5750,#5751,#5752,#5753,
#5754,#5755,#5756,#5757,#5758,#5759,#5760,#5761,#5762,#5763,#5764,#5765,
#5766,#5767,#5768,#5769,#5770,#5771,#5772,#5773,#5774,#5775,#5776,#5777,
#5778,#5779,#5780,#5781,#5782,#5783,#5784,#5785,#5786,#5787,#5788,#5789,
#5790,#5791,#5792,#5793,#5794,#5795,#5796,#5797,#5798,#5799,#5800,#5801,
#5802,#5803,#5804,#5805,#5806,#5807,#5808,#5809,#5810,#5811,#5812,#5813,
#5814,#5815,#5816,#5817,#5818,#5819,#5820,#5821,#5822,#5823,#5824,#5825,
#5826,#5827,#5828,#5829,#5830,#5831,#5832,#5833,#5834,#5835,#5836,#5837,
#5838,#5839,#5840,#5841,#5842,#5843,#5844,#5845,#5846,#5847,#5848,#5849,
#5850,#5851,#5852,#5853,#5854,#5855,#5856,#5857,#5858,#5859,#5860,#5861,
#5862,#5863,#5864,#5865,#5866,#5867,#5868,#5869,#5870,#5871,#5872,#5873,
#5874,#5875,#5876,#5877,#5878,#5879,#5880,#5881,#5882,#5883,#5884,#5885,
#5886,#5887,#5888,#5889,#5890,#5891,#5892,#5893,#5894,#5895,#5896,#5897,
#5898,#5899,#5900,#5901,#5902,#5903,#5904,#5905,#5906,#5907,#5908,#5909,
#5910,#5911,#5912),(#5913,#5914,#5915,#5916,#5917,#5918,#5919,#5920,#5921,
#5922,#5923,#5924,#5925,#5926,#5927,#5928,#5929,#5930,#5931,#5932,#5933,
#5934,#5935,#5936,#5937,#5938,#5939,#5940,#5941,#5942,#5943,#5944,#5945,
#5946,#5947,#5948,#5949,#5950,#5951,#5952,#5953,#5954,#5955,#5956,#5957,
#5958,#5959,#5960,#5961,#5962,#5963,#5964,#5965,#5966,#5967,#5968,#5969,
#5970,#5971,#5972,#5973,#5974,#5975,#5976,#5977,#5978,#5979,#5980,#5981,
#5982,#5983,#5984,#5985,#5986,#5987,#5988,#5989,#5990,#5991,#5992,#5993,
#5994,#5995,#5996,#5997,#5998,#5999,#6000,#6001,#6002,#6003,#6004,#6005,
#6006,#6007,#6008,#6009,#6010,#6011,#6012,#6013,#6014,#6015,#6016,#6017,
#6018,#6019,#6020,#6021,#6022,#6023,#6024,#6025,#6026,#6027,#6028,#6029,
#6030,#6031,#6032,#6033,#6034,#6035,#6036,#6037,#6038,#6039,#6040,#6041,
#6042,#6043,#6044,#6045,#6046,#6047,#6048,#6049,#6050,#6051,#6052,#6053,
#6054,#6055,#6056,#6057,#6058,#6059,#6060,#6061,#6062,#6063,#6064,#6065,
#6066,#6067,#6068,#6069,#6070,#6071,#6072,#6073,#6074,#6075,#6076,#6077,
#6078,#6079,#6080,#6081,#6082,#6083,#6084,#6085,#6086,#6087,#6088,#6089,
#6090,#6091,#6092,#6093,#6094,#6095,#6096,#6097,#6098,#6099,#6100,#6101,
#6102,#6103,#6104,#6105,#6106,#6107,#6108,#6109,#6110,#6111,#6112,#6113,
#6114,#6115,#6116,#6117,#6118,#6119,#6120,#6121,#6122,#6123,#6124,#6125,
#6126,#6127,#6128,#6129,#6130,#6131,#6132,#6133,#6134,#6135,#6136,#6137,
#6138,#6139,#6140,#6141,#6142,#6143,#6144,#6145,#6146,#6147,#6148,#6149,
#6150,#6151,#6152,#6153,#6154,#6155,#6156,#6157,#6158,#6159,#6160,#6161,
#6162,#6163,#6164,#6165,#6166,#6167,#6168,#6169,#6170,#6171,#6172,#6173,
#6174,#6175,#6176,#6177,#6178,#6179,#6180,#6181,#6182,#6183,#6184,#6185,
#6186,#6187,#6188,#6189,#6190,#6191,#6192,#6193,#6194,#6195,#6196,#6197,
#6198,#6199,#6200,#6201,#6202,#6203,#6204,#6205,#6206,#6207,#6208,#6209,
#6210,#6211,#6212,#6213,#6214,#6215,#6216,#6217,#6218,#6219,#6220,#6221,
#6222,#6223,#6224,#6225,#6226,#6227,#6228,#6229,#6230,#6231,#6232,#6233,
#6234,#6235,#6236,#6237,#6238,#6239,#6240,#6241,#6242,#6243,#6244,#6245,
#6246,#6247,#6248,#6249,#6250,#6251,#6252,#6253,#6254,#6255,#6256,#6257,
#6258,#6259,#6260,#6261,#6262,#6263,#6264,#6265,#6266,#6267,#6268,#6269,
#6270,#6271,#6272,#6273,#6274,#6275,#6276,#6277,#6278,#6279,#6280,#6281,
#6282,#6283,#6284,#6285,#6286,#6287,#6288,#6289,#6290,#6291,#6292,#6293,
#6294,#6295,#6296,#6297,#6298,#6299,#6300,#6301,#6302,#6303,#6304,#6305,
#6306,#6307,#6308,#6309,#6310,#6311,#6312,#6313,#6314,#6315,#6316,#6317,
#6318,#6319,#6320,#6321,#6322,#6323,#6324,#6325,#6326,#6327,#6328,#6329,
#6330,#6331,#6332,#6333,#6334,#6335,#6336,#6337,#6338,#6339,#6340,#6341,
#6342,#6343,#6344,#6345,#6346,#6347,#6348,#6349,#6350,#6351,#6352,#6353,
#6354,#6355,#6356,#6357,#6358,#6359,#6360,#6361,#6362,#6363,#6364,#6365,
#6366,#6367,#6368,#6369,#6370,#6371,#6372,#6373,#6374,#6375,#6376,#6377,
#6378,#6379,#6380,#6381,#6382,#6383,#6384,#6385,#6386,#6387,#6388,#6389,
#6390,#6391,#6392,#6393,#6394,#6395,#6396,#6397,#6398,#6399,#6400,#6401,
#6402,#6403,#6404,#6405,#6406,#6407,#6408,#6409,#6410,#6411,#6412,#6413,
#6414,#6415,#6416,#6417,#6418,#6419,#6420,#6421,#6422,#6423,#6424,#6425,
#6426,#6427,#6428,#6429,#6430,#6431,#6432,#6433,#6434,#6435,#6436,#6437,
#6438,#6439,#6440,#6441,#6442,#6443,#6444,#6445,#6446,#6447,#6448,#6449,
#6450,#6451,#6452,#6453,#6454,#6455,#6456,#6457,#6458,#6459,#6460,#6461,
#6462,#6463,#6464,#6465,#6466,#6467,#6468,#6469,#6470,#6471,#6472,#6473,
#6474,#6475,#6476,#6477,#6478,#6479,#6480,#6481,#6482,#6483,#6484,#6485,
#6486,#6487,#6488,#6489,#6490,#6491,#6492,#6493,#6494,#6495,#6496,#6497,
#6498,#6499,#6500,#6501,#6502,#6503,#6504,#6505,#6506,#6507,#6508,#6509,
#6510,#6511,#6512,#6513,#6514,#6515,#6516,#6517,#6518,#6519,#6520,#6521,
#6522,#6523,#6524,#6525,#6526,#6527,#6528,#6529,#6530,#6531,#6532,#6533,
#6534,#6535,#6536,#6537,#6538,#6539,#6540,#6541,#6542,#6543,#6544,#6545,
#6546,#6547,#6548,#6549,#6550,#6551,#6552,#6553,#6554,#6555,#6556,#6557,
#6558,#6559,#6560,#6561,#6562,#6563,#6564,#6565,#6566,#6567,#6568,#6569,
#6570,#6571,#6572,#6573,#6574,#6575,#6576,#6577,#6578,#6579,#6580,#6581,
#6582,#6583,#6584,#6585,#6586,#6587,#6588,#6589,#6590,#6591,#6592,#6593,
#6594,#6595,#6596,#6597,#6598,#6599,#6600,#6601,#6602,#6603,#6604,#6605,
#6606,#6607,#6608,#6609,#6610,#6611,#6612,#6613,#6614,#6615,#6616,#6617,
#6618,#6619,#6620,#6621,#6622,#6623,#6624,#6625,#6626,#6627,#6628,#6629,
#6630,#6631,#6632,#6633,#6634,#6635,#6636,#6637,#6638,#6639,#6640,#6641,
#6642,#6643,#6644,#6645,#6646,#6647,#6648,#6649,#6650,#6651,#6652,#6653,
#6654,#6655,#6656,#6657,#6658,#6659,#6660,#6661,#6662,#6663,#6664,#6665,
#6666,#6667,#6668,#6669,#6670,#6671,#6672,#6673,#6674,#6675,#6676,#6677,
#6678,#6679,#6680,#6681,#6682,#6683,#6684,#6685,#6686,#6687,#6688,#6689,
#6690,#6691,#6692,#6693,#6694,#6695,#6696,#6697,#6698,#6699,#6700,#6701,
#6702,#6703,#6704,#6705,#6706,#6707,#6708,#6709,#6710,#6711,#6712,#6713,
#6714,#6715,#6716,#6717,#6718,#6719,#6720,#6721,#6722,#6723,#6724,#6725,
#6726,#6727,#6728,#6729,#6730,#6731,#6732,#6733,#6734,#6735,#6736,#6737,
#6738,#6739,#6740,#6741,#6742,#6743,#6744,#6745,#6746,#6747,#6748,#6749,
#6750,#6751,#6752,#6753,#6754,#6755,#6756,#6757,#6758,#6759,#6760,#6761,
#6762,#6763,#6764,#6765,#6766,#6767,#6768,#6769,#6770,#6771,#6772,#6773,
#6774,#6775,#6776,#6777,#6778,#6779,#6780,#6781,#6782,#6783,#6784,#6785,
#6786,#6787,#6788,#6789,#6790,#6791,#6792,#6793,#6794,#6795,#6796,#6797,
#6798,#6799,#6800,#6801,#6802,#6803,#6804,#6805,#6806,#6807,#6808,#6809,
#6810,#6811,#6812,#6813,#6814,#6815,#6816,#6817,#6818,#6819,#6820,#6821,
#6822,#6823,#6824,#6825,#6826,#6827,#6828,#6829,#6830,#6831,#6832,#6833,
#6834,#6835,#6836,#6837,#6838,#6839,#6840,#6841,#6842,#6843,#6844,#6845,
#6846,#6847,#6848,#6849,#6850,#6851,#6852,#6853,#6854,#6855,#6856,#6857,
#6858,#6859,#6860,#6861,#6862,#6863,#6864,#6865,#6866,#6867,#6868,#6869,
#6870,#6871,#6872,#6873,#6874,#6875,#6876,#6877,#6878,#6879,#6880,#6881,
#6882,#6883,#6884,#6885,#6886,#6887,#6888,#6889,#6890,#6891,#6892,#6893,
#6894,#6895,#6896,#6897,#6898,#6899,#6900,#6901,#6902,#6903,#6904,#6905,
#6906,#6907,#6908,#6909,#6910,#6911,#6912,#6913,#6914,#6915,#6916,#6917,
#6918,#6919,#6920,#6921,#6922,#6923,#6924,#6925,#6926,#6927,#6928,#6929,
#6930,#6931,#6932,#6933,#6934,#6935,#6936,#6937,#6938,#6939,#6940,#6941,
#6942,#6943,#6944,#6945,#6946,#6947,#6948,#6949,#6950,#6951,#6952,#6953,
#6954,#6955,#6956,#6957,#6958,#6959,#6960,#6961,#6962,#6963,#6964,#6965,
#6966,#6967,#6968,#6969,#6970,#6971,#6972,#6973,#6974,#6975,#6976,#6977,
#6978,#6979,#6980,#6981,#6982,#6983,#6984,#6985,#6986,#6987,#6988,#6989,
#6990,#6991,#6992,#6993,#6994,#6995,#6996,#6997,#6998,#6999,#7000,#7001,
#7002,#7003,#7004,#7005,#7006,#7007,#7008,#7009,#7010,#7011,#7012,#7013,
#7014,#7015,#7016,#7017,#7018,#7019,#7020,#7021,#7022,#7023,#7024,#7025,
#7026,#7027,#7028,#7029,#7030,#7031,#7032,#7033,#7034,#7035,#7036,#7037,
#7038,#7039,#7040,#7041,#7042,#7043,#7044,#7045,#7046,#7047,#7048,#7049,
#7050,#7051,#7052,#7053,#7054,#7055,#7056,#7057,#7058,#7059,#7060,#7061,
#7062,#7063,#7064,#7065,#7066,#7067,#7068,#7069,#7070,#7071,#7072,#7073,
#7074,#7075,#7076,#7077,#7078,#7079,#7080,#7081,#7082,#7083,#7084,#7085,
#7086,#7087,#7088,#7089,#7090,#7091,#7092,#7093,#7094,#7095,#7096,#7097,
#7098,#7099,#7100,#7101,#7102,#7103,#7104,#7105,#7106,#7107,#7108,#7109,
#7110,#7111,#7112,#7113,#7114,#7115,#7116,#7117,#7118,#7119,#7120,#7121,
#7122,#7123,#7124,#7125,#7126,#7127,#7128,#7129,#7130,#7131,#7132,#7133,
#7134,#7135,#7136,#7137,#7138,#7139,#7140,#7141,#7142,#7143,#7144,#7145,
#7146,#7147,#7148,#7149,#7150,#7151,#7152,#7153,#7154,#7155,#7156,#7157,
#7158,#7159,#7160,#7161,#7162,#7163,#7164,#7165,#7166,#7167,#7168,#7169,
#7170,#7171,#7172,#7173,#7174,#7175,#7176,#7177,#7178,#7179,#7180,#7181,
#7182,#7183)),.UNSPECIFIED.,.F.,.F.,.F.)
B_SPLINE_SURFACE_WITH_KNOTS((2,2),(3,2,2,2,2,2,2,2,2,2,2,2,2,2,2,2,2,2,
2,2,2,2,2,2,2,2,2,2,2,2,2,2,2,2,2,2,2,2,2,2,2,2,2,2,2,2,2,2,2,2,2,2,2,2,
2,2,2,2,2,2,2,2,2,2,2,2,2,2,2,2,2,2,2,2,2,2,2,2,2,2,2,2,2,2,2,2,2,2,2,2,
2,2,2,2,2,2,2,2,2,2,2,2,2,2,2,2,2,2,2,2,2,2,2,2,2,2,2,2,2,2,2,2,2,2,2,2,
2,2,2,2,2,2,2,2,2,2,2,2,2,2,2,2,2,2,2,2,2,2,2,2,2,2,2,2,2,2,2,2,2,2,2,2,
2,2,2,2,2,2,2,2,2,2,2,2,2,2,2,2,2,2,2,2,2,2,2,2,2,2,2,2,2,2,2,2,2,2,2,2,
2,2,2,2,2,2,2,2,2,2,2,2,2,2,2,2,2,2,2,2,2,2,2,2,2,2,2,2,2,2,2,2,2,2,2,2,
2,2,2,2,2,2,2,2,2,2,2,2,2,2,2,2,2,2,2,2,2,2,2,2,2,2,2,2,2,2,2,2,2,2,2,2,
2,2,2,2,2,2,2,2,2,2,2,2,2,2,2,2,2,2,2,2,2,2,2,2,2,2,2,2,2,2,2,2,2,2,2,2,
2,2,2,2,2,2,2,2,2,2,2,2,2,2,2,2,2,2,2,2,2,2,2,2,2,2,2,2,2,2,2,2,2,2,2,2,
2,2,2,2,2,2,2,2,2,2,2,2,2,2,2,2,2,2,2,2,2,2,2,2,2,2,2,2,2,2,2,2,2,2,2,2,
2,2,2,2,2,2,2,2,2,2,2,2,2,2,2,2,2,2,2,2,2,2,2,2,2,2,2,2,2,2,2,2,2,2,2,2,
2,2,2,2,2,2,2,2,2,2,2,2,2,2,2,2,2,2,2,2,2,2,2,2,2,2,2,2,2,2,2,2,2,2,2,2,
2,2,2,2,2,2,2,2,2,2,2,2,2,2,2,2,2,2,2,2,2,2,2,2,2,2,2,2,2,2,2,2,2,2,2,2,
2,2,2,2,2,2,2,2,2,2,2,2,2,2,2,2,2,2,2,2,2,2,2,2,2,2,2,2,2,2,2,2,2,2,2,2,
2,2,2,2,2,2,2,2,2,2,2,2,2,2,2,2,2,2,2,2,2,2,2,2,2,2,2,2,2,2,2,2,2,2,2,2,
2,2,2,2,2,2,2,2,2,2,2,2,2,2,2,2,2,2,2,2,2,2,2,2,2,2,2,2,2,2,2,2,2,2,2,2,
2,2,2,2,2,2,2,2,2,2,2,2,2,2,2,2,2,2,2,2,2,2,2,2,2,2,2,2,2,2,2,2,2,2,2,2,
2,2,2,2,2,3),(0.,1.0000000013075),(0.,0.00157232704402516,0.00314465408805031,
0.00471698113207547,0.00628930817610063,0.00786163522012579,0.00943396226415094,
0.0110062893081761,0.0125786163522013,0.0141509433962264,0.0157232704402516,
0.0172955974842767,0.0188679245283019,0.020440251572327,0.0220125786163522,
0.0235849056603774,0.0251572327044025,0.0267295597484277,0.0283018867924528,
0.029874213836478,0.0314465408805031,0.0330188679245283,0.0345911949685535,
0.0361635220125786,0.0377358490566038,0.0393081761006289,0.0408805031446541,
0.0424528301886792,0.0440251572327044,0.0455974842767296,0.0471698113207547,
0.0487421383647799,0.050314465408805,0.0518867924528302,0.0534591194968553,
0.0550314465408805,0.0566037735849057,0.0581761006289308,0.059748427672956,
0.0613207547169811,0.0628930817610063,0.0644654088050314,0.0660377358490566,
0.0676100628930818,0.0691823899371069,0.0707547169811321,0.0723270440251572,
0.0738993710691824,0.0754716981132075,0.0770440251572327,0.0786163522012579,
0.080188679245283,0.0817610062893082,0.0833333333333333,0.0849056603773585,
0.0864779874213836,0.0880503144654088,0.089622641509434,0.0911949685534591,
0.0927672955974843,0.0943396226415094,0.0959119496855346,0.0974842767295598,
0.0990566037735849,0.10062893081761,0.102201257861635,0.10377358490566,
0.105345911949686,0.106918238993711,0.108490566037736,0.110062893081761,
0.111635220125786,0.113207547169811,0.114779874213836,0.116352201257862,
0.117924528301887,0.119496855345912,0.121069182389937,0.122641509433962,
0.124213836477987,0.125786163522013,0.127358490566038,0.128930817610063,
0.130503144654088,0.132075471698113,0.133647798742138,0.135220125786164,
0.136792452830189,0.138364779874214,0.139937106918239,0.141509433962264,
0.143081761006289,0.144654088050314,0.14622641509434,0.147798742138365,
0.14937106918239,0.150943396226415,0.15251572327044,0.154088050314465,0.155660377358491,
0.157232704402516,0.158805031446541,0.160377358490566,0.161949685534591,
0.163522012578616,0.165094339622642,0.166666666666667,0.168238993710692,
0.169811320754717,0.171383647798742,0.172955974842767,0.174528301886792,
0.176100628930818,0.177672955974843,0.179245283018868,0.180817610062893,
0.182389937106918,0.183962264150943,0.185534591194969,0.187106918238994,
0.188679245283019,0.190251572327044,0.191823899371069,0.193396226415094,
0.19496855345912,0.196540880503145,0.19811320754717,0.199685534591195,0.20125786163522,
0.202830188679245,0.20440251572327,0.205974842767296,0.207547169811321,
0.209119496855346,0.210691823899371,0.212264150943396,0.213836477987421,
0.215408805031447,0.216981132075472,0.218553459119497,0.220125786163522,
0.221698113207547,0.223270440251572,0.224842767295597,0.226415094339623,
0.227987421383648,0.229559748427673,0.231132075471698,0.232704402515723,
0.234276729559748,0.235849056603774,0.237421383647799,0.238993710691824,
0.240566037735849,0.242138364779874,0.243710691823899,0.245283018867925,
0.24685534591195,0.248427672955975,0.25,0.251572327044025,0.25314465408805,
0.254716981132075,0.256289308176101,0.257861635220126,0.259433962264151,
0.261006289308176,0.262578616352201,0.264150943396226,0.265723270440252,
0.267295597484277,0.268867924528302,0.270440251572327,0.272012578616352,
0.273584905660377,0.275157232704403,0.276729559748428,0.278301886792453,
0.279874213836478,0.281446540880503,0.283018867924528,0.284591194968553,
0.286163522012579,0.287735849056604,0.289308176100629,0.290880503144654,
0.292452830188679,0.294025157232704,0.29559748427673,0.297169811320755,
0.29874213836478,0.300314465408805,0.30188679245283,0.303459119496855,0.30503144654088,
0.306603773584906,0.308176100628931,0.309748427672956,0.311320754716981,
0.312893081761006,0.314465408805031,0.316037735849057,0.317610062893082,
0.319182389937107,0.320754716981132,0.322327044025157,0.323899371069182,
0.325471698113208,0.327044025157233,0.328616352201258,0.330188679245283,
0.331761006289308,0.333333333333333,0.334905660377358,0.336477987421384,
0.338050314465409,0.339622641509434,0.341194968553459,0.342767295597484,
0.344339622641509,0.345911949685535,0.34748427672956,0.349056603773585,
0.35062893081761,0.352201257861635,0.35377358490566,0.355345911949686,0.356918238993711,
0.358490566037736,0.360062893081761,0.361635220125786,0.363207547169811,
0.364779874213836,0.366352201257862,0.367924528301887,0.369496855345912,
0.371069182389937,0.372641509433962,0.374213836477987,0.375786163522013,
0.377358490566038,0.378930817610063,0.380503144654088,0.382075471698113,
0.383647798742138,0.385220125786164,0.386792452830189,0.388364779874214,
0.389937106918239,0.391509433962264,0.393081761006289,0.394654088050314,
0.39622641509434,0.397798742138365,0.39937106918239,0.400943396226415,0.40251572327044,
0.404088050314465,0.405660377358491,0.407232704402516,0.408805031446541,
0.410377358490566,0.411949685534591,0.413522012578616,0.415094339622642,
0.416666666666667,0.418238993710692,0.419811320754717,0.421383647798742,
0.422955974842767,0.424528301886792,0.426100628930818,0.427672955974843,
0.429245283018868,0.430817610062893,0.432389937106918,0.433962264150943,
0.435534591194969,0.437106918238994,0.438679245283019,0.440251572327044,
0.441823899371069,0.443396226415094,0.44496855345912,0.446540880503145,
0.44811320754717,0.449685534591195,0.45125786163522,0.452830188679245,0.45440251572327,
0.455974842767296,0.457547169811321,0.459119496855346,0.460691823899371,
0.462264150943396,0.463836477987421,0.465408805031447,0.466981132075472,
0.468553459119497,0.470125786163522,0.471698113207547,0.473270440251572,
0.474842767295597,0.476415094339623,0.477987421383648,0.479559748427673,
0.481132075471698,0.482704402515723,0.484276729559748,0.485849056603774,
0.487421383647799,0.488993710691824,0.490566037735849,0.492138364779874,
0.493710691823899,0.495283018867925,0.49685534591195,0.498427672955975,
0.5,0.501572327044025,0.50314465408805,0.504716981132076,0.506289308176101,
0.507861635220126,0.509433962264151,0.511006289308176,0.512578616352201,
0.514150943396226,0.515723270440252,0.517295597484277,0.518867924528302,
0.520440251572327,0.522012578616352,0.523584905660377,0.525157232704403,
0.526729559748428,0.528301886792453,0.529874213836478,0.531446540880503,
0.533018867924528,0.534591194968553,0.536163522012579,0.537735849056604,
0.539308176100629,0.540880503144654,0.542452830188679,0.544025157232704,
0.54559748427673,0.547169811320755,0.54874213836478,0.550314465408805,0.55188679245283,
0.553459119496855,0.555031446540881,0.556603773584906,0.558176100628931,
0.559748427672956,0.561320754716981,0.562893081761006,0.564465408805031,
0.566037735849057,0.567610062893082,0.569182389937107,0.570754716981132,
0.572327044025157,0.573899371069182,0.575471698113208,0.577044025157233,
0.578616352201258,0.580188679245283,0.581761006289308,0.583333333333333,
0.584905660377358,0.586477987421384,0.588050314465409,0.589622641509434,
0.591194968553459,0.592767295597484,0.594339622641509,0.595911949685535,
0.59748427672956,0.599056603773585,0.60062893081761,0.602201257861635,0.60377358490566,
0.605345911949686,0.606918238993711,0.608490566037736,0.610062893081761,
0.611635220125786,0.613207547169811,0.614779874213837,0.616352201257862,
0.617924528301887,0.619496855345912,0.621069182389937,0.622641509433962,
0.624213836477987,0.625786163522013,0.627358490566038,0.628930817610063,
0.630503144654088,0.632075471698113,0.633647798742138,0.635220125786163,
0.636792452830189,0.638364779874214,0.639937106918239,0.641509433962264,
0.643081761006289,0.644654088050314,0.64622641509434,0.647798742138365,
0.64937106918239,0.650943396226415,0.65251572327044,0.654088050314465,0.655660377358491,
0.657232704402516,0.658805031446541,0.660377358490566,0.661949685534591,
0.663522012578616,0.665094339622642,0.666666666666667,0.668238993710692,
0.669811320754717,0.671383647798742,0.672955974842767,0.674528301886792,
0.676100628930818,0.677672955974843,0.679245283018868,0.680817610062893,
0.682389937106918,0.683962264150943,0.685534591194969,0.687106918238994,
0.688679245283019,0.690251572327044,0.691823899371069,0.693396226415094,
0.694968553459119,0.696540880503145,0.69811320754717,0.699685534591195,
0.70125786163522,0.702830188679245,0.70440251572327,0.705974842767296,0.707547169811321,
0.709119496855346,0.710691823899371,0.712264150943396,0.713836477987421,
0.715408805031447,0.716981132075472,0.718553459119497,0.720125786163522,
0.721698113207547,0.723270440251572,0.724842767295597,0.726415094339623,
0.727987421383648,0.729559748427673,0.731132075471698,0.732704402515723,
0.734276729559748,0.735849056603774,0.737421383647799,0.738993710691824,
0.740566037735849,0.742138364779874,0.743710691823899,0.745283018867924,
0.74685534591195,0.748427672955975,0.75,0.751572327044025,0.75314465408805,
0.754716981132076,0.756289308176101,0.757861635220126,0.759433962264151,
0.761006289308176,0.762578616352201,0.764150943396226,0.765723270440252,
0.767295597484277,0.768867924528302,0.770440251572327,0.772012578616352,
0.773584905660377,0.775157232704403,0.776729559748428,0.778301886792453,
0.779874213836478,0.781446540880503,0.783018867924528,0.784591194968553,
0.786163522012579,0.787735849056604,0.789308176100629,0.790880503144654,
0.792452830188679,0.794025157232704,0.79559748427673,0.797169811320755,
0.79874213836478,0.800314465408805,0.80188679245283,0.803459119496855,0.805031446540881,
0.806603773584906,0.808176100628931,0.809748427672956,0.811320754716981,
0.812893081761006,0.814465408805031,0.816037735849057,0.817610062893082,
0.819182389937107,0.820754716981132,0.822327044025157,0.823899371069182,
0.825471698113208,0.827044025157233,0.828616352201258,0.830188679245283,
0.831761006289308,0.833333333333333,0.834905660377358,0.836477987421384,
0.838050314465409,0.839622641509434,0.841194968553459,0.842767295597484,
0.844339622641509,0.845911949685535,0.84748427672956,0.849056603773585,
0.85062893081761,0.852201257861635,0.85377358490566,0.855345911949686,0.856918238993711,
0.858490566037736,0.860062893081761,0.861635220125786,0.863207547169811,
0.864779874213837,0.866352201257862,0.867924528301887,0.869496855345912,
0.871069182389937,0.872641509433962,0.874213836477987,0.875786163522013,
0.877358490566038,0.878930817610063,0.880503144654088,0.882075471698113,
0.883647798742138,0.885220125786163,0.886792452830189,0.888364779874214,
0.889937106918239,0.891509433962264,0.893081761006289,0.894654088050314,
0.89622641509434,0.897798742138365,0.89937106918239,0.900943396226415,0.90251572327044,
0.904088050314465,0.905660377358491,0.907232704402516,0.908805031446541,
0.910377358490566,0.911949685534591,0.913522012578616,0.915094339622642,
0.916666666666667,0.918238993710692,0.919811320754717,0.921383647798742,
0.922955974842767,0.924528301886792,0.926100628930818,0.927672955974843,
0.929245283018868,0.930817610062893,0.932389937106918,0.933962264150943,
0.935534591194969,0.937106918238994,0.938679245283019,0.940251572327044,
0.941823899371069,0.943396226415094,0.944968553459119,0.946540880503145,
0.94811320754717,0.949685534591195,0.95125786163522,0.952830188679245,0.95440251572327,
0.955974842767296,0.957547169811321,0.959119496855346,0.960691823899371,
0.962264150943396,0.963836477987421,0.965408805031447,0.966981132075472,
0.968553459119497,0.970125786163522,0.971698113207547,0.973270440251572,
0.974842767295597,0.976415094339623,0.977987421383648,0.979559748427673,
0.981132075471698,0.982704402515723,0.984276729559748,0.985849056603774,
0.987421383647799,0.988993710691824,0.990566037735849,0.992138364779874,
0.993710691823899,0.995283018867924,0.99685534591195,0.997310988253444),
 .UNSPECIFIED.)
GEOMETRIC_REPRESENTATION_ITEM()
RATIONAL_B_SPLINE_SURFACE(((1.,0.866025403784439,1.,0.866025403784439,1.,
0.866025403784439,1.,0.866025403784439,1.,0.866025403784439,1.,0.866025403784439,
1.,0.866025403784439,1.,0.866025403784439,1.,0.866025403784439,1.,0.866025403784439,
1.,0.866025403784439,1.,0.866025403784439,1.,0.866025403784439,1.,0.866025403784439,
1.,0.866025403784439,1.,0.866025403784439,1.,0.866025403784439,1.,0.866025403784439,
1.,0.866025403784439,1.,0.866025403784439,1.,0.866025403784439,1.,0.866025403784439,
1.,0.866025403784439,1.,0.866025403784439,1.,0.866025403784439,1.,0.866025403784439,
1.,0.866025403784439,1.,0.866025403784439,1.,0.866025403784439,1.,0.866025403784439,
1.,0.866025403784439,1.,0.866025403784439,1.,0.866025403784439,1.,0.866025403784439,
1.,0.866025403784439,1.,0.866025403784439,1.,0.866025403784439,1.,0.866025403784439,
1.,0.866025403784439,1.,0.866025403784439,1.,0.866025403784439,1.,0.866025403784439,
1.,0.866025403784439,1.,0.866025403784439,1.,0.866025403784439,1.,0.866025403784439,
1.,0.866025403784439,1.,0.866025403784439,1.,0.866025403784439,1.,0.866025403784439,
1.,0.866025403784439,1.,0.866025403784439,1.,0.866025403784439,1.,0.866025403784439,
1.,0.866025403784439,1.,0.866025403784439,1.,0.866025403784439,1.,0.866025403784439,
1.,0.866025403784439,1.,0.866025403784439,1.,0.866025403784439,1.,0.866025403784439,
1.,0.866025403784439,1.,0.866025403784439,1.,0.866025403784439,1.,0.866025403784439,
1.,0.866025403784439,1.,0.866025403784439,1.,0.866025403784439,1.,0.866025403784439,
1.,0.866025403784439,1.,0.866025403784439,1.,0.866025403784439,1.,0.866025403784439,
1.,0.866025403784439,1.,0.866025403784439,1.,0.866025403784439,1.,0.866025403784439,
1.,0.866025403784439,1.,0.866025403784439,1.,0.866025403784439,1.,0.866025403784439,
1.,0.866025403784439,1.,0.866025403784439,1.,0.866025403784439,1.,0.866025403784439,
1.,0.866025403784439,1.,0.866025403784439,1.,0.866025403784439,1.,0.866025403784439,
1.,0.866025403784439,1.,0.866025403784439,1.,0.866025403784439,1.,0.866025403784439,
1.,0.866025403784439,1.,0.866025403784439,1.,0.866025403784439,1.,0.866025403784439,
1.,0.866025403784439,1.,0.866025403784439,1.,0.866025403784439,1.,0.866025403784439,
1.,0.866025403784439,1.,0.866025403784439,1.,0.866025403784439,1.,0.866025403784439,
1.,0.866025403784439,1.,0.866025403784439,1.,0.866025403784439,1.,0.866025403784439,
1.,0.866025403784439,1.,0.866025403784439,1.,0.866025403784439,1.,0.866025403784439,
1.,0.866025403784439,1.,0.866025403784439,1.,0.866025403784439,1.,0.866025403784439,
1.,0.866025403784439,1.,0.866025403784439,1.,0.866025403784439,1.,0.866025403784439,
1.,0.866025403784439,1.,0.866025403784439,1.,0.866025403784439,1.,0.866025403784439,
1.,0.866025403784439,1.,0.866025403784439,1.,0.866025403784439,1.,0.866025403784439,
1.,0.866025403784439,1.,0.866025403784439,1.,0.866025403784439,1.,0.866025403784439,
1.,0.866025403784439,1.,0.866025403784439,1.,0.866025403784439,1.,0.866025403784439,
1.,0.866025403784439,1.,0.866025403784439,1.,0.866025403784439,1.,0.866025403784439,
1.,0.866025403784439,1.,0.866025403784439,1.,0.866025403784439,1.,0.866025403784439,
1.,0.866025403784439,1.,0.866025403784439,1.,0.866025403784439,1.,0.866025403784439,
1.,0.866025403784439,1.,0.866025403784439,1.,0.866025403784439,1.,0.866025403784439,
1.,0.866025403784439,1.,0.866025403784439,1.,0.866025403784439,1.,0.866025403784439,
1.,0.866025403784439,1.,0.866025403784439,1.,0.866025403784439,1.,0.866025403784439,
1.,0.866025403784439,1.,0.866025403784439,1.,0.866025403784439,1.,0.866025403784439,
1.,0.866025403784439,1.,0.866025403784439,1.,0.866025403784439,1.,0.866025403784439,
1.,0.866025403784439,1.,0.866025403784439,1.,0.866025403784439,1.,0.866025403784439,
1.,0.866025403784439,1.,0.866025403784439,1.,0.866025403784439,1.,0.866025403784439,
1.,0.866025403784439,1.,0.866025403784439,1.,0.866025403784439,1.,0.866025403784439,
1.,0.866025403784439,1.,0.866025403784439,1.,0.866025403784439,1.,0.866025403784439,
1.,0.866025403784439,1.,0.866025403784439,1.,0.866025403784439,1.,0.866025403784439,
1.,0.866025403784439,1.,0.866025403784439,1.,0.866025403784439,1.,0.866025403784439,
1.,0.866025403784439,1.,0.866025403784439,1.,0.866025403784439,1.,0.866025403784439,
1.,0.866025403784439,1.,0.866025403784439,1.,0.866025403784439,1.,0.866025403784439,
1.,0.866025403784439,1.,0.866025403784439,1.,0.866025403784439,1.,0.866025403784439,
1.,0.866025403784439,1.,0.866025403784439,1.,0.866025403784439,1.,0.866025403784439,
1.,0.866025403784439,1.,0.866025403784439,1.,0.866025403784439,1.,0.866025403784439,
1.,0.866025403784439,1.,0.866025403784439,1.,0.866025403784439,1.,0.866025403784439,
1.,0.866025403784439,1.,0.866025403784439,1.,0.866025403784439,1.,0.866025403784439,
1.,0.866025403784439,1.,0.866025403784439,1.,0.866025403784439,1.,0.866025403784439,
1.,0.866025403784439,1.,0.866025403784439,1.,0.866025403784439,1.,0.866025403784439,
1.,0.866025403784439,1.,0.866025403784439,1.,0.866025403784439,1.,0.866025403784439,
1.,0.866025403784439,1.,0.866025403784439,1.,0.866025403784439,1.,0.866025403784439,
1.,0.866025403784439,1.,0.866025403784439,1.,0.866025403784439,1.,0.866025403784439,
1.,0.866025403784439,1.,0.866025403784439,1.,0.866025403784439,1.,0.866025403784439,
1.,0.866025403784439,1.,0.866025403784439,1.,0.866025403784439,1.,0.866025403784439,
1.,0.866025403784439,1.,0.866025403784439,1.,0.866025403784439,1.,0.866025403784439,
1.,0.866025403784439,1.,0.866025403784439,1.,0.866025403784439,1.,0.866025403784439,
1.,0.866025403784439,1.,0.866025403784439,1.,0.866025403784439,1.,0.866025403784439,
1.,0.866025403784439,1.,0.866025403784439,1.,0.866025403784439,1.,0.866025403784439,
1.,0.866025403784439,1.,0.866025403784439,1.,0.866025403784439,1.,0.866025403784439,
1.,0.866025403784439,1.,0.866025403784439,1.,0.866025403784439,1.,0.866025403784439,
1.,0.866025403784439,1.,0.866025403784439,1.,0.866025403784439,1.,0.866025403784439,
1.,0.866025403784439,1.,0.866025403784439,1.,0.866025403784439,1.,0.866025403784439,
1.,0.866025403784439,1.,0.866025403784439,1.,0.866025403784439,1.,0.866025403784439,
1.,0.866025403784439,1.,0.866025403784439,1.,0.866025403784439,1.,0.866025403784439,
1.,0.866025403784439,1.,0.866025403784439,1.,0.866025403784439,1.,0.866025403784439,
1.,0.866025403784439,1.,0.866025403784439,1.,0.866025403784439,1.,0.866025403784439,
1.,0.866025403784439,1.,0.866025403784439,1.,0.866025403784439,1.,0.866025403784439,
1.,0.866025403784439,1.,0.866025403784439,1.,0.866025403784439,1.,0.866025403784439,
1.,0.866025403784439,1.,0.866025403784439,1.,0.866025403784439,1.,0.866025403784439,
1.,0.866025403784439,1.,0.866025403784439,1.,0.866025403784439,1.,0.866025403784439,
1.,0.866025403784439,1.,0.866025403784439,1.,0.866025403784439,1.,0.866025403784439,
1.,0.866025403784439,1.,0.866025403784439,1.,0.866025403784439,1.,0.866025403784439,
1.,0.866025403784439,1.,0.866025403784439,1.,0.866025403784439,1.,0.866025403784439,
1.,0.866025403784439,1.,0.866025403784439,1.,0.866025403784439,1.,0.866025403784439,
1.,0.866025403784439,1.,0.866025403784439,1.,0.866025403784439,1.,0.866025403784439,
1.,0.866025403784439,1.,0.866025403784439,1.,0.866025403784439,1.,0.866025403784439,
1.,0.866025403784439,1.,0.866025403784439,1.,0.866025403784439,1.,0.866025403784439,
1.,0.866025403784439,1.,0.866025403784439,1.,0.866025403784439,1.,0.866025403784439,
1.,0.866025403784439,1.,0.866025403784439,1.,0.866025403784439,1.,0.866025403784439,
1.,0.866025403784439,1.,0.866025403784439,1.,0.866025403784439,1.,0.866025403784439,
1.,0.866025403784439,1.,0.866025403784439,1.,0.866025403784439,1.,0.866025403784439,
1.,0.866025403784439,1.,0.866025403784439,1.,0.866025403784439,1.,0.866025403784439,
1.,0.866025403784439,1.,0.866025403784439,1.,0.866025403784439,1.,0.866025403784439,
1.,0.866025403784439,1.,0.866025403784439,1.,0.866025403784439,1.,0.866025403784439,
1.,0.866025403784439,1.,0.866025403784439,1.,0.866025403784439,1.,0.866025403784439,
1.,0.866025403784439,1.,0.866025403784439,1.,0.866025403784439,1.,0.866025403784439,
1.,0.866025403784439,1.,0.866025403784439,1.,0.866025403784439,1.,0.866025403784439,
1.,0.866025403784439,1.,0.866025403784439,1.,0.866025403784439,1.,0.866025403784439,
1.,0.866025403784439,1.,0.866025403784439,1.,0.866025403784439,1.,0.866025403784439,
1.,0.866025403784439,1.,0.866025403784439,1.,0.866025403784439,1.,0.866025403784439,
1.,0.866025403784439,1.,0.866025403784439,1.,0.866025403784439,1.,0.866025403784439,
1.,0.866025403784439,1.,0.866025403784439,1.,0.866025403784439,1.,0.866025403784439,
1.,0.866025403784439,1.,0.866025403784439,1.,0.866025403784439,1.,0.866025403784439,
1.,0.866025403784439,1.,0.866025403784439,1.,0.866025403784439,1.,0.866025403784439,
1.,0.866025403784439,1.,0.866025403784439,1.,0.866025403784439,1.,0.866025403784439,
1.,0.866025403784439,1.,0.866025403784439,1.,0.866025403784439,1.,0.866025403784439,
1.,0.866025403784439,1.,0.866025403784439,1.,0.866025403784439,1.,0.866025403784439,
1.,0.866025403784439,1.,0.866025403784439,1.,0.866025403784439,1.,0.866025403784439,
1.,0.866025403784439,1.,0.866025403784439,1.,0.866025403784439,1.,0.866025403784439,
1.,0.866025403784439,1.,0.866025403784439,1.,0.866025403784439,1.,0.866025403784439,
1.,0.866025403784439,1.,0.866025403784439,1.,0.866025403784439,1.,0.866025403784439,
1.,0.866025403784439,1.,0.866025403784439,1.,0.866025403784439,1.,0.866025403784439,
1.,0.866025403784439,1.,0.866025403784439,1.,0.866025403784439,1.,0.866025403784439,
1.,0.866025403784439,1.,0.866025403784439,1.,0.866025403784439,1.,0.866025403784439,
1.,0.866025403784439,1.,0.866025403784439,1.,0.866025403784439,1.,0.866025403784439,
1.,0.866025403784439,1.,0.866025403784439,1.,0.866025403784439,1.,0.866025403784439,
1.,0.866025403784439,1.,0.866025403784439,1.,0.866025403784439,1.,0.866025403784439,
1.,0.866025403784439,1.,0.866025403784439,1.,0.866025403784439,1.,0.866025403784439,
1.,0.866025403784439,1.,0.866025403784439,1.,0.866025403784439,1.,0.866025403784439,
1.,0.866025403784439,1.,0.866025403784439,1.,0.866025403784439,1.,0.866025403784439,
1.,0.866025403784439,1.,0.866025403784439,1.,0.866025403784439,1.,0.866025403784439,
1.,0.866025403784439,1.,0.866025403784439,1.,0.866025403784439,1.,0.866025403784439,
1.,0.866025403784439,1.,0.866025403784439,1.,0.866025403784439,1.,0.866025403784439,
1.,0.866025403784439,1.,0.866025403784439,1.,0.866025403784439,1.,0.866025403784439,
1.,0.866025403784439,1.,0.866025403784439,1.,0.866025403784439,1.,0.866025403784439,
1.,0.866025403784439,1.,0.866025403784439,1.,0.866025403784439,1.,0.866025403784439,
1.,0.866025403784439,1.,0.866025403784439,1.,0.866025403784439,1.,0.866025403784439,
1.,0.866025403784439,1.,0.866025403784439,1.,0.866025403784439,1.,0.866025403784439,
1.,0.866025403784439,1.,0.866025403784439,1.,0.866025403784439,1.,0.866025403784439,
1.,0.866025403784439,1.,0.866025403784439,1.,0.866025403784439,1.,0.866025403784439,
1.,0.866025403784439,1.,0.866025403784439,1.,0.866025403784439,1.,0.866025403784439,
1.,0.866025403784439,1.,0.866025403784439,1.,0.866025403784439,1.,0.866025403784439,
1.,0.866025403784439,1.,0.866025403784439,1.,0.866025403784439,1.,0.866025403784439,
1.,0.866025403784439,1.,0.866025403784439,1.,0.866025403784439,1.,0.866025403784439,
1.,0.866025403784439,1.,0.866025403784439,1.,0.866025403784439,1.,0.866025403784439,
1.,0.866025403784439,1.,0.866025403784439,1.,0.866025403784439,1.,0.866025403784439,
1.,0.866025403784439,1.,0.866025403784439,1.,0.866025403784439,1.,0.866025403784439,
1.,0.866025403784439,1.,0.866025403784439,1.,0.866025403784439,1.,0.866025403784439,
1.,0.866025403784439,1.,0.866025403784439,1.,0.866025403784439,1.,0.866025403784439,
1.,0.866025403784439,1.,0.866025403784439,1.,0.866025403784439,1.,0.866025403784439,
1.,0.866025403784439,1.,0.866025403784439,1.,0.866025403784439,1.,0.866025403784439,
1.,0.866025403784439,1.,0.866025403784439,1.,0.866025403784439,1.,0.866025403784439,
1.,0.866025403784439,1.,0.866025403784439,1.,0.866025403784439,1.,0.866025403784439,
1.,0.866025403784439,1.,0.866025403784439,1.,0.866025403784439,1.,0.866025403784439,
1.,0.866025403784439,1.,0.866025403784439,1.,0.866025403784439,1.,0.866025403784439,
1.,0.866025403784439,1.,0.866025403784439,1.,0.866025403784439,1.,0.866025403784439,
1.,0.866025403784439,1.,0.866025403784439,1.,0.866025403784439,1.,0.866025403784439,
1.,0.866025403784439,1.,0.866025403784439,1.,0.866025403784439,1.,0.866025403784439,
1.,0.866025403784439,1.,0.866025403784439,1.,0.866025403784439,1.,0.866025403784439,
1.,0.866025403784439,1.,0.866025403784439,1.,0.866025403784439,1.,0.866025403784439,
1.,0.866025403784439,1.,0.866025403784439,1.,0.866025403784439,1.,0.866025403784439,
1.,0.866025403784439,1.,0.866025403784439,1.,0.866025403784439,1.,0.866025403784439,
1.,0.866025403784439,1.,0.866025403784439,1.,0.866025403784439,1.,0.866025403784439,
1.,0.866025403784439,1.,0.866025403784439,1.,0.866025403784439,1.,0.866025403784439,
1.,0.866025403784439,1.,0.866025403784439,1.,0.866025403784439,1.,0.866025403784439,
1.,0.866025403784439,1.,0.866025403784439,1.,0.866025403784439,1.,0.866025403784439,
1.,0.866025403784439,1.,0.866025403784439,1.,0.866025403784439,1.,0.866025403784439,
1.,0.866025403784439,1.,0.866025403784439,1.,0.866025403784439,1.,0.866025403784439,
1.,0.866025403784439,1.,0.866025403784439,1.,0.866025403784439,1.,0.866025403784439,
1.,0.866025403784439,1.,0.866025403784439,1.,0.866025403784439,1.,0.866025403784439,
1.,0.961175698813797,0.944853071902794),(1.,0.866025403784439,1.,0.866025403784439,
1.,0.866025403784439,1.,0.866025403784439,1.,0.866025403784439,1.,0.866025403784439,
1.,0.866025403784439,1.,0.866025403784439,1.,0.866025403784439,1.,0.866025403784439,
1.,0.866025403784439,1.,0.866025403784439,1.,0.866025403784439,1.,0.866025403784439,
1.,0.866025403784439,1.,0.866025403784439,1.,0.866025403784439,1.,0.866025403784439,
1.,0.866025403784439,1.,0.866025403784439,1.,0.866025403784439,1.,0.866025403784439,
1.,0.866025403784439,1.,0.866025403784439,1.,0.866025403784439,1.,0.866025403784439,
1.,0.866025403784439,1.,0.866025403784439,1.,0.866025403784439,1.,0.866025403784439,
1.,0.866025403784439,1.,0.866025403784439,1.,0.866025403784439,1.,0.866025403784439,
1.,0.866025403784439,1.,0.866025403784439,1.,0.866025403784439,1.,0.866025403784439,
1.,0.866025403784439,1.,0.866025403784439,1.,0.866025403784439,1.,0.866025403784439,
1.,0.866025403784439,1.,0.866025403784439,1.,0.866025403784439,1.,0.866025403784439,
1.,0.866025403784439,1.,0.866025403784439,1.,0.866025403784439,1.,0.866025403784439,
1.,0.866025403784439,1.,0.866025403784439,1.,0.866025403784439,1.,0.866025403784439,
1.,0.866025403784439,1.,0.866025403784439,1.,0.866025403784439,1.,0.866025403784439,
1.,0.866025403784439,1.,0.866025403784439,1.,0.866025403784439,1.,0.866025403784439,
1.,0.866025403784439,1.,0.866025403784439,1.,0.866025403784439,1.,0.866025403784439,
1.,0.866025403784439,1.,0.866025403784439,1.,0.866025403784439,1.,0.866025403784439,
1.,0.866025403784439,1.,0.866025403784439,1.,0.866025403784439,1.,0.866025403784439,
1.,0.866025403784439,1.,0.866025403784439,1.,0.866025403784439,1.,0.866025403784439,
1.,0.866025403784439,1.,0.866025403784439,1.,0.866025403784439,1.,0.866025403784439,
1.,0.866025403784439,1.,0.866025403784439,1.,0.866025403784439,1.,0.866025403784439,
1.,0.866025403784439,1.,0.866025403784439,1.,0.866025403784439,1.,0.866025403784439,
1.,0.866025403784439,1.,0.866025403784439,1.,0.866025403784439,1.,0.866025403784439,
1.,0.866025403784439,1.,0.866025403784439,1.,0.866025403784439,1.,0.866025403784439,
1.,0.866025403784439,1.,0.866025403784439,1.,0.866025403784439,1.,0.866025403784439,
1.,0.866025403784439,1.,0.866025403784439,1.,0.866025403784439,1.,0.866025403784439,
1.,0.866025403784439,1.,0.866025403784439,1.,0.866025403784439,1.,0.866025403784439,
1.,0.866025403784439,1.,0.866025403784439,1.,0.866025403784439,1.,0.866025403784439,
1.,0.866025403784439,1.,0.866025403784439,1.,0.866025403784439,1.,0.866025403784439,
1.,0.866025403784439,1.,0.866025403784439,1.,0.866025403784439,1.,0.866025403784439,
1.,0.866025403784439,1.,0.866025403784439,1.,0.866025403784439,1.,0.866025403784439,
1.,0.866025403784439,1.,0.866025403784439,1.,0.866025403784439,1.,0.866025403784439,
1.,0.866025403784439,1.,0.866025403784439,1.,0.866025403784439,1.,0.866025403784439,
1.,0.866025403784439,1.,0.866025403784439,1.,0.866025403784439,1.,0.866025403784439,
1.,0.866025403784439,1.,0.866025403784439,1.,0.866025403784439,1.,0.866025403784439,
1.,0.866025403784439,1.,0.866025403784439,1.,0.866025403784439,1.,0.866025403784439,
1.,0.866025403784439,1.,0.866025403784439,1.,0.866025403784439,1.,0.866025403784439,
1.,0.866025403784439,1.,0.866025403784439,1.,0.866025403784439,1.,0.866025403784439,
1.,0.866025403784439,1.,0.866025403784439,1.,0.866025403784439,1.,0.866025403784439,
1.,0.866025403784439,1.,0.866025403784439,1.,0.866025403784439,1.,0.866025403784439,
1.,0.866025403784439,1.,0.866025403784439,1.,0.866025403784439,1.,0.866025403784439,
1.,0.866025403784439,1.,0.866025403784439,1.,0.866025403784439,1.,0.866025403784439,
1.,0.866025403784439,1.,0.866025403784439,1.,0.866025403784439,1.,0.866025403784439,
1.,0.866025403784439,1.,0.866025403784439,1.,0.866025403784439,1.,0.866025403784439,
1.,0.866025403784439,1.,0.866025403784439,1.,0.866025403784439,1.,0.866025403784439,
1.,0.866025403784439,1.,0.866025403784439,1.,0.866025403784439,1.,0.866025403784439,
1.,0.866025403784439,1.,0.866025403784439,1.,0.866025403784439,1.,0.866025403784439,
1.,0.866025403784439,1.,0.866025403784439,1.,0.866025403784439,1.,0.866025403784439,
1.,0.866025403784439,1.,0.866025403784439,1.,0.866025403784439,1.,0.866025403784439,
1.,0.866025403784439,1.,0.866025403784439,1.,0.866025403784439,1.,0.866025403784439,
1.,0.866025403784439,1.,0.866025403784439,1.,0.866025403784439,1.,0.866025403784439,
1.,0.866025403784439,1.,0.866025403784439,1.,0.866025403784439,1.,0.866025403784439,
1.,0.866025403784439,1.,0.866025403784439,1.,0.866025403784439,1.,0.866025403784439,
1.,0.866025403784439,1.,0.866025403784439,1.,0.866025403784439,1.,0.866025403784439,
1.,0.866025403784439,1.,0.866025403784439,1.,0.866025403784439,1.,0.866025403784439,
1.,0.866025403784439,1.,0.866025403784439,1.,0.866025403784439,1.,0.866025403784439,
1.,0.866025403784439,1.,0.866025403784439,1.,0.866025403784439,1.,0.866025403784439,
1.,0.866025403784439,1.,0.866025403784439,1.,0.866025403784439,1.,0.866025403784439,
1.,0.866025403784439,1.,0.866025403784439,1.,0.866025403784439,1.,0.866025403784439,
1.,0.866025403784439,1.,0.866025403784439,1.,0.866025403784439,1.,0.866025403784439,
1.,0.866025403784439,1.,0.866025403784439,1.,0.866025403784439,1.,0.866025403784439,
1.,0.866025403784439,1.,0.866025403784439,1.,0.866025403784439,1.,0.866025403784439,
1.,0.866025403784439,1.,0.866025403784439,1.,0.866025403784439,1.,0.866025403784439,
1.,0.866025403784439,1.,0.866025403784439,1.,0.866025403784439,1.,0.866025403784439,
1.,0.866025403784439,1.,0.866025403784439,1.,0.866025403784439,1.,0.866025403784439,
1.,0.866025403784439,1.,0.866025403784439,1.,0.866025403784439,1.,0.866025403784439,
1.,0.866025403784439,1.,0.866025403784439,1.,0.866025403784439,1.,0.866025403784439,
1.,0.866025403784439,1.,0.866025403784439,1.,0.866025403784439,1.,0.866025403784439,
1.,0.866025403784439,1.,0.866025403784439,1.,0.866025403784439,1.,0.866025403784439,
1.,0.866025403784439,1.,0.866025403784439,1.,0.866025403784439,1.,0.866025403784439,
1.,0.866025403784439,1.,0.866025403784439,1.,0.866025403784439,1.,0.866025403784439,
1.,0.866025403784439,1.,0.866025403784439,1.,0.866025403784439,1.,0.866025403784439,
1.,0.866025403784439,1.,0.866025403784439,1.,0.866025403784439,1.,0.866025403784439,
1.,0.866025403784439,1.,0.866025403784439,1.,0.866025403784439,1.,0.866025403784439,
1.,0.866025403784439,1.,0.866025403784439,1.,0.866025403784439,1.,0.866025403784439,
1.,0.866025403784439,1.,0.866025403784439,1.,0.866025403784439,1.,0.866025403784439,
1.,0.866025403784439,1.,0.866025403784439,1.,0.866025403784439,1.,0.866025403784439,
1.,0.866025403784439,1.,0.866025403784439,1.,0.866025403784439,1.,0.866025403784439,
1.,0.866025403784439,1.,0.866025403784439,1.,0.866025403784439,1.,0.866025403784439,
1.,0.866025403784439,1.,0.866025403784439,1.,0.866025403784439,1.,0.866025403784439,
1.,0.866025403784439,1.,0.866025403784439,1.,0.866025403784439,1.,0.866025403784439,
1.,0.866025403784439,1.,0.866025403784439,1.,0.866025403784439,1.,0.866025403784439,
1.,0.866025403784439,1.,0.866025403784439,1.,0.866025403784439,1.,0.866025403784439,
1.,0.866025403784439,1.,0.866025403784439,1.,0.866025403784439,1.,0.866025403784439,
1.,0.866025403784439,1.,0.866025403784439,1.,0.866025403784439,1.,0.866025403784439,
1.,0.866025403784439,1.,0.866025403784439,1.,0.866025403784439,1.,0.866025403784439,
1.,0.866025403784439,1.,0.866025403784439,1.,0.866025403784439,1.,0.866025403784439,
1.,0.866025403784439,1.,0.866025403784439,1.,0.866025403784439,1.,0.866025403784439,
1.,0.866025403784439,1.,0.866025403784439,1.,0.866025403784439,1.,0.866025403784439,
1.,0.866025403784439,1.,0.866025403784439,1.,0.866025403784439,1.,0.866025403784439,
1.,0.866025403784439,1.,0.866025403784439,1.,0.866025403784439,1.,0.866025403784439,
1.,0.866025403784439,1.,0.866025403784439,1.,0.866025403784439,1.,0.866025403784439,
1.,0.866025403784439,1.,0.866025403784439,1.,0.866025403784439,1.,0.866025403784439,
1.,0.866025403784439,1.,0.866025403784439,1.,0.866025403784439,1.,0.866025403784439,
1.,0.866025403784439,1.,0.866025403784439,1.,0.866025403784439,1.,0.866025403784439,
1.,0.866025403784439,1.,0.866025403784439,1.,0.866025403784439,1.,0.866025403784439,
1.,0.866025403784439,1.,0.866025403784439,1.,0.866025403784439,1.,0.866025403784439,
1.,0.866025403784439,1.,0.866025403784439,1.,0.866025403784439,1.,0.866025403784439,
1.,0.866025403784439,1.,0.866025403784439,1.,0.866025403784439,1.,0.866025403784439,
1.,0.866025403784439,1.,0.866025403784439,1.,0.866025403784439,1.,0.866025403784439,
1.,0.866025403784439,1.,0.866025403784439,1.,0.866025403784439,1.,0.866025403784439,
1.,0.866025403784439,1.,0.866025403784439,1.,0.866025403784439,1.,0.866025403784439,
1.,0.866025403784439,1.,0.866025403784439,1.,0.866025403784439,1.,0.866025403784439,
1.,0.866025403784439,1.,0.866025403784439,1.,0.866025403784439,1.,0.866025403784439,
1.,0.866025403784439,1.,0.866025403784439,1.,0.866025403784439,1.,0.866025403784439,
1.,0.866025403784439,1.,0.866025403784439,1.,0.866025403784439,1.,0.866025403784439,
1.,0.866025403784439,1.,0.866025403784439,1.,0.866025403784439,1.,0.866025403784439,
1.,0.866025403784439,1.,0.866025403784439,1.,0.866025403784439,1.,0.866025403784439,
1.,0.866025403784439,1.,0.866025403784439,1.,0.866025403784439,1.,0.866025403784439,
1.,0.866025403784439,1.,0.866025403784439,1.,0.866025403784439,1.,0.866025403784439,
1.,0.866025403784439,1.,0.866025403784439,1.,0.866025403784439,1.,0.866025403784439,
1.,0.866025403784439,1.,0.866025403784439,1.,0.866025403784439,1.,0.866025403784439,
1.,0.866025403784439,1.,0.866025403784439,1.,0.866025403784439,1.,0.866025403784439,
1.,0.866025403784439,1.,0.866025403784439,1.,0.866025403784439,1.,0.866025403784439,
1.,0.866025403784439,1.,0.866025403784439,1.,0.866025403784439,1.,0.866025403784439,
1.,0.866025403784439,1.,0.866025403784439,1.,0.866025403784439,1.,0.866025403784439,
1.,0.866025403784439,1.,0.866025403784439,1.,0.866025403784439,1.,0.866025403784439,
1.,0.866025403784439,1.,0.866025403784439,1.,0.866025403784439,1.,0.866025403784439,
1.,0.866025403784439,1.,0.866025403784439,1.,0.866025403784439,1.,0.866025403784439,
1.,0.866025403784439,1.,0.866025403784439,1.,0.866025403784439,1.,0.866025403784439,
1.,0.866025403784439,1.,0.866025403784439,1.,0.866025403784439,1.,0.866025403784439,
1.,0.866025403784439,1.,0.866025403784439,1.,0.866025403784439,1.,0.866025403784439,
1.,0.866025403784439,1.,0.866025403784439,1.,0.866025403784439,1.,0.866025403784439,
1.,0.866025403784439,1.,0.866025403784439,1.,0.866025403784439,1.,0.866025403784439,
1.,0.866025403784439,1.,0.866025403784439,1.,0.866025403784439,1.,0.866025403784439,
1.,0.866025403784439,1.,0.866025403784439,1.,0.866025403784439,1.,0.866025403784439,
1.,0.866025403784439,1.,0.866025403784439,1.,0.866025403784439,1.,0.866025403784439,
1.,0.866025403784439,1.,0.866025403784439,1.,0.866025403784439,1.,0.866025403784439,
1.,0.866025403784439,1.,0.866025403784439,1.,0.866025403784439,1.,0.866025403784439,
1.,0.866025403784439,1.,0.866025403784439,1.,0.866025403784439,1.,0.866025403784439,
1.,0.866025403784439,1.,0.866025403784439,1.,0.866025403784439,1.,0.866025403784439,
1.,0.866025403784439,1.,0.866025403784439,1.,0.866025403784439,1.,0.866025403784439,
1.,0.866025403784439,1.,0.866025403784439,1.,0.866025403784439,1.,0.866025403784439,
1.,0.866025403784439,1.,0.866025403784439,1.,0.866025403784439,1.,0.866025403784439,
1.,0.866025403784439,1.,0.866025403784439,1.,0.866025403784439,1.,0.866025403784439,
1.,0.866025403784439,1.,0.866025403784439,1.,0.866025403784439,1.,0.866025403784439,
1.,0.866025403784439,1.,0.866025403784439,1.,0.866025403784439,1.,0.866025403784439,
1.,0.866025403784439,1.,0.866025403784439,1.,0.866025403784439,1.,0.866025403784439,
1.,0.866025403784439,1.,0.866025403784439,1.,0.866025403784439,1.,0.866025403784439,
1.,0.866025403784439,1.,0.866025403784439,1.,0.866025403784439,1.,0.866025403784439,
1.,0.866025403784439,1.,0.866025403784439,1.,0.866025403784439,1.,0.866025403784439,
1.,0.866025403784439,1.,0.866025403784439,1.,0.866025403784439,1.,0.866025403784439,
1.,0.866025403784439,1.,0.866025403784439,1.,0.866025403784439,1.,0.866025403784439,
1.,0.866025403784439,1.,0.866025403784439,1.,0.866025403784439,1.,0.866025403784439,
1.,0.866025403784439,1.,0.866025403784439,1.,0.866025403784439,1.,0.866025403784439,
1.,0.866025403784439,1.,0.866025403784439,1.,0.866025403784439,1.,0.866025403784439,
1.,0.866025403784439,1.,0.866025403784439,1.,0.866025403784439,1.,0.866025403784439,
1.,0.866025403784439,1.,0.866025403784439,1.,0.866025403784439,1.,0.866025403784439,
1.,0.866025403784439,1.,0.866025403784439,1.,0.866025403784439,1.,0.866025403784439,
1.,0.866025403784439,1.,0.866025403784439,1.,0.866025403784439,1.,0.866025403784439,
1.,0.866025403784439,1.,0.866025403784439,1.,0.866025403784439,1.,0.866025403784439,
1.,0.866025403784439,1.,0.866025403784439,1.,0.866025403784439,1.,0.866025403784439,
1.,0.866025403784439,1.,0.866025403784439,1.,0.866025403784439,1.,0.866025403784439,
1.,0.866025403784439,1.,0.866025403784439,1.,0.866025403784439,1.,0.866025403784439,
1.,0.866025403784439,1.,0.866025403784439,1.,0.866025403784439,1.,0.866025403784439,
1.,0.866025403784439,1.,0.866025403784439,1.,0.866025403784439,1.,0.866025403784439,
1.,0.866025403784439,1.,0.866025403784439,1.,0.866025403784439,1.,0.866025403784439,
1.,0.866025403784439,1.,0.866025403784439,1.,0.866025403784439,1.,0.866025403784439,
1.,0.961175698813797,0.944853071902794)))
REPRESENTATION_ITEM('')
SURFACE()
);
#64=(
BOUNDED_SURFACE()
B_SPLINE_SURFACE(1,2,((#7227,#7228,#7229,#7230,#7231,#7232,#7233,#7234,
#7235,#7236,#7237,#7238,#7239,#7240,#7241,#7242,#7243,#7244,#7245,#7246,
#7247,#7248,#7249,#7250,#7251,#7252,#7253,#7254,#7255,#7256,#7257,#7258,
#7259,#7260,#7261,#7262,#7263,#7264,#7265,#7266,#7267,#7268,#7269,#7270,
#7271,#7272,#7273,#7274,#7275,#7276,#7277,#7278,#7279,#7280,#7281,#7282,
#7283,#7284,#7285,#7286,#7287,#7288,#7289,#7290,#7291,#7292,#7293,#7294,
#7295,#7296,#7297,#7298,#7299,#7300,#7301,#7302,#7303,#7304,#7305,#7306,
#7307,#7308,#7309,#7310,#7311,#7312,#7313,#7314,#7315,#7316,#7317,#7318,
#7319,#7320,#7321,#7322,#7323,#7324,#7325,#7326,#7327,#7328,#7329,#7330,
#7331,#7332,#7333,#7334,#7335,#7336,#7337,#7338,#7339,#7340,#7341,#7342,
#7343,#7344,#7345,#7346,#7347,#7348,#7349,#7350,#7351,#7352,#7353,#7354,
#7355,#7356,#7357,#7358,#7359,#7360,#7361,#7362,#7363,#7364,#7365,#7366,
#7367,#7368,#7369,#7370,#7371,#7372,#7373,#7374,#7375,#7376,#7377,#7378,
#7379,#7380,#7381,#7382,#7383,#7384,#7385,#7386,#7387,#7388,#7389,#7390,
#7391,#7392,#7393,#7394,#7395,#7396,#7397,#7398,#7399,#7400,#7401,#7402,
#7403,#7404,#7405,#7406,#7407,#7408,#7409,#7410,#7411,#7412,#7413,#7414,
#7415,#7416,#7417,#7418,#7419,#7420,#7421,#7422,#7423,#7424,#7425,#7426,
#7427,#7428,#7429,#7430,#7431,#7432,#7433,#7434,#7435,#7436,#7437,#7438,
#7439,#7440,#7441,#7442,#7443,#7444,#7445,#7446,#7447,#7448,#7449,#7450,
#7451,#7452,#7453,#7454,#7455,#7456,#7457,#7458,#7459,#7460,#7461,#7462,
#7463,#7464,#7465,#7466,#7467,#7468,#7469,#7470,#7471,#7472,#7473,#7474,
#7475,#7476,#7477,#7478,#7479,#7480,#7481,#7482,#7483,#7484,#7485,#7486,
#7487,#7488,#7489,#7490,#7491,#7492,#7493,#7494,#7495,#7496,#7497,#7498,
#7499,#7500,#7501,#7502,#7503,#7504,#7505,#7506,#7507,#7508,#7509,#7510,
#7511,#7512,#7513,#7514,#7515,#7516,#7517,#7518,#7519,#7520,#7521,#7522,
#7523,#7524,#7525,#7526,#7527,#7528,#7529,#7530,#7531,#7532,#7533,#7534,
#7535,#7536,#7537,#7538,#7539,#7540,#7541,#7542,#7543,#7544,#7545,#7546,
#7547,#7548,#7549,#7550,#7551,#7552,#7553,#7554,#7555,#7556,#7557,#7558,
#7559,#7560,#7561,#7562,#7563,#7564,#7565,#7566,#7567,#7568,#7569,#7570,
#7571,#7572,#7573,#7574,#7575,#7576,#7577,#7578,#7579,#7580,#7581,#7582,
#7583,#7584,#7585,#7586,#7587,#7588,#7589,#7590,#7591,#7592,#7593,#7594,
#7595,#7596,#7597,#7598,#7599,#7600,#7601,#7602,#7603,#7604,#7605,#7606,
#7607,#7608,#7609,#7610,#7611,#7612,#7613,#7614,#7615,#7616,#7617,#7618,
#7619,#7620,#7621,#7622,#7623,#7624,#7625,#7626,#7627,#7628,#7629,#7630,
#7631,#7632,#7633,#7634,#7635,#7636,#7637,#7638,#7639,#7640,#7641,#7642,
#7643,#7644,#7645,#7646,#7647,#7648,#7649,#7650,#7651,#7652,#7653,#7654,
#7655,#7656,#7657,#7658,#7659,#7660,#7661,#7662,#7663,#7664,#7665,#7666,
#7667,#7668,#7669,#7670,#7671,#7672,#7673,#7674,#7675,#7676,#7677,#7678,
#7679,#7680,#7681,#7682,#7683,#7684,#7685,#7686,#7687,#7688,#7689,#7690,
#7691,#7692,#7693,#7694,#7695,#7696,#7697,#7698,#7699,#7700,#7701,#7702,
#7703,#7704,#7705,#7706,#7707,#7708,#7709,#7710,#7711,#7712,#7713,#7714,
#7715,#7716,#7717,#7718,#7719,#7720,#7721,#7722,#7723,#7724,#7725,#7726,
#7727,#7728,#7729,#7730,#7731,#7732,#7733,#7734,#7735,#7736,#7737,#7738,
#7739,#7740,#7741,#7742,#7743,#7744,#7745,#7746,#7747,#7748,#7749,#7750,
#7751,#7752,#7753,#7754,#7755,#7756,#7757,#7758,#7759,#7760,#7761,#7762,
#7763,#7764,#7765,#7766,#7767,#7768,#7769,#7770,#7771,#7772,#7773,#7774,
#7775,#7776,#7777,#7778,#7779,#7780,#7781,#7782,#7783,#7784,#7785,#7786,
#7787,#7788,#7789,#7790,#7791,#7792,#7793,#7794,#7795,#7796,#7797,#7798,
#7799,#7800,#7801,#7802,#7803,#7804,#7805,#7806,#7807,#7808,#7809,#7810,
#7811,#7812,#7813,#7814,#7815,#7816,#7817,#7818,#7819,#7820,#7821,#7822,
#7823,#7824,#7825,#7826,#7827,#7828,#7829,#7830,#7831,#7832,#7833,#7834,
#7835,#7836,#7837,#7838,#7839,#7840,#7841,#7842,#7843,#7844,#7845,#7846,
#7847,#7848,#7849,#7850,#7851,#7852,#7853,#7854,#7855,#7856,#7857,#7858,
#7859,#7860,#7861,#7862,#7863,#7864,#7865,#7866,#7867,#7868,#7869,#7870,
#7871,#7872,#7873,#7874,#7875,#7876,#7877,#7878,#7879,#7880,#7881,#7882,
#7883,#7884,#7885,#7886,#7887,#7888,#7889,#7890,#7891,#7892,#7893,#7894,
#7895,#7896,#7897,#7898,#7899,#7900,#7901,#7902,#7903,#7904,#7905,#7906,
#7907,#7908,#7909,#7910,#7911,#7912,#7913,#7914,#7915,#7916,#7917,#7918,
#7919,#7920,#7921,#7922,#7923,#7924,#7925,#7926,#7927,#7928,#7929,#7930,
#7931,#7932,#7933,#7934,#7935,#7936,#7937,#7938,#7939,#7940,#7941,#7942,
#7943,#7944,#7945,#7946,#7947,#7948,#7949,#7950,#7951,#7952,#7953,#7954,
#7955,#7956,#7957,#7958,#7959,#7960,#7961,#7962,#7963,#7964,#7965,#7966,
#7967,#7968,#7969,#7970,#7971,#7972,#7973,#7974,#7975,#7976,#7977,#7978,
#7979,#7980,#7981,#7982,#7983,#7984,#7985,#7986,#7987,#7988,#7989,#7990,
#7991,#7992,#7993,#7994,#7995,#7996,#7997,#7998,#7999,#8000,#8001,#8002,
#8003,#8004,#8005,#8006,#8007,#8008,#8009,#8010,#8011,#8012,#8013,#8014,
#8015,#8016,#8017,#8018,#8019,#8020,#8021,#8022,#8023,#8024,#8025,#8026,
#8027,#8028,#8029,#8030,#8031,#8032,#8033,#8034,#8035,#8036,#8037,#8038,
#8039,#8040,#8041,#8042,#8043,#8044,#8045,#8046,#8047,#8048,#8049,#8050,
#8051,#8052,#8053,#8054,#8055,#8056,#8057,#8058,#8059,#8060,#8061,#8062,
#8063,#8064,#8065,#8066,#8067,#8068,#8069,#8070,#8071,#8072,#8073,#8074,
#8075,#8076,#8077,#8078,#8079,#8080,#8081,#8082,#8083,#8084,#8085,#8086,
#8087,#8088,#8089,#8090,#8091,#8092,#8093,#8094,#8095,#8096,#8097,#8098,
#8099,#8100,#8101,#8102,#8103,#8104,#8105,#8106,#8107,#8108,#8109,#8110,
#8111,#8112,#8113,#8114,#8115,#8116,#8117,#8118,#8119,#8120,#8121,#8122,
#8123,#8124,#8125,#8126,#8127,#8128,#8129,#8130,#8131,#8132,#8133,#8134,
#8135,#8136,#8137,#8138,#8139,#8140,#8141,#8142,#8143,#8144,#8145,#8146,
#8147,#8148,#8149,#8150,#8151,#8152,#8153,#8154,#8155,#8156,#8157,#8158,
#8159,#8160,#8161,#8162,#8163,#8164,#8165,#8166,#8167,#8168,#8169,#8170,
#8171,#8172,#8173,#8174,#8175,#8176,#8177,#8178,#8179,#8180,#8181,#8182,
#8183,#8184,#8185,#8186,#8187,#8188,#8189,#8190,#8191,#8192,#8193,#8194,
#8195,#8196,#8197,#8198,#8199,#8200,#8201,#8202,#8203,#8204,#8205,#8206,
#8207,#8208,#8209,#8210,#8211,#8212,#8213,#8214,#8215,#8216,#8217,#8218,
#8219,#8220,#8221,#8222,#8223,#8224,#8225,#8226,#8227,#8228,#8229,#8230,
#8231,#8232,#8233,#8234,#8235,#8236,#8237,#8238,#8239,#8240,#8241,#8242,
#8243,#8244,#8245,#8246,#8247,#8248,#8249,#8250,#8251,#8252,#8253,#8254,
#8255,#8256,#8257,#8258,#8259,#8260,#8261,#8262,#8263,#8264,#8265,#8266,
#8267,#8268,#8269,#8270,#8271,#8272,#8273,#8274,#8275,#8276,#8277,#8278,
#8279,#8280,#8281,#8282,#8283,#8284,#8285,#8286,#8287,#8288,#8289,#8290,
#8291,#8292,#8293,#8294,#8295,#8296,#8297,#8298,#8299,#8300,#8301,#8302,
#8303,#8304,#8305,#8306,#8307,#8308,#8309,#8310,#8311,#8312,#8313,#8314,
#8315,#8316,#8317,#8318,#8319,#8320,#8321,#8322,#8323,#8324,#8325,#8326,
#8327,#8328,#8329,#8330,#8331,#8332,#8333,#8334,#8335,#8336,#8337,#8338,
#8339,#8340,#8341,#8342,#8343,#8344,#8345,#8346,#8347,#8348,#8349,#8350,
#8351,#8352,#8353,#8354,#8355,#8356,#8357,#8358,#8359,#8360,#8361,#8362,
#8363,#8364,#8365,#8366,#8367,#8368,#8369,#8370,#8371,#8372,#8373,#8374,
#8375,#8376,#8377,#8378,#8379,#8380,#8381,#8382,#8383,#8384,#8385,#8386,
#8387,#8388,#8389,#8390,#8391,#8392,#8393,#8394,#8395,#8396,#8397,#8398,
#8399,#8400,#8401,#8402,#8403,#8404,#8405,#8406,#8407,#8408,#8409,#8410,
#8411,#8412,#8413,#8414,#8415,#8416,#8417,#8418,#8419,#8420,#8421,#8422,
#8423,#8424,#8425,#8426,#8427,#8428,#8429,#8430,#8431,#8432,#8433,#8434,
#8435,#8436,#8437,#8438,#8439,#8440,#8441,#8442,#8443,#8444,#8445,#8446,
#8447,#8448,#8449,#8450,#8451,#8452,#8453,#8454,#8455,#8456,#8457,#8458,
#8459,#8460,#8461,#8462,#8463,#8464,#8465,#8466,#8467,#8468,#8469,#8470,
#8471,#8472,#8473,#8474,#8475,#8476,#8477,#8478,#8479,#8480,#8481,#8482,
#8483,#8484,#8485,#8486,#8487,#8488,#8489,#8490,#8491,#8492,#8493,#8494,
#8495,#8496,#8497),(#8498,#8499,#8500,#8501,#8502,#8503,#8504,#8505,#8506,
#8507,#8508,#8509,#8510,#8511,#8512,#8513,#8514,#8515,#8516,#8517,#8518,
#8519,#8520,#8521,#8522,#8523,#8524,#8525,#8526,#8527,#8528,#8529,#8530,
#8531,#8532,#8533,#8534,#8535,#8536,#8537,#8538,#8539,#8540,#8541,#8542,
#8543,#8544,#8545,#8546,#8547,#8548,#8549,#8550,#8551,#8552,#8553,#8554,
#8555,#8556,#8557,#8558,#8559,#8560,#8561,#8562,#8563,#8564,#8565,#8566,
#8567,#8568,#8569,#8570,#8571,#8572,#8573,#8574,#8575,#8576,#8577,#8578,
#8579,#8580,#8581,#8582,#8583,#8584,#8585,#8586,#8587,#8588,#8589,#8590,
#8591,#8592,#8593,#8594,#8595,#8596,#8597,#8598,#8599,#8600,#8601,#8602,
#8603,#8604,#8605,#8606,#8607,#8608,#8609,#8610,#8611,#8612,#8613,#8614,
#8615,#8616,#8617,#8618,#8619,#8620,#8621,#8622,#8623,#8624,#8625,#8626,
#8627,#8628,#8629,#8630,#8631,#8632,#8633,#8634,#8635,#8636,#8637,#8638,
#8639,#8640,#8641,#8642,#8643,#8644,#8645,#8646,#8647,#8648,#8649,#8650,
#8651,#8652,#8653,#8654,#8655,#8656,#8657,#8658,#8659,#8660,#8661,#8662,
#8663,#8664,#8665,#8666,#8667,#8668,#8669,#8670,#8671,#8672,#8673,#8674,
#8675,#8676,#8677,#8678,#8679,#8680,#8681,#8682,#8683,#8684,#8685,#8686,
#8687,#8688,#8689,#8690,#8691,#8692,#8693,#8694,#8695,#8696,#8697,#8698,
#8699,#8700,#8701,#8702,#8703,#8704,#8705,#8706,#8707,#8708,#8709,#8710,
#8711,#8712,#8713,#8714,#8715,#8716,#8717,#8718,#8719,#8720,#8721,#8722,
#8723,#8724,#8725,#8726,#8727,#8728,#8729,#8730,#8731,#8732,#8733,#8734,
#8735,#8736,#8737,#8738,#8739,#8740,#8741,#8742,#8743,#8744,#8745,#8746,
#8747,#8748,#8749,#8750,#8751,#8752,#8753,#8754,#8755,#8756,#8757,#8758,
#8759,#8760,#8761,#8762,#8763,#8764,#8765,#8766,#8767,#8768,#8769,#8770,
#8771,#8772,#8773,#8774,#8775,#8776,#8777,#8778,#8779,#8780,#8781,#8782,
#8783,#8784,#8785,#8786,#8787,#8788,#8789,#8790,#8791,#8792,#8793,#8794,
#8795,#8796,#8797,#8798,#8799,#8800,#8801,#8802,#8803,#8804,#8805,#8806,
#8807,#8808,#8809,#8810,#8811,#8812,#8813,#8814,#8815,#8816,#8817,#8818,
#8819,#8820,#8821,#8822,#8823,#8824,#8825,#8826,#8827,#8828,#8829,#8830,
#8831,#8832,#8833,#8834,#8835,#8836,#8837,#8838,#8839,#8840,#8841,#8842,
#8843,#8844,#8845,#8846,#8847,#8848,#8849,#8850,#8851,#8852,#8853,#8854,
#8855,#8856,#8857,#8858,#8859,#8860,#8861,#8862,#8863,#8864,#8865,#8866,
#8867,#8868,#8869,#8870,#8871,#8872,#8873,#8874,#8875,#8876,#8877,#8878,
#8879,#8880,#8881,#8882,#8883,#8884,#8885,#8886,#8887,#8888,#8889,#8890,
#8891,#8892,#8893,#8894,#8895,#8896,#8897,#8898,#8899,#8900,#8901,#8902,
#8903,#8904,#8905,#8906,#8907,#8908,#8909,#8910,#8911,#8912,#8913,#8914,
#8915,#8916,#8917,#8918,#8919,#8920,#8921,#8922,#8923,#8924,#8925,#8926,
#8927,#8928,#8929,#8930,#8931,#8932,#8933,#8934,#8935,#8936,#8937,#8938,
#8939,#8940,#8941,#8942,#8943,#8944,#8945,#8946,#8947,#8948,#8949,#8950,
#8951,#8952,#8953,#8954,#8955,#8956,#8957,#8958,#8959,#8960,#8961,#8962,
#8963,#8964,#8965,#8966,#8967,#8968,#8969,#8970,#8971,#8972,#8973,#8974,
#8975,#8976,#8977,#8978,#8979,#8980,#8981,#8982,#8983,#8984,#8985,#8986,
#8987,#8988,#8989,#8990,#8991,#8992,#8993,#8994,#8995,#8996,#8997,#8998,
#8999,#9000,#9001,#9002,#9003,#9004,#9005,#9006,#9007,#9008,#9009,#9010,
#9011,#9012,#9013,#9014,#9015,#9016,#9017,#9018,#9019,#9020,#9021,#9022,
#9023,#9024,#9025,#9026,#9027,#9028,#9029,#9030,#9031,#9032,#9033,#9034,
#9035,#9036,#9037,#9038,#9039,#9040,#9041,#9042,#9043,#9044,#9045,#9046,
#9047,#9048,#9049,#9050,#9051,#9052,#9053,#9054,#9055,#9056,#9057,#9058,
#9059,#9060,#9061,#9062,#9063,#9064,#9065,#9066,#9067,#9068,#9069,#9070,
#9071,#9072,#9073,#9074,#9075,#9076,#9077,#9078,#9079,#9080,#9081,#9082,
#9083,#9084,#9085,#9086,#9087,#9088,#9089,#9090,#9091,#9092,#9093,#9094,
#9095,#9096,#9097,#9098,#9099,#9100,#9101,#9102,#9103,#9104,#9105,#9106,
#9107,#9108,#9109,#9110,#9111,#9112,#9113,#9114,#9115,#9116,#9117,#9118,
#9119,#9120,#9121,#9122,#9123,#9124,#9125,#9126,#9127,#9128,#9129,#9130,
#9131,#9132,#9133,#9134,#9135,#9136,#9137,#9138,#9139,#9140,#9141,#9142,
#9143,#9144,#9145,#9146,#9147,#9148,#9149,#9150,#9151,#9152,#9153,#9154,
#9155,#9156,#9157,#9158,#9159,#9160,#9161,#9162,#9163,#9164,#9165,#9166,
#9167,#9168,#9169,#9170,#9171,#9172,#9173,#9174,#9175,#9176,#9177,#9178,
#9179,#9180,#9181,#9182,#9183,#9184,#9185,#9186,#9187,#9188,#9189,#9190,
#9191,#9192,#9193,#9194,#9195,#9196,#9197,#9198,#9199,#9200,#9201,#9202,
#9203,#9204,#9205,#9206,#9207,#9208,#9209,#9210,#9211,#9212,#9213,#9214,
#9215,#9216,#9217,#9218,#9219,#9220,#9221,#9222,#9223,#9224,#9225,#9226,
#9227,#9228,#9229,#9230,#9231,#9232,#9233,#9234,#9235,#9236,#9237,#9238,
#9239,#9240,#9241,#9242,#9243,#9244,#9245,#9246,#9247,#9248,#9249,#9250,
#9251,#9252,#9253,#9254,#9255,#9256,#9257,#9258,#9259,#9260,#9261,#9262,
#9263,#9264,#9265,#9266,#9267,#9268,#9269,#9270,#9271,#9272,#9273,#9274,
#9275,#9276,#9277,#9278,#9279,#9280,#9281,#9282,#9283,#9284,#9285,#9286,
#9287,#9288,#9289,#9290,#9291,#9292,#9293,#9294,#9295,#9296,#9297,#9298,
#9299,#9300,#9301,#9302,#9303,#9304,#9305,#9306,#9307,#9308,#9309,#9310,
#9311,#9312,#9313,#9314,#9315,#9316,#9317,#9318,#9319,#9320,#9321,#9322,
#9323,#9324,#9325,#9326,#9327,#9328,#9329,#9330,#9331,#9332,#9333,#9334,
#9335,#9336,#9337,#9338,#9339,#9340,#9341,#9342,#9343,#9344,#9345,#9346,
#9347,#9348,#9349,#9350,#9351,#9352,#9353,#9354,#9355,#9356,#9357,#9358,
#9359,#9360,#9361,#9362,#9363,#9364,#9365,#9366,#9367,#9368,#9369,#9370,
#9371,#9372,#9373,#9374,#9375,#9376,#9377,#9378,#9379,#9380,#9381,#9382,
#9383,#9384,#9385,#9386,#9387,#9388,#9389,#9390,#9391,#9392,#9393,#9394,
#9395,#9396,#9397,#9398,#9399,#9400,#9401,#9402,#9403,#9404,#9405,#9406,
#9407,#9408,#9409,#9410,#9411,#9412,#9413,#9414,#9415,#9416,#9417,#9418,
#9419,#9420,#9421,#9422,#9423,#9424,#9425,#9426,#9427,#9428,#9429,#9430,
#9431,#9432,#9433,#9434,#9435,#9436,#9437,#9438,#9439,#9440,#9441,#9442,
#9443,#9444,#9445,#9446,#9447,#9448,#9449,#9450,#9451,#9452,#9453,#9454,
#9455,#9456,#9457,#9458,#9459,#9460,#9461,#9462,#9463,#9464,#9465,#9466,
#9467,#9468,#9469,#9470,#9471,#9472,#9473,#9474,#9475,#9476,#9477,#9478,
#9479,#9480,#9481,#9482,#9483,#9484,#9485,#9486,#9487,#9488,#9489,#9490,
#9491,#9492,#9493,#9494,#9495,#9496,#9497,#9498,#9499,#9500,#9501,#9502,
#9503,#9504,#9505,#9506,#9507,#9508,#9509,#9510,#9511,#9512,#9513,#9514,
#9515,#9516,#9517,#9518,#9519,#9520,#9521,#9522,#9523,#9524,#9525,#9526,
#9527,#9528,#9529,#9530,#9531,#9532,#9533,#9534,#9535,#9536,#9537,#9538,
#9539,#9540,#9541,#9542,#9543,#9544,#9545,#9546,#9547,#9548,#9549,#9550,
#9551,#9552,#9553,#9554,#9555,#9556,#9557,#9558,#9559,#9560,#9561,#9562,
#9563,#9564,#9565,#9566,#9567,#9568,#9569,#9570,#9571,#9572,#9573,#9574,
#9575,#9576,#9577,#9578,#9579,#9580,#9581,#9582,#9583,#9584,#9585,#9586,
#9587,#9588,#9589,#9590,#9591,#9592,#9593,#9594,#9595,#9596,#9597,#9598,
#9599,#9600,#9601,#9602,#9603,#9604,#9605,#9606,#9607,#9608,#9609,#9610,
#9611,#9612,#9613,#9614,#9615,#9616,#9617,#9618,#9619,#9620,#9621,#9622,
#9623,#9624,#9625,#9626,#9627,#9628,#9629,#9630,#9631,#9632,#9633,#9634,
#9635,#9636,#9637,#9638,#9639,#9640,#9641,#9642,#9643,#9644,#9645,#9646,
#9647,#9648,#9649,#9650,#9651,#9652,#9653,#9654,#9655,#9656,#9657,#9658,
#9659,#9660,#9661,#9662,#9663,#9664,#9665,#9666,#9667,#9668,#9669,#9670,
#9671,#9672,#9673,#9674,#9675,#9676,#9677,#9678,#9679,#9680,#9681,#9682,
#9683,#9684,#9685,#9686,#9687,#9688,#9689,#9690,#9691,#9692,#9693,#9694,
#9695,#9696,#9697,#9698,#9699,#9700,#9701,#9702,#9703,#9704,#9705,#9706,
#9707,#9708,#9709,#9710,#9711,#9712,#9713,#9714,#9715,#9716,#9717,#9718,
#9719,#9720,#9721,#9722,#9723,#9724,#9725,#9726,#9727,#9728,#9729,#9730,
#9731,#9732,#9733,#9734,#9735,#9736,#9737,#9738,#9739,#9740,#9741,#9742,
#9743,#9744,#9745,#9746,#9747,#9748,#9749,#9750,#9751,#9752,#9753,#9754,
#9755,#9756,#9757,#9758,#9759,#9760,#9761,#9762,#9763,#9764,#9765,#9766,
#9767,#9768)),.UNSPECIFIED.,.F.,.F.,.F.)
B_SPLINE_SURFACE_WITH_KNOTS((2,2),(3,2,2,2,2,2,2,2,2,2,2,2,2,2,2,2,2,2,
2,2,2,2,2,2,2,2,2,2,2,2,2,2,2,2,2,2,2,2,2,2,2,2,2,2,2,2,2,2,2,2,2,2,2,2,
2,2,2,2,2,2,2,2,2,2,2,2,2,2,2,2,2,2,2,2,2,2,2,2,2,2,2,2,2,2,2,2,2,2,2,2,
2,2,2,2,2,2,2,2,2,2,2,2,2,2,2,2,2,2,2,2,2,2,2,2,2,2,2,2,2,2,2,2,2,2,2,2,
2,2,2,2,2,2,2,2,2,2,2,2,2,2,2,2,2,2,2,2,2,2,2,2,2,2,2,2,2,2,2,2,2,2,2,2,
2,2,2,2,2,2,2,2,2,2,2,2,2,2,2,2,2,2,2,2,2,2,2,2,2,2,2,2,2,2,2,2,2,2,2,2,
2,2,2,2,2,2,2,2,2,2,2,2,2,2,2,2,2,2,2,2,2,2,2,2,2,2,2,2,2,2,2,2,2,2,2,2,
2,2,2,2,2,2,2,2,2,2,2,2,2,2,2,2,2,2,2,2,2,2,2,2,2,2,2,2,2,2,2,2,2,2,2,2,
2,2,2,2,2,2,2,2,2,2,2,2,2,2,2,2,2,2,2,2,2,2,2,2,2,2,2,2,2,2,2,2,2,2,2,2,
2,2,2,2,2,2,2,2,2,2,2,2,2,2,2,2,2,2,2,2,2,2,2,2,2,2,2,2,2,2,2,2,2,2,2,2,
2,2,2,2,2,2,2,2,2,2,2,2,2,2,2,2,2,2,2,2,2,2,2,2,2,2,2,2,2,2,2,2,2,2,2,2,
2,2,2,2,2,2,2,2,2,2,2,2,2,2,2,2,2,2,2,2,2,2,2,2,2,2,2,2,2,2,2,2,2,2,2,2,
2,2,2,2,2,2,2,2,2,2,2,2,2,2,2,2,2,2,2,2,2,2,2,2,2,2,2,2,2,2,2,2,2,2,2,2,
2,2,2,2,2,2,2,2,2,2,2,2,2,2,2,2,2,2,2,2,2,2,2,2,2,2,2,2,2,2,2,2,2,2,2,2,
2,2,2,2,2,2,2,2,2,2,2,2,2,2,2,2,2,2,2,2,2,2,2,2,2,2,2,2,2,2,2,2,2,2,2,2,
2,2,2,2,2,2,2,2,2,2,2,2,2,2,2,2,2,2,2,2,2,2,2,2,2,2,2,2,2,2,2,2,2,2,2,2,
2,2,2,2,2,2,2,2,2,2,2,2,2,2,2,2,2,2,2,2,2,2,2,2,2,2,2,2,2,2,2,2,2,2,2,2,
2,2,2,2,2,2,2,2,2,2,2,2,2,2,2,2,2,2,2,2,2,2,2,2,2,2,2,2,2,2,2,2,2,2,2,2,
2,2,2,2,2,3),(-0.0161647051742108,1.),(0.,0.00157232704402516,0.00314465408805031,
0.00471698113207547,0.00628930817610063,0.00786163522012579,0.00943396226415094,
0.0110062893081761,0.0125786163522013,0.0141509433962264,0.0157232704402516,
0.0172955974842767,0.0188679245283019,0.020440251572327,0.0220125786163522,
0.0235849056603774,0.0251572327044025,0.0267295597484277,0.0283018867924528,
0.029874213836478,0.0314465408805031,0.0330188679245283,0.0345911949685535,
0.0361635220125786,0.0377358490566038,0.0393081761006289,0.0408805031446541,
0.0424528301886792,0.0440251572327044,0.0455974842767296,0.0471698113207547,
0.0487421383647799,0.050314465408805,0.0518867924528302,0.0534591194968553,
0.0550314465408805,0.0566037735849057,0.0581761006289308,0.059748427672956,
0.0613207547169811,0.0628930817610063,0.0644654088050314,0.0660377358490566,
0.0676100628930818,0.0691823899371069,0.0707547169811321,0.0723270440251572,
0.0738993710691824,0.0754716981132075,0.0770440251572327,0.0786163522012579,
0.080188679245283,0.0817610062893082,0.0833333333333333,0.0849056603773585,
0.0864779874213836,0.0880503144654088,0.089622641509434,0.0911949685534591,
0.0927672955974843,0.0943396226415094,0.0959119496855346,0.0974842767295598,
0.0990566037735849,0.10062893081761,0.102201257861635,0.10377358490566,
0.105345911949686,0.106918238993711,0.108490566037736,0.110062893081761,
0.111635220125786,0.113207547169811,0.114779874213836,0.116352201257862,
0.117924528301887,0.119496855345912,0.121069182389937,0.122641509433962,
0.124213836477987,0.125786163522013,0.127358490566038,0.128930817610063,
0.130503144654088,0.132075471698113,0.133647798742138,0.135220125786164,
0.136792452830189,0.138364779874214,0.139937106918239,0.141509433962264,
0.143081761006289,0.144654088050314,0.14622641509434,0.147798742138365,
0.14937106918239,0.150943396226415,0.15251572327044,0.154088050314465,0.155660377358491,
0.157232704402516,0.158805031446541,0.160377358490566,0.161949685534591,
0.163522012578616,0.165094339622642,0.166666666666667,0.168238993710692,
0.169811320754717,0.171383647798742,0.172955974842767,0.174528301886792,
0.176100628930818,0.177672955974843,0.179245283018868,0.180817610062893,
0.182389937106918,0.183962264150943,0.185534591194969,0.187106918238994,
0.188679245283019,0.190251572327044,0.191823899371069,0.193396226415094,
0.19496855345912,0.196540880503145,0.19811320754717,0.199685534591195,0.20125786163522,
0.202830188679245,0.20440251572327,0.205974842767296,0.207547169811321,
0.209119496855346,0.210691823899371,0.212264150943396,0.213836477987421,
0.215408805031447,0.216981132075472,0.218553459119497,0.220125786163522,
0.221698113207547,0.223270440251572,0.224842767295597,0.226415094339623,
0.227987421383648,0.229559748427673,0.231132075471698,0.232704402515723,
0.234276729559748,0.235849056603774,0.237421383647799,0.238993710691824,
0.240566037735849,0.242138364779874,0.243710691823899,0.245283018867925,
0.24685534591195,0.248427672955975,0.25,0.251572327044025,0.25314465408805,
0.254716981132075,0.256289308176101,0.257861635220126,0.259433962264151,
0.261006289308176,0.262578616352201,0.264150943396226,0.265723270440252,
0.267295597484277,0.268867924528302,0.270440251572327,0.272012578616352,
0.273584905660377,0.275157232704403,0.276729559748428,0.278301886792453,
0.279874213836478,0.281446540880503,0.283018867924528,0.284591194968553,
0.286163522012579,0.287735849056604,0.289308176100629,0.290880503144654,
0.292452830188679,0.294025157232704,0.29559748427673,0.297169811320755,
0.29874213836478,0.300314465408805,0.30188679245283,0.303459119496855,0.30503144654088,
0.306603773584906,0.308176100628931,0.309748427672956,0.311320754716981,
0.312893081761006,0.314465408805031,0.316037735849057,0.317610062893082,
0.319182389937107,0.320754716981132,0.322327044025157,0.323899371069182,
0.325471698113208,0.327044025157233,0.328616352201258,0.330188679245283,
0.331761006289308,0.333333333333333,0.334905660377358,0.336477987421384,
0.338050314465409,0.339622641509434,0.341194968553459,0.342767295597484,
0.344339622641509,0.345911949685535,0.34748427672956,0.349056603773585,
0.35062893081761,0.352201257861635,0.35377358490566,0.355345911949686,0.356918238993711,
0.358490566037736,0.360062893081761,0.361635220125786,0.363207547169811,
0.364779874213836,0.366352201257862,0.367924528301887,0.369496855345912,
0.371069182389937,0.372641509433962,0.374213836477987,0.375786163522013,
0.377358490566038,0.378930817610063,0.380503144654088,0.382075471698113,
0.383647798742138,0.385220125786164,0.386792452830189,0.388364779874214,
0.389937106918239,0.391509433962264,0.393081761006289,0.394654088050314,
0.39622641509434,0.397798742138365,0.39937106918239,0.400943396226415,0.40251572327044,
0.404088050314465,0.405660377358491,0.407232704402516,0.408805031446541,
0.410377358490566,0.411949685534591,0.413522012578616,0.415094339622642,
0.416666666666667,0.418238993710692,0.419811320754717,0.421383647798742,
0.422955974842767,0.424528301886792,0.426100628930818,0.427672955974843,
0.429245283018868,0.430817610062893,0.432389937106918,0.433962264150943,
0.435534591194969,0.437106918238994,0.438679245283019,0.440251572327044,
0.441823899371069,0.443396226415094,0.44496855345912,0.446540880503145,
0.44811320754717,0.449685534591195,0.45125786163522,0.452830188679245,0.45440251572327,
0.455974842767296,0.457547169811321,0.459119496855346,0.460691823899371,
0.462264150943396,0.463836477987421,0.465408805031447,0.466981132075472,
0.468553459119497,0.470125786163522,0.471698113207547,0.473270440251572,
0.474842767295597,0.476415094339623,0.477987421383648,0.479559748427673,
0.481132075471698,0.482704402515723,0.484276729559748,0.485849056603774,
0.487421383647799,0.488993710691824,0.490566037735849,0.492138364779874,
0.493710691823899,0.495283018867925,0.49685534591195,0.498427672955975,
0.5,0.501572327044025,0.50314465408805,0.504716981132076,0.506289308176101,
0.507861635220126,0.509433962264151,0.511006289308176,0.512578616352201,
0.514150943396226,0.515723270440252,0.517295597484277,0.518867924528302,
0.520440251572327,0.522012578616352,0.523584905660377,0.525157232704403,
0.526729559748428,0.528301886792453,0.529874213836478,0.531446540880503,
0.533018867924528,0.534591194968553,0.536163522012579,0.537735849056604,
0.539308176100629,0.540880503144654,0.542452830188679,0.544025157232704,
0.54559748427673,0.547169811320755,0.54874213836478,0.550314465408805,0.55188679245283,
0.553459119496855,0.555031446540881,0.556603773584906,0.558176100628931,
0.559748427672956,0.561320754716981,0.562893081761006,0.564465408805031,
0.566037735849057,0.567610062893082,0.569182389937107,0.570754716981132,
0.572327044025157,0.573899371069182,0.575471698113208,0.577044025157233,
0.578616352201258,0.580188679245283,0.581761006289308,0.583333333333333,
0.584905660377358,0.586477987421384,0.588050314465409,0.589622641509434,
0.591194968553459,0.592767295597484,0.594339622641509,0.595911949685535,
0.59748427672956,0.599056603773585,0.60062893081761,0.602201257861635,0.60377358490566,
0.605345911949686,0.606918238993711,0.608490566037736,0.610062893081761,
0.611635220125786,0.613207547169811,0.614779874213837,0.616352201257862,
0.617924528301887,0.619496855345912,0.621069182389937,0.622641509433962,
0.624213836477987,0.625786163522013,0.627358490566038,0.628930817610063,
0.630503144654088,0.632075471698113,0.633647798742138,0.635220125786163,
0.636792452830189,0.638364779874214,0.639937106918239,0.641509433962264,
0.643081761006289,0.644654088050314,0.64622641509434,0.647798742138365,
0.64937106918239,0.650943396226415,0.65251572327044,0.654088050314465,0.655660377358491,
0.657232704402516,0.658805031446541,0.660377358490566,0.661949685534591,
0.663522012578616,0.665094339622642,0.666666666666667,0.668238993710692,
0.669811320754717,0.671383647798742,0.672955974842767,0.674528301886792,
0.676100628930818,0.677672955974843,0.679245283018868,0.680817610062893,
0.682389937106918,0.683962264150943,0.685534591194969,0.687106918238994,
0.688679245283019,0.690251572327044,0.691823899371069,0.693396226415094,
0.694968553459119,0.696540880503145,0.69811320754717,0.699685534591195,
0.70125786163522,0.702830188679245,0.70440251572327,0.705974842767296,0.707547169811321,
0.709119496855346,0.710691823899371,0.712264150943396,0.713836477987421,
0.715408805031447,0.716981132075472,0.718553459119497,0.720125786163522,
0.721698113207547,0.723270440251572,0.724842767295597,0.726415094339623,
0.727987421383648,0.729559748427673,0.731132075471698,0.732704402515723,
0.734276729559748,0.735849056603774,0.737421383647799,0.738993710691824,
0.740566037735849,0.742138364779874,0.743710691823899,0.745283018867924,
0.74685534591195,0.748427672955975,0.75,0.751572327044025,0.75314465408805,
0.754716981132076,0.756289308176101,0.757861635220126,0.759433962264151,
0.761006289308176,0.762578616352201,0.764150943396226,0.765723270440252,
0.767295597484277,0.768867924528302,0.770440251572327,0.772012578616352,
0.773584905660377,0.775157232704403,0.776729559748428,0.778301886792453,
0.779874213836478,0.781446540880503,0.783018867924528,0.784591194968553,
0.786163522012579,0.787735849056604,0.789308176100629,0.790880503144654,
0.792452830188679,0.794025157232704,0.79559748427673,0.797169811320755,
0.79874213836478,0.800314465408805,0.80188679245283,0.803459119496855,0.805031446540881,
0.806603773584906,0.808176100628931,0.809748427672956,0.811320754716981,
0.812893081761006,0.814465408805031,0.816037735849057,0.817610062893082,
0.819182389937107,0.820754716981132,0.822327044025157,0.823899371069182,
0.825471698113208,0.827044025157233,0.828616352201258,0.830188679245283,
0.831761006289308,0.833333333333333,0.834905660377358,0.836477987421384,
0.838050314465409,0.839622641509434,0.841194968553459,0.842767295597484,
0.844339622641509,0.845911949685535,0.84748427672956,0.849056603773585,
0.85062893081761,0.852201257861635,0.85377358490566,0.855345911949686,0.856918238993711,
0.858490566037736,0.860062893081761,0.861635220125786,0.863207547169811,
0.864779874213837,0.866352201257862,0.867924528301887,0.869496855345912,
0.871069182389937,0.872641509433962,0.874213836477987,0.875786163522013,
0.877358490566038,0.878930817610063,0.880503144654088,0.882075471698113,
0.883647798742138,0.885220125786163,0.886792452830189,0.888364779874214,
0.889937106918239,0.891509433962264,0.893081761006289,0.894654088050314,
0.89622641509434,0.897798742138365,0.89937106918239,0.900943396226415,0.90251572327044,
0.904088050314465,0.905660377358491,0.907232704402516,0.908805031446541,
0.910377358490566,0.911949685534591,0.913522012578616,0.915094339622642,
0.916666666666667,0.918238993710692,0.919811320754717,0.921383647798742,
0.922955974842767,0.924528301886792,0.926100628930818,0.927672955974843,
0.929245283018868,0.930817610062893,0.932389937106918,0.933962264150943,
0.935534591194969,0.937106918238994,0.938679245283019,0.940251572327044,
0.941823899371069,0.943396226415094,0.944968553459119,0.946540880503145,
0.94811320754717,0.949685534591195,0.95125786163522,0.952830188679245,0.95440251572327,
0.955974842767296,0.957547169811321,0.959119496855346,0.960691823899371,
0.962264150943396,0.963836477987421,0.965408805031447,0.966981132075472,
0.968553459119497,0.970125786163522,0.971698113207547,0.973270440251572,
0.974842767295597,0.976415094339623,0.977987421383648,0.979559748427673,
0.981132075471698,0.982704402515723,0.984276729559748,0.985849056603774,
0.987421383647799,0.988993710691824,0.990566037735849,0.992138364779874,
0.993710691823899,0.995283018867924,0.99685534591195,0.997310967235791),
 .UNSPECIFIED.)
GEOMETRIC_REPRESENTATION_ITEM()
RATIONAL_B_SPLINE_SURFACE(((1.,0.866025403784439,1.,0.866025403784439,1.,
0.866025403784439,1.,0.866025403784439,1.,0.866025403784439,1.,0.866025403784439,
1.,0.866025403784439,1.,0.866025403784439,1.,0.866025403784439,1.,0.866025403784439,
1.,0.866025403784439,1.,0.866025403784439,1.,0.866025403784439,1.,0.866025403784439,
1.,0.866025403784439,1.,0.866025403784439,1.,0.866025403784439,1.,0.866025403784439,
1.,0.866025403784439,1.,0.866025403784439,1.,0.866025403784439,1.,0.866025403784439,
1.,0.866025403784439,1.,0.866025403784439,1.,0.866025403784439,1.,0.866025403784439,
1.,0.866025403784439,1.,0.866025403784439,1.,0.866025403784439,1.,0.866025403784439,
1.,0.866025403784439,1.,0.866025403784439,1.,0.866025403784439,1.,0.866025403784439,
1.,0.866025403784439,1.,0.866025403784439,1.,0.866025403784439,1.,0.866025403784439,
1.,0.866025403784439,1.,0.866025403784439,1.,0.866025403784439,1.,0.866025403784439,
1.,0.866025403784439,1.,0.866025403784439,1.,0.866025403784439,1.,0.866025403784439,
1.,0.866025403784439,1.,0.866025403784439,1.,0.866025403784439,1.,0.866025403784439,
1.,0.866025403784439,1.,0.866025403784439,1.,0.866025403784439,1.,0.866025403784439,
1.,0.866025403784439,1.,0.866025403784439,1.,0.866025403784439,1.,0.866025403784439,
1.,0.866025403784439,1.,0.866025403784439,1.,0.866025403784439,1.,0.866025403784439,
1.,0.866025403784439,1.,0.866025403784439,1.,0.866025403784439,1.,0.866025403784439,
1.,0.866025403784439,1.,0.866025403784439,1.,0.866025403784439,1.,0.866025403784439,
1.,0.866025403784439,1.,0.866025403784439,1.,0.866025403784439,1.,0.866025403784439,
1.,0.866025403784439,1.,0.866025403784439,1.,0.866025403784439,1.,0.866025403784439,
1.,0.866025403784439,1.,0.866025403784439,1.,0.866025403784439,1.,0.866025403784439,
1.,0.866025403784439,1.,0.866025403784439,1.,0.866025403784439,1.,0.866025403784439,
1.,0.866025403784439,1.,0.866025403784439,1.,0.866025403784439,1.,0.866025403784439,
1.,0.866025403784439,1.,0.866025403784439,1.,0.866025403784439,1.,0.866025403784439,
1.,0.866025403784439,1.,0.866025403784439,1.,0.866025403784439,1.,0.866025403784439,
1.,0.866025403784439,1.,0.866025403784439,1.,0.866025403784439,1.,0.866025403784439,
1.,0.866025403784439,1.,0.866025403784439,1.,0.866025403784439,1.,0.866025403784439,
1.,0.866025403784439,1.,0.866025403784439,1.,0.866025403784439,1.,0.866025403784439,
1.,0.866025403784439,1.,0.866025403784439,1.,0.866025403784439,1.,0.866025403784439,
1.,0.866025403784439,1.,0.866025403784439,1.,0.866025403784439,1.,0.866025403784439,
1.,0.866025403784439,1.,0.866025403784439,1.,0.866025403784439,1.,0.866025403784439,
1.,0.866025403784439,1.,0.866025403784439,1.,0.866025403784439,1.,0.866025403784439,
1.,0.866025403784439,1.,0.866025403784439,1.,0.866025403784439,1.,0.866025403784439,
1.,0.866025403784439,1.,0.866025403784439,1.,0.866025403784439,1.,0.866025403784439,
1.,0.866025403784439,1.,0.866025403784439,1.,0.866025403784439,1.,0.866025403784439,
1.,0.866025403784439,1.,0.866025403784439,1.,0.866025403784439,1.,0.866025403784439,
1.,0.866025403784439,1.,0.866025403784439,1.,0.866025403784439,1.,0.866025403784439,
1.,0.866025403784439,1.,0.866025403784439,1.,0.866025403784439,1.,0.866025403784439,
1.,0.866025403784439,1.,0.866025403784439,1.,0.866025403784439,1.,0.866025403784439,
1.,0.866025403784439,1.,0.866025403784439,1.,0.866025403784439,1.,0.866025403784439,
1.,0.866025403784439,1.,0.866025403784439,1.,0.866025403784439,1.,0.866025403784439,
1.,0.866025403784439,1.,0.866025403784439,1.,0.866025403784439,1.,0.866025403784439,
1.,0.866025403784439,1.,0.866025403784439,1.,0.866025403784439,1.,0.866025403784439,
1.,0.866025403784439,1.,0.866025403784439,1.,0.866025403784439,1.,0.866025403784439,
1.,0.866025403784439,1.,0.866025403784439,1.,0.866025403784439,1.,0.866025403784439,
1.,0.866025403784439,1.,0.866025403784439,1.,0.866025403784439,1.,0.866025403784439,
1.,0.866025403784439,1.,0.866025403784439,1.,0.866025403784439,1.,0.866025403784439,
1.,0.866025403784439,1.,0.866025403784439,1.,0.866025403784439,1.,0.866025403784439,
1.,0.866025403784439,1.,0.866025403784439,1.,0.866025403784439,1.,0.866025403784439,
1.,0.866025403784439,1.,0.866025403784439,1.,0.866025403784439,1.,0.866025403784439,
1.,0.866025403784439,1.,0.866025403784439,1.,0.866025403784439,1.,0.866025403784439,
1.,0.866025403784439,1.,0.866025403784439,1.,0.866025403784439,1.,0.866025403784439,
1.,0.866025403784439,1.,0.866025403784439,1.,0.866025403784439,1.,0.866025403784439,
1.,0.866025403784439,1.,0.866025403784439,1.,0.866025403784439,1.,0.866025403784439,
1.,0.866025403784439,1.,0.866025403784439,1.,0.866025403784439,1.,0.866025403784439,
1.,0.866025403784439,1.,0.866025403784439,1.,0.866025403784439,1.,0.866025403784439,
1.,0.866025403784439,1.,0.866025403784439,1.,0.866025403784439,1.,0.866025403784439,
1.,0.866025403784439,1.,0.866025403784439,1.,0.866025403784439,1.,0.866025403784439,
1.,0.866025403784439,1.,0.866025403784439,1.,0.866025403784439,1.,0.866025403784439,
1.,0.866025403784439,1.,0.866025403784439,1.,0.866025403784439,1.,0.866025403784439,
1.,0.866025403784439,1.,0.866025403784439,1.,0.866025403784439,1.,0.866025403784439,
1.,0.866025403784439,1.,0.866025403784439,1.,0.866025403784439,1.,0.866025403784439,
1.,0.866025403784439,1.,0.866025403784439,1.,0.866025403784439,1.,0.866025403784439,
1.,0.866025403784439,1.,0.866025403784439,1.,0.866025403784439,1.,0.866025403784439,
1.,0.866025403784439,1.,0.866025403784439,1.,0.866025403784439,1.,0.866025403784439,
1.,0.866025403784439,1.,0.866025403784439,1.,0.866025403784439,1.,0.866025403784439,
1.,0.866025403784439,1.,0.866025403784439,1.,0.866025403784439,1.,0.866025403784439,
1.,0.866025403784439,1.,0.866025403784439,1.,0.866025403784439,1.,0.866025403784439,
1.,0.866025403784439,1.,0.866025403784439,1.,0.866025403784439,1.,0.866025403784439,
1.,0.866025403784439,1.,0.866025403784439,1.,0.866025403784439,1.,0.866025403784439,
1.,0.866025403784439,1.,0.866025403784439,1.,0.866025403784439,1.,0.866025403784439,
1.,0.866025403784439,1.,0.866025403784439,1.,0.866025403784439,1.,0.866025403784439,
1.,0.866025403784439,1.,0.866025403784439,1.,0.866025403784439,1.,0.866025403784439,
1.,0.866025403784439,1.,0.866025403784439,1.,0.866025403784439,1.,0.866025403784439,
1.,0.866025403784439,1.,0.866025403784439,1.,0.866025403784439,1.,0.866025403784439,
1.,0.866025403784439,1.,0.866025403784439,1.,0.866025403784439,1.,0.866025403784439,
1.,0.866025403784439,1.,0.866025403784439,1.,0.866025403784439,1.,0.866025403784439,
1.,0.866025403784439,1.,0.866025403784439,1.,0.866025403784439,1.,0.866025403784439,
1.,0.866025403784439,1.,0.866025403784439,1.,0.866025403784439,1.,0.866025403784439,
1.,0.866025403784439,1.,0.866025403784439,1.,0.866025403784439,1.,0.866025403784439,
1.,0.866025403784439,1.,0.866025403784439,1.,0.866025403784439,1.,0.866025403784439,
1.,0.866025403784439,1.,0.866025403784439,1.,0.866025403784439,1.,0.866025403784439,
1.,0.866025403784439,1.,0.866025403784439,1.,0.866025403784439,1.,0.866025403784439,
1.,0.866025403784439,1.,0.866025403784439,1.,0.866025403784439,1.,0.866025403784439,
1.,0.866025403784439,1.,0.866025403784439,1.,0.866025403784439,1.,0.866025403784439,
1.,0.866025403784439,1.,0.866025403784439,1.,0.866025403784439,1.,0.866025403784439,
1.,0.866025403784439,1.,0.866025403784439,1.,0.866025403784439,1.,0.866025403784439,
1.,0.866025403784439,1.,0.866025403784439,1.,0.866025403784439,1.,0.866025403784439,
1.,0.866025403784439,1.,0.866025403784439,1.,0.866025403784439,1.,0.866025403784439,
1.,0.866025403784439,1.,0.866025403784439,1.,0.866025403784439,1.,0.866025403784439,
1.,0.866025403784439,1.,0.866025403784439,1.,0.866025403784439,1.,0.866025403784439,
1.,0.866025403784439,1.,0.866025403784439,1.,0.866025403784439,1.,0.866025403784439,
1.,0.866025403784439,1.,0.866025403784439,1.,0.866025403784439,1.,0.866025403784439,
1.,0.866025403784439,1.,0.866025403784439,1.,0.866025403784439,1.,0.866025403784439,
1.,0.866025403784439,1.,0.866025403784439,1.,0.866025403784439,1.,0.866025403784439,
1.,0.866025403784439,1.,0.866025403784439,1.,0.866025403784439,1.,0.866025403784439,
1.,0.866025403784439,1.,0.866025403784439,1.,0.866025403784439,1.,0.866025403784439,
1.,0.866025403784439,1.,0.866025403784439,1.,0.866025403784439,1.,0.866025403784439,
1.,0.866025403784439,1.,0.866025403784439,1.,0.866025403784439,1.,0.866025403784439,
1.,0.866025403784439,1.,0.866025403784439,1.,0.866025403784439,1.,0.866025403784439,
1.,0.866025403784439,1.,0.866025403784439,1.,0.866025403784439,1.,0.866025403784439,
1.,0.866025403784439,1.,0.866025403784439,1.,0.866025403784439,1.,0.866025403784439,
1.,0.866025403784439,1.,0.866025403784439,1.,0.866025403784439,1.,0.866025403784439,
1.,0.866025403784439,1.,0.866025403784439,1.,0.866025403784439,1.,0.866025403784439,
1.,0.866025403784439,1.,0.866025403784439,1.,0.866025403784439,1.,0.866025403784439,
1.,0.866025403784439,1.,0.866025403784439,1.,0.866025403784439,1.,0.866025403784439,
1.,0.866025403784439,1.,0.866025403784439,1.,0.866025403784439,1.,0.866025403784439,
1.,0.866025403784439,1.,0.866025403784439,1.,0.866025403784439,1.,0.866025403784439,
1.,0.866025403784439,1.,0.866025403784439,1.,0.866025403784439,1.,0.866025403784439,
1.,0.866025403784439,1.,0.866025403784439,1.,0.866025403784439,1.,0.866025403784439,
1.,0.866025403784439,1.,0.866025403784439,1.,0.866025403784439,1.,0.866025403784439,
1.,0.866025403784439,1.,0.866025403784439,1.,0.866025403784439,1.,0.866025403784439,
1.,0.866025403784439,1.,0.866025403784439,1.,0.866025403784439,1.,0.866025403784439,
1.,0.866025403784439,1.,0.866025403784439,1.,0.866025403784439,1.,0.866025403784439,
1.,0.866025403784439,1.,0.866025403784439,1.,0.866025403784439,1.,0.866025403784439,
1.,0.866025403784439,1.,0.866025403784439,1.,0.866025403784439,1.,0.866025403784439,
1.,0.866025403784439,1.,0.866025403784439,1.,0.866025403784439,1.,0.866025403784439,
1.,0.866025403784439,1.,0.866025403784439,1.,0.866025403784439,1.,0.866025403784439,
1.,0.866025403784439,1.,0.866025403784439,1.,0.866025403784439,1.,0.866025403784439,
1.,0.866025403784439,1.,0.866025403784439,1.,0.866025403784439,1.,0.866025403784439,
1.,0.866025403784439,1.,0.866025403784439,1.,0.866025403784439,1.,0.866025403784439,
1.,0.866025403784439,1.,0.866025403784439,1.,0.866025403784439,1.,0.866025403784439,
1.,0.866025403784439,1.,0.866025403784439,1.,0.866025403784439,1.,0.866025403784439,
1.,0.866025403784439,1.,0.866025403784439,1.,0.866025403784439,1.,0.866025403784439,
1.,0.866025403784439,1.,0.866025403784439,1.,0.866025403784439,1.,0.866025403784439,
1.,0.866025403784439,1.,0.866025403784439,1.,0.866025403784439,1.,0.866025403784439,
1.,0.866025403784439,1.,0.866025403784439,1.,0.866025403784439,1.,0.866025403784439,
1.,0.866025403784439,1.,0.866025403784439,1.,0.866025403784439,1.,0.866025403784439,
1.,0.866025403784439,1.,0.866025403784439,1.,0.866025403784439,1.,0.866025403784439,
1.,0.866025403784439,1.,0.866025403784439,1.,0.866025403784439,1.,0.866025403784439,
1.,0.866025403784439,1.,0.866025403784439,1.,0.866025403784439,1.,0.866025403784439,
1.,0.866025403784439,1.,0.866025403784439,1.,0.866025403784439,1.,0.866025403784439,
1.,0.866025403784439,1.,0.866025403784439,1.,0.866025403784439,1.,0.866025403784439,
1.,0.866025403784439,1.,0.866025403784439,1.,0.866025403784439,1.,0.866025403784439,
1.,0.866025403784439,1.,0.866025403784439,1.,0.866025403784439,1.,0.866025403784439,
1.,0.866025403784439,1.,0.866025403784439,1.,0.866025403784439,1.,0.866025403784439,
1.,0.866025403784439,1.,0.866025403784439,1.,0.866025403784439,1.,0.866025403784439,
1.,0.866025403784439,1.,0.866025403784439,1.,0.866025403784439,1.,0.866025403784439,
1.,0.866025403784439,1.,0.866025403784439,1.,0.866025403784439,1.,0.866025403784439,
1.,0.866025403784439,1.,0.866025403784439,1.,0.866025403784439,1.,0.866025403784439,
1.,0.866025403784439,1.,0.866025403784439,1.,0.866025403784439,1.,0.866025403784439,
1.,0.866025403784439,1.,0.866025403784439,1.,0.866025403784439,1.,0.866025403784439,
1.,0.866025403784439,1.,0.866025403784439,1.,0.866025403784439,1.,0.866025403784439,
1.,0.866025403784439,1.,0.866025403784439,1.,0.866025403784439,1.,0.866025403784439,
1.,0.866025403784439,1.,0.866025403784439,1.,0.866025403784439,1.,0.866025403784439,
1.,0.866025403784439,1.,0.866025403784439,1.,0.866025403784439,1.,0.866025403784439,
1.,0.866025403784439,1.,0.866025403784439,1.,0.866025403784439,1.,0.866025403784439,
1.,0.866025403784439,1.,0.866025403784439,1.,0.866025403784439,1.,0.866025403784439,
1.,0.866025403784439,1.,0.866025403784439,1.,0.866025403784439,1.,0.866025403784439,
1.,0.866025403784439,1.,0.866025403784439,1.,0.866025403784439,1.,0.866025403784439,
1.,0.866025403784439,1.,0.866025403784439,1.,0.866025403784439,1.,0.866025403784439,
1.,0.866025403784439,1.,0.866025403784439,1.,0.866025403784439,1.,0.866025403784439,
1.,0.866025403784439,1.,0.866025403784439,1.,0.866025403784439,1.,0.866025403784439,
1.,0.866025403784439,1.,0.866025403784439,1.,0.866025403784439,1.,0.866025403784439,
1.,0.866025403784439,1.,0.866025403784439,1.,0.866025403784439,1.,0.866025403784439,
1.,0.866025403784439,1.,0.866025403784439,1.,0.866025403784439,1.,0.866025403784439,
1.,0.866025403784439,1.,0.866025403784439,1.,0.866025403784439,1.,0.866025403784439,
1.,0.866025403784439,1.,0.866025403784439,1.,0.866025403784439,1.,0.866025403784439,
1.,0.866025403784439,1.,0.866025403784439,1.,0.866025403784439,1.,0.866025403784439,
1.,0.961177489682721,0.944854577795434),(1.,0.866025403784439,1.,0.866025403784439,
1.,0.866025403784439,1.,0.866025403784439,1.,0.866025403784439,1.,0.866025403784439,
1.,0.866025403784439,1.,0.866025403784439,1.,0.866025403784439,1.,0.866025403784439,
1.,0.866025403784439,1.,0.866025403784439,1.,0.866025403784439,1.,0.866025403784439,
1.,0.866025403784439,1.,0.866025403784439,1.,0.866025403784439,1.,0.866025403784439,
1.,0.866025403784439,1.,0.866025403784439,1.,0.866025403784439,1.,0.866025403784439,
1.,0.866025403784439,1.,0.866025403784439,1.,0.866025403784439,1.,0.866025403784439,
1.,0.866025403784439,1.,0.866025403784439,1.,0.866025403784439,1.,0.866025403784439,
1.,0.866025403784439,1.,0.866025403784439,1.,0.866025403784439,1.,0.866025403784439,
1.,0.866025403784439,1.,0.866025403784439,1.,0.866025403784439,1.,0.866025403784439,
1.,0.866025403784439,1.,0.866025403784439,1.,0.866025403784439,1.,0.866025403784439,
1.,0.866025403784439,1.,0.866025403784439,1.,0.866025403784439,1.,0.866025403784439,
1.,0.866025403784439,1.,0.866025403784439,1.,0.866025403784439,1.,0.866025403784439,
1.,0.866025403784439,1.,0.866025403784439,1.,0.866025403784439,1.,0.866025403784439,
1.,0.866025403784439,1.,0.866025403784439,1.,0.866025403784439,1.,0.866025403784439,
1.,0.866025403784439,1.,0.866025403784439,1.,0.866025403784439,1.,0.866025403784439,
1.,0.866025403784439,1.,0.866025403784439,1.,0.866025403784439,1.,0.866025403784439,
1.,0.866025403784439,1.,0.866025403784439,1.,0.866025403784439,1.,0.866025403784439,
1.,0.866025403784439,1.,0.866025403784439,1.,0.866025403784439,1.,0.866025403784439,
1.,0.866025403784439,1.,0.866025403784439,1.,0.866025403784439,1.,0.866025403784439,
1.,0.866025403784439,1.,0.866025403784439,1.,0.866025403784439,1.,0.866025403784439,
1.,0.866025403784439,1.,0.866025403784439,1.,0.866025403784439,1.,0.866025403784439,
1.,0.866025403784439,1.,0.866025403784439,1.,0.866025403784439,1.,0.866025403784439,
1.,0.866025403784439,1.,0.866025403784439,1.,0.866025403784439,1.,0.866025403784439,
1.,0.866025403784439,1.,0.866025403784439,1.,0.866025403784439,1.,0.866025403784439,
1.,0.866025403784439,1.,0.866025403784439,1.,0.866025403784439,1.,0.866025403784439,
1.,0.866025403784439,1.,0.866025403784439,1.,0.866025403784439,1.,0.866025403784439,
1.,0.866025403784439,1.,0.866025403784439,1.,0.866025403784439,1.,0.866025403784439,
1.,0.866025403784439,1.,0.866025403784439,1.,0.866025403784439,1.,0.866025403784439,
1.,0.866025403784439,1.,0.866025403784439,1.,0.866025403784439,1.,0.866025403784439,
1.,0.866025403784439,1.,0.866025403784439,1.,0.866025403784439,1.,0.866025403784439,
1.,0.866025403784439,1.,0.866025403784439,1.,0.866025403784439,1.,0.866025403784439,
1.,0.866025403784439,1.,0.866025403784439,1.,0.866025403784439,1.,0.866025403784439,
1.,0.866025403784439,1.,0.866025403784439,1.,0.866025403784439,1.,0.866025403784439,
1.,0.866025403784439,1.,0.866025403784439,1.,0.866025403784439,1.,0.866025403784439,
1.,0.866025403784439,1.,0.866025403784439,1.,0.866025403784439,1.,0.866025403784439,
1.,0.866025403784439,1.,0.866025403784439,1.,0.866025403784439,1.,0.866025403784439,
1.,0.866025403784439,1.,0.866025403784439,1.,0.866025403784439,1.,0.866025403784439,
1.,0.866025403784439,1.,0.866025403784439,1.,0.866025403784439,1.,0.866025403784439,
1.,0.866025403784439,1.,0.866025403784439,1.,0.866025403784439,1.,0.866025403784439,
1.,0.866025403784439,1.,0.866025403784439,1.,0.866025403784439,1.,0.866025403784439,
1.,0.866025403784439,1.,0.866025403784439,1.,0.866025403784439,1.,0.866025403784439,
1.,0.866025403784439,1.,0.866025403784439,1.,0.866025403784439,1.,0.866025403784439,
1.,0.866025403784439,1.,0.866025403784439,1.,0.866025403784439,1.,0.866025403784439,
1.,0.866025403784439,1.,0.866025403784439,1.,0.866025403784439,1.,0.866025403784439,
1.,0.866025403784439,1.,0.866025403784439,1.,0.866025403784439,1.,0.866025403784439,
1.,0.866025403784439,1.,0.866025403784439,1.,0.866025403784439,1.,0.866025403784439,
1.,0.866025403784439,1.,0.866025403784439,1.,0.866025403784439,1.,0.866025403784439,
1.,0.866025403784439,1.,0.866025403784439,1.,0.866025403784439,1.,0.866025403784439,
1.,0.866025403784439,1.,0.866025403784439,1.,0.866025403784439,1.,0.866025403784439,
1.,0.866025403784439,1.,0.866025403784439,1.,0.866025403784439,1.,0.866025403784439,
1.,0.866025403784439,1.,0.866025403784439,1.,0.866025403784439,1.,0.866025403784439,
1.,0.866025403784439,1.,0.866025403784439,1.,0.866025403784439,1.,0.866025403784439,
1.,0.866025403784439,1.,0.866025403784439,1.,0.866025403784439,1.,0.866025403784439,
1.,0.866025403784439,1.,0.866025403784439,1.,0.866025403784439,1.,0.866025403784439,
1.,0.866025403784439,1.,0.866025403784439,1.,0.866025403784439,1.,0.866025403784439,
1.,0.866025403784439,1.,0.866025403784439,1.,0.866025403784439,1.,0.866025403784439,
1.,0.866025403784439,1.,0.866025403784439,1.,0.866025403784439,1.,0.866025403784439,
1.,0.866025403784439,1.,0.866025403784439,1.,0.866025403784439,1.,0.866025403784439,
1.,0.866025403784439,1.,0.866025403784439,1.,0.866025403784439,1.,0.866025403784439,
1.,0.866025403784439,1.,0.866025403784439,1.,0.866025403784439,1.,0.866025403784439,
1.,0.866025403784439,1.,0.866025403784439,1.,0.866025403784439,1.,0.866025403784439,
1.,0.866025403784439,1.,0.866025403784439,1.,0.866025403784439,1.,0.866025403784439,
1.,0.866025403784439,1.,0.866025403784439,1.,0.866025403784439,1.,0.866025403784439,
1.,0.866025403784439,1.,0.866025403784439,1.,0.866025403784439,1.,0.866025403784439,
1.,0.866025403784439,1.,0.866025403784439,1.,0.866025403784439,1.,0.866025403784439,
1.,0.866025403784439,1.,0.866025403784439,1.,0.866025403784439,1.,0.866025403784439,
1.,0.866025403784439,1.,0.866025403784439,1.,0.866025403784439,1.,0.866025403784439,
1.,0.866025403784439,1.,0.866025403784439,1.,0.866025403784439,1.,0.866025403784439,
1.,0.866025403784439,1.,0.866025403784439,1.,0.866025403784439,1.,0.866025403784439,
1.,0.866025403784439,1.,0.866025403784439,1.,0.866025403784439,1.,0.866025403784439,
1.,0.866025403784439,1.,0.866025403784439,1.,0.866025403784439,1.,0.866025403784439,
1.,0.866025403784439,1.,0.866025403784439,1.,0.866025403784439,1.,0.866025403784439,
1.,0.866025403784439,1.,0.866025403784439,1.,0.866025403784439,1.,0.866025403784439,
1.,0.866025403784439,1.,0.866025403784439,1.,0.866025403784439,1.,0.866025403784439,
1.,0.866025403784439,1.,0.866025403784439,1.,0.866025403784439,1.,0.866025403784439,
1.,0.866025403784439,1.,0.866025403784439,1.,0.866025403784439,1.,0.866025403784439,
1.,0.866025403784439,1.,0.866025403784439,1.,0.866025403784439,1.,0.866025403784439,
1.,0.866025403784439,1.,0.866025403784439,1.,0.866025403784439,1.,0.866025403784439,
1.,0.866025403784439,1.,0.866025403784439,1.,0.866025403784439,1.,0.866025403784439,
1.,0.866025403784439,1.,0.866025403784439,1.,0.866025403784439,1.,0.866025403784439,
1.,0.866025403784439,1.,0.866025403784439,1.,0.866025403784439,1.,0.866025403784439,
1.,0.866025403784439,1.,0.866025403784439,1.,0.866025403784439,1.,0.866025403784439,
1.,0.866025403784439,1.,0.866025403784439,1.,0.866025403784439,1.,0.866025403784439,
1.,0.866025403784439,1.,0.866025403784439,1.,0.866025403784439,1.,0.866025403784439,
1.,0.866025403784439,1.,0.866025403784439,1.,0.866025403784439,1.,0.866025403784439,
1.,0.866025403784439,1.,0.866025403784439,1.,0.866025403784439,1.,0.866025403784439,
1.,0.866025403784439,1.,0.866025403784439,1.,0.866025403784439,1.,0.866025403784439,
1.,0.866025403784439,1.,0.866025403784439,1.,0.866025403784439,1.,0.866025403784439,
1.,0.866025403784439,1.,0.866025403784439,1.,0.866025403784439,1.,0.866025403784439,
1.,0.866025403784439,1.,0.866025403784439,1.,0.866025403784439,1.,0.866025403784439,
1.,0.866025403784439,1.,0.866025403784439,1.,0.866025403784439,1.,0.866025403784439,
1.,0.866025403784439,1.,0.866025403784439,1.,0.866025403784439,1.,0.866025403784439,
1.,0.866025403784439,1.,0.866025403784439,1.,0.866025403784439,1.,0.866025403784439,
1.,0.866025403784439,1.,0.866025403784439,1.,0.866025403784439,1.,0.866025403784439,
1.,0.866025403784439,1.,0.866025403784439,1.,0.866025403784439,1.,0.866025403784439,
1.,0.866025403784439,1.,0.866025403784439,1.,0.866025403784439,1.,0.866025403784439,
1.,0.866025403784439,1.,0.866025403784439,1.,0.866025403784439,1.,0.866025403784439,
1.,0.866025403784439,1.,0.866025403784439,1.,0.866025403784439,1.,0.866025403784439,
1.,0.866025403784439,1.,0.866025403784439,1.,0.866025403784439,1.,0.866025403784439,
1.,0.866025403784439,1.,0.866025403784439,1.,0.866025403784439,1.,0.866025403784439,
1.,0.866025403784439,1.,0.866025403784439,1.,0.866025403784439,1.,0.866025403784439,
1.,0.866025403784439,1.,0.866025403784439,1.,0.866025403784439,1.,0.866025403784439,
1.,0.866025403784439,1.,0.866025403784439,1.,0.866025403784439,1.,0.866025403784439,
1.,0.866025403784439,1.,0.866025403784439,1.,0.866025403784439,1.,0.866025403784439,
1.,0.866025403784439,1.,0.866025403784439,1.,0.866025403784439,1.,0.866025403784439,
1.,0.866025403784439,1.,0.866025403784439,1.,0.866025403784439,1.,0.866025403784439,
1.,0.866025403784439,1.,0.866025403784439,1.,0.866025403784439,1.,0.866025403784439,
1.,0.866025403784439,1.,0.866025403784439,1.,0.866025403784439,1.,0.866025403784439,
1.,0.866025403784439,1.,0.866025403784439,1.,0.866025403784439,1.,0.866025403784439,
1.,0.866025403784439,1.,0.866025403784439,1.,0.866025403784439,1.,0.866025403784439,
1.,0.866025403784439,1.,0.866025403784439,1.,0.866025403784439,1.,0.866025403784439,
1.,0.866025403784439,1.,0.866025403784439,1.,0.866025403784439,1.,0.866025403784439,
1.,0.866025403784439,1.,0.866025403784439,1.,0.866025403784439,1.,0.866025403784439,
1.,0.866025403784439,1.,0.866025403784439,1.,0.866025403784439,1.,0.866025403784439,
1.,0.866025403784439,1.,0.866025403784439,1.,0.866025403784439,1.,0.866025403784439,
1.,0.866025403784439,1.,0.866025403784439,1.,0.866025403784439,1.,0.866025403784439,
1.,0.866025403784439,1.,0.866025403784439,1.,0.866025403784439,1.,0.866025403784439,
1.,0.866025403784439,1.,0.866025403784439,1.,0.866025403784439,1.,0.866025403784439,
1.,0.866025403784439,1.,0.866025403784439,1.,0.866025403784439,1.,0.866025403784439,
1.,0.866025403784439,1.,0.866025403784439,1.,0.866025403784439,1.,0.866025403784439,
1.,0.866025403784439,1.,0.866025403784439,1.,0.866025403784439,1.,0.866025403784439,
1.,0.866025403784439,1.,0.866025403784439,1.,0.866025403784439,1.,0.866025403784439,
1.,0.866025403784439,1.,0.866025403784439,1.,0.866025403784439,1.,0.866025403784439,
1.,0.866025403784439,1.,0.866025403784439,1.,0.866025403784439,1.,0.866025403784439,
1.,0.866025403784439,1.,0.866025403784439,1.,0.866025403784439,1.,0.866025403784439,
1.,0.866025403784439,1.,0.866025403784439,1.,0.866025403784439,1.,0.866025403784439,
1.,0.866025403784439,1.,0.866025403784439,1.,0.866025403784439,1.,0.866025403784439,
1.,0.866025403784439,1.,0.866025403784439,1.,0.866025403784439,1.,0.866025403784439,
1.,0.866025403784439,1.,0.866025403784439,1.,0.866025403784439,1.,0.866025403784439,
1.,0.866025403784439,1.,0.866025403784439,1.,0.866025403784439,1.,0.866025403784439,
1.,0.866025403784439,1.,0.866025403784439,1.,0.866025403784439,1.,0.866025403784439,
1.,0.866025403784439,1.,0.866025403784439,1.,0.866025403784439,1.,0.866025403784439,
1.,0.866025403784439,1.,0.866025403784439,1.,0.866025403784439,1.,0.866025403784439,
1.,0.866025403784439,1.,0.866025403784439,1.,0.866025403784439,1.,0.866025403784439,
1.,0.866025403784439,1.,0.866025403784439,1.,0.866025403784439,1.,0.866025403784439,
1.,0.866025403784439,1.,0.866025403784439,1.,0.866025403784439,1.,0.866025403784439,
1.,0.866025403784439,1.,0.866025403784439,1.,0.866025403784439,1.,0.866025403784439,
1.,0.866025403784439,1.,0.866025403784439,1.,0.866025403784439,1.,0.866025403784439,
1.,0.866025403784439,1.,0.866025403784439,1.,0.866025403784439,1.,0.866025403784439,
1.,0.866025403784439,1.,0.866025403784439,1.,0.866025403784439,1.,0.866025403784439,
1.,0.866025403784439,1.,0.866025403784439,1.,0.866025403784439,1.,0.866025403784439,
1.,0.866025403784439,1.,0.866025403784439,1.,0.866025403784439,1.,0.866025403784439,
1.,0.866025403784439,1.,0.866025403784439,1.,0.866025403784439,1.,0.866025403784439,
1.,0.866025403784439,1.,0.866025403784439,1.,0.866025403784439,1.,0.866025403784439,
1.,0.866025403784439,1.,0.866025403784439,1.,0.866025403784439,1.,0.866025403784439,
1.,0.866025403784439,1.,0.866025403784439,1.,0.866025403784439,1.,0.866025403784439,
1.,0.866025403784439,1.,0.866025403784439,1.,0.866025403784439,1.,0.866025403784439,
1.,0.866025403784439,1.,0.866025403784439,1.,0.866025403784439,1.,0.866025403784439,
1.,0.866025403784439,1.,0.866025403784439,1.,0.866025403784439,1.,0.866025403784439,
1.,0.866025403784439,1.,0.866025403784439,1.,0.866025403784439,1.,0.866025403784439,
1.,0.866025403784439,1.,0.866025403784439,1.,0.866025403784439,1.,0.866025403784439,
1.,0.866025403784439,1.,0.866025403784439,1.,0.866025403784439,1.,0.866025403784439,
1.,0.866025403784439,1.,0.866025403784439,1.,0.866025403784439,1.,0.866025403784439,
1.,0.866025403784439,1.,0.866025403784439,1.,0.866025403784439,1.,0.866025403784439,
1.,0.866025403784439,1.,0.866025403784439,1.,0.866025403784439,1.,0.866025403784439,
1.,0.866025403784439,1.,0.866025403784439,1.,0.866025403784439,1.,0.866025403784439,
1.,0.866025403784439,1.,0.866025403784439,1.,0.866025403784439,1.,0.866025403784439,
1.,0.866025403784439,1.,0.866025403784439,1.,0.866025403784439,1.,0.866025403784439,
1.,0.961177489682721,0.944854577795434)))
REPRESENTATION_ITEM('')
SURFACE()
);
#65=B_SPLINE_CURVE_WITH_KNOTS('',3,(#3540,#3541,#3542,#3543,#3544,#3545,
#3546,#3547,#3548,#3549,#3550,#3551,#3552,#3553,#3554,#3555,#3556,#3557,
#3558,#3559),.UNSPECIFIED.,.F.,.F.,(4,2,2,2,2,2,2,2,2,4),(-0.622449302504414,
-0.602698010393903,-0.526004880371973,-0.445959911298277,-0.367327050519426,
-0.291259341940103,-0.211590365655144,-0.133821287178804,-0.0681146419635469,
-2.00520727152319E-5),.UNSPECIFIED.);
#66=B_SPLINE_CURVE_WITH_KNOTS('',3,(#3569,#3570,#3571,#3572,#3573,#3574,
#3575,#3576,#3577,#3578,#3579,#3580,#3581,#3582,#3583,#3584),
 .UNSPECIFIED.,.F.,.F.,(4,2,2,2,2,2,2,4),(-0.462334159991009,-0.394668919789225,
-0.328266148938867,-0.252215701312488,-0.17329149580553,-0.0971873778249495,
-0.0493231403597584,-3.47740632798757E-5),.UNSPECIFIED.);
#67=B_SPLINE_CURVE_WITH_KNOTS('',3,(#3589,#3590,#3591,#3592,#3593,#3594,
#3595,#3596,#3597,#3598,#3599,#3600,#3601,#3602,#3603,#3604,#3605,#3606,
#3607,#3608,#3609,#3610,#3611,#3612,#3613,#3614,#3615,#3616,#3617,#3618,
#3619,#3620,#3621,#3622,#3623,#3624),.UNSPECIFIED.,.F.,.F.,(4,2,2,2,2,2,
2,2,2,2,2,2,2,2,2,2,2,4),(-1.88592410587206,-1.85408617146932,-1.7777971269776,
-1.69806748653657,-1.61972768584256,-1.54333501691836,-1.46281579632766,
-1.38537641266744,-1.30740264102123,-1.22789473761476,-1.15136658423606,
-1.07167820080295,-0.993215731607202,-0.917046017721851,-0.837334341285013,
-0.759740251060977,-0.682391259072564,-0.622449302504414),.UNSPECIFIED.);
#68=B_SPLINE_CURVE_WITH_KNOTS('',3,(#3625,#3626,#3627,#3628,#3629,#3630,
#3631,#3632,#3633,#3634,#3635,#3636,#3637,#3638,#3639,#3640,#3641,#3642,
#3643,#3644,#3645,#3646,#3647,#3648,#3649,#3650,#3651,#3652,#3653,#3654,
#3655,#3656,#3657,#3658,#3659,#3660),.UNSPECIFIED.,.F.,.F.,(4,2,2,2,2,2,
2,2,2,2,2,2,2,2,2,2,2,4),(-15.8059078484382,-15.7284811974429,-15.653665517221,
-15.5754272842413,-15.4956816545495,-15.4194524679912,-15.3403583161977,
-15.2615169409565,-15.1844370832093,-15.1043175204315,-15.0275796663467,
-14.949602957522,-14.869883690514,-14.7937631863142,-14.7149253060571,-14.6353699334314,
-14.5585040517355,-14.5425064158919),.UNSPECIFIED.);
#69=B_SPLINE_CURVE_WITH_KNOTS('',3,(#3665,#3666,#3667,#3668,#3669,#3670,
#3671,#3672,#3673,#3674,#3675,#3676,#3677,#3678,#3679,#3680,#3681,#3682,
#3683,#3684,#3685,#3686,#3687,#3688,#3689,#3690,#3691,#3692,#3693,#3694,
#3695,#3696,#3697,#3698,#3699,#3700),.UNSPECIFIED.,.F.,.F.,(4,2,2,2,2,2,
2,2,2,2,2,2,2,2,2,2,2,4),(-3.14856413016895,-3.10489715100778,-3.02882540004088,
-2.94914924352566,-2.87133041628292,-2.79447109853634,-2.71452323561515,
-2.63760099185768,-2.55846074620274,-2.47954611547811,-2.40343190159831,
-2.32375077684371,-2.24569432443027,-2.16913428536013,-2.08892367482231,
-2.01176419496968,-1.93327835509454,-1.88592410587206),.UNSPECIFIED.);
#70=B_SPLINE_CURVE_WITH_KNOTS('',3,(#3701,#3702,#3703,#3704,#3705,#3706,
#3707,#3708,#3709,#3710,#3711,#3712,#3713,#3714,#3715,#3716,#3717,#3718,
#3719,#3720,#3721,#3722,#3723,#3724,#3725,#3726,#3727,#3728,#3729,#3730,
#3731,#3732,#3733,#3734,#3735,#3736),.UNSPECIFIED.,.F.,.F.,(4,2,2,2,2,2,
2,2,2,2,2,2,2,2,2,2,2,4),(-14.5425064158919,-14.4786220808176,-14.4015249062871,
-14.3237607179729,-14.2440259604515,-14.1678844570661,-14.0892544615079,
-14.0088975164845,-13.9321945193582,-13.8524947872604,-13.7749409217465,
-13.6973342483475,-13.6175448741017,-13.5412682628649,-13.4627911009055,
-13.3830294511391,-13.3064818519847,-13.2786570707264),.UNSPECIFIED.);
#71=B_SPLINE_CURVE_WITH_KNOTS('',3,(#3741,#3742,#3743,#3744,#3745,#3746,
#3747,#3748,#3749,#3750,#3751,#3752,#3753,#3754,#3755,#3756,#3757,#3758,
#3759,#3760,#3761,#3762,#3763,#3764,#3765,#3766,#3767,#3768,#3769,#3770,
#3771,#3772,#3773,#3774,#3775,#3776),.UNSPECIFIED.,.F.,.F.,(4,2,2,2,2,2,
2,2,2,2,2,2,2,2,2,2,2,4),(-4.41185428584948,-4.3572695192111,-4.28091869991991,
-4.2003622348938,-4.12289038795177,-4.04502319430417,-3.96547714842458,
-3.8889144417926,-3.80922320997531,-3.73072226209172,-3.65456967880987,
-3.57485814630795,-3.49722481002858,-3.41995305829719,-3.340215623117,-3.26348228462995,
-3.18357901441996,-3.14856413016895),.UNSPECIFIED.);
#72=B_SPLINE_CURVE_WITH_KNOTS('',3,(#3777,#3778,#3779,#3780,#3781,#3782,
#3783,#3784,#3785,#3786,#3787,#3788,#3789,#3790,#3791,#3792,#3793,#3794,
#3795,#3796,#3797,#3798,#3799,#3800,#3801,#3802,#3803,#3804,#3805,#3806,
#3807,#3808,#3809,#3810,#3811,#3812),.UNSPECIFIED.,.F.,.F.,(4,2,2,2,2,2,
2,2,2,2,2,2,2,2,2,2,2,4),(-13.2786570707264,-13.2269572259644,-13.1487311386957,
-13.0712676976676,-12.9907288947824,-12.9141887326979,-12.8358248605999,
-12.7559984258067,-12.6796649388668,-12.6004455529773,-12.5216609022194,
-12.4444654353247,-12.3642224886698,-12.287473412726,-12.2093801513485,
-12.1295887274691,-12.053390175169,-12.0137481254518),.UNSPECIFIED.);
#73=B_SPLINE_CURVE_WITH_KNOTS('',3,(#3817,#3818,#3819,#3820,#3821,#3822,
#3823,#3824,#3825,#3826,#3827,#3828,#3829,#3830,#3831,#3832,#3833,#3834,
#3835,#3836,#3837,#3838,#3839,#3840,#3841,#3842,#3843,#3844,#3845,#3846,
#3847,#3848,#3849,#3850,#3851,#3852),.UNSPECIFIED.,.F.,.F.,(4,2,2,2,2,2,
2,2,2,2,2,2,2,2,2,2,2,4),(-5.67436912094876,-5.60860430470927,-5.53183780362614,
-5.45186994916378,-5.37493132522109,-5.29595326180489,-5.21701483115353,
-5.14090272904409,-5.06124241308089,-4.98316085041372,-4.90666931989548,
-4.8264294684555,-4.74924503691536,-4.67089592646034,-4.59167221241137,
-4.51536004512522,-4.43564240150157,-4.41185428584948),.UNSPECIFIED.);
#74=B_SPLINE_CURVE_WITH_KNOTS('',3,(#3853,#3854,#3855,#3856,#3857,#3858,
#3859,#3860,#3861,#3862,#3863,#3864,#3865,#3866,#3867,#3868,#3869,#3870,
#3871,#3872,#3873,#3874,#3875,#3876,#3877,#3878,#3879,#3880,#3881,#3882,
#3883,#3884,#3885,#3886,#3887,#3888),.UNSPECIFIED.,.F.,.F.,(4,2,2,2,2,2,
2,2,2,2,2,2,2,2,2,2,2,4),(-12.0137481254518,-11.9744359470122,-11.8949588787454,
-11.8179869666914,-11.7379919855391,-11.6609061237253,-11.5830357049354,
-11.5032367518886,-11.4270418099655,-11.3483057128929,-11.2680400224234,
-11.1912415811657,-11.1114403116993,-11.0339137135885,-10.9562121549183,
-10.8763660484795,-10.800056548405,-10.7491628692134),.UNSPECIFIED.);
#75=B_SPLINE_CURVE_WITH_KNOTS('',3,(#3893,#3894,#3895,#3896,#3897,#3898,
#3899,#3900,#3901,#3902,#3903,#3904,#3905,#3906,#3907,#3908,#3909,#3910,
#3911,#3912,#3913,#3914,#3915,#3916,#3917,#3918,#3919,#3920,#3921,#3922,
#3923,#3924,#3925,#3926,#3927,#3928),.UNSPECIFIED.,.F.,.F.,(4,2,2,2,2,2,
2,2,2,2,2,2,2,2,2,2,2,4),(-6.93678766774197,-6.85961386328993,-6.7818900142282,
-6.70234030795459,-6.62577637948793,-6.5461183676422,-6.46761316913563,
-6.39151035618055,-6.31183531759777,-6.23419654946404,-6.15703732358235,
-6.07729038628634,-6.00055034959348,-5.92082722654057,-5.84213067069773,
-5.76608624718667,-5.68643900560237,-5.67436912094876),.UNSPECIFIED.);
#76=B_SPLINE_CURVE_WITH_KNOTS('',3,(#3929,#3930,#3931,#3932,#3933,#3934,
#3935,#3936,#3937,#3938,#3939,#3940,#3941,#3942,#3943,#3944,#3945,#3946,
#3947,#3948,#3949,#3950,#3951,#3952,#3953,#3954,#3955,#3956,#3957,#3958,
#3959,#3960,#3961,#3962,#3963,#3964),.UNSPECIFIED.,.F.,.F.,(4,2,2,2,2,2,
2,2,2,2,2,2,2,2,2,2,2,4),(-10.7491628692134,-10.721484683818,-10.6416636053348,
-10.5650269069308,-10.4854075391908,-10.407237710163,-10.329686918681,-10.2490538966559,
-10.1725061967339,-10.0940538094768,-10.014182649809,-9.93777708958984,
-9.85847000380012,-9.77976984720712,-9.70249493208427,-9.62216623393326,
-9.54543533647372,-9.48343899875196),.UNSPECIFIED.);
#77=B_SPLINE_CURVE_WITH_KNOTS('',3,(#3969,#3970,#3971,#3972,#3973,#3974,
#3975,#3976,#3977,#3978,#3979,#3980,#3981,#3982,#3983,#3984,#3985,#3986,
#3987,#3988,#3989,#3990,#3991,#3992,#3993,#3994,#3995,#3996,#3997,#3998,
#3999,#4000,#4001,#4002,#4003,#4004,#4005,#4006),.UNSPECIFIED.,.F.,.F.,
(4,2,2,2,2,2,2,2,2,2,2,2,2,2,2,2,2,2,4),(-8.19874268237018,-8.18783288474684,
-8.11091176744568,-8.03213823044703,-7.9532105718062,-7.87713164764008,
-7.79752959642434,-7.71945696582131,-7.64306894803688,-7.56283468402714,
-7.48565903996338,-7.40748596661602,-7.32826524264494,-7.25196001383447,
-7.17229117661081,-7.09391918147949,-7.01764348240122,-6.937084532239,-6.93678766774197),
 .UNSPECIFIED.);
#78=B_SPLINE_CURVE_WITH_KNOTS('',3,(#4007,#4008,#4009,#4010,#4011,#4012,
#4013,#4014,#4015,#4016,#4017,#4018,#4019,#4020,#4021,#4022,#4023,#4024,
#4025,#4026,#4027,#4028,#4029,#4030,#4031,#4032,#4033,#4034,#4035,#4036,
#4037,#4038,#4039,#4040,#4041,#4042),.UNSPECIFIED.,.F.,.F.,(4,2,2,2,2,2,
2,2,2,2,2,2,2,2,2,2,2,4),(-9.48343899875196,-9.4672619853537,-9.38743432009354,
-9.31118896360937,-9.23215524393813,-9.15278522986094,-9.0757428182935,
-8.9956717661025,-8.91862693582825,-8.84068607390281,-8.76085868335287,
-8.68464121549572,-8.60583518265837,-8.52569108674793,-8.44883212217652,
-8.36896559366926,-8.29149686349102,-8.21851276396746),.UNSPECIFIED.);
#79=B_SPLINE_CURVE_WITH_KNOTS('',3,(#4047,#4048,#4049,#4050,#4051,#4052,
#4053,#4054,#4055,#4056,#4057,#4058,#4059,#4060,#4061,#4062,#4063,#4064,
#4065,#4066,#4067,#4068,#4069,#4070,#4071,#4072,#4073,#4074,#4075,#4076,
#4077,#4078,#4079,#4080,#4081,#4082),.UNSPECIFIED.,.F.,.F.,(4,2,2,2,2,2,
2,2,2,2,2,2,2,2,2,2,2,4),(-9.45989242392903,-9.43999077650971,-9.36038187512455,
-9.28427999581966,-9.20531546624748,-9.12662757343301,-9.04702763321718,
-8.96941790488596,-8.89241104834552,-8.81268983345869,-8.73597722731793,
-8.65647973487902,-8.5778031757691,-8.5018188310753,-8.42223856028909,-8.34442217750091,
-8.26778576297144,-8.19874268237018),.UNSPECIFIED.);
#80=B_SPLINE_CURVE_WITH_KNOTS('',3,(#4083,#4084,#4085,#4086,#4087,#4088,
#4089,#4090,#4091,#4092,#4093,#4094,#4095,#4096,#4097,#4098,#4099,#4100,
#4101,#4102,#4103,#4104,#4105,#4106,#4107,#4108,#4109,#4110,#4111,#4112,
#4113,#4114,#4115,#4116,#4117,#4118,#4119,#4120),.UNSPECIFIED.,.F.,.F.,
(4,2,2,2,2,2,2,2,2,2,2,2,2,2,2,2,2,2,4),(-8.21851276396746,-8.21373558189498,
-8.13386834694535,-8.05755710295663,-7.97892605602102,-7.89908098113983,
-7.81919898031824,-7.74071772777192,-7.66417313720762,-7.58350912693979,
-7.50592987918485,-7.42778926135171,-7.34813866162646,-7.27147276625184,
-7.19163483030402,-7.11303172035878,-7.03671511852042,-6.95685331088016,
-6.95266604471072),.UNSPECIFIED.);
#81=B_SPLINE_CURVE_WITH_KNOTS('',3,(#4125,#4126,#4127,#4128,#4129,#4130,
#4131,#4132,#4133,#4134,#4135,#4136,#4137,#4138,#4139,#4140,#4141,#4142,
#4143,#4144,#4145,#4146,#4147,#4148,#4149,#4150,#4151,#4152,#4153,#4154,
#4155,#4156,#4157,#4158,#4159,#4160),.UNSPECIFIED.,.F.,.F.,(4,2,2,2,2,2,
2,2,2,2,2,2,2,2,2,2,2,4),(-10.7208831151999,-10.689909461682,-10.6096449748488,
-10.5331987333682,-10.4537678957129,-10.376358802264,-10.2990102493312,
-10.2194492767843,-10.143369370979,-10.0651520735019,-9.98562100504683,
-9.90932376044898,-9.83006115144956,-9.75195515827296,-9.67474235452267,
-9.59446715610431,-9.51810101957741,-9.45989242392903),.UNSPECIFIED.);
#82=B_SPLINE_CURVE_WITH_KNOTS('',3,(#4161,#4162,#4163,#4164,#4165,#4166,
#4167,#4168,#4169,#4170,#4171,#4172,#4173,#4174,#4175,#4176,#4177,#4178,
#4179,#4180,#4181,#4182,#4183,#4184,#4185,#4186,#4187,#4188,#4189,#4190,
#4191,#4192,#4193,#4194,#4195,#4196),.UNSPECIFIED.,.F.,.F.,(4,2,2,2,2,2,
2,2,2,2,2,2,2,2,2,2,2,4),(-6.95266604471072,-6.87912035870533,-6.80161111519335,
-6.72177597678322,-6.64494587478012,-6.56472359442252,-6.48595176267986,
-6.40974122844908,-6.32992356240856,-6.25201727672208,-6.17494198405241,
-6.09490861806319,-6.0179008787191,-5.93846147131654,-5.8594675035079,-5.78324336357049,
-5.70343001040883,-5.6879113601691),.UNSPECIFIED.);
#83=B_SPLINE_CURVE_WITH_KNOTS('',3,(#4201,#4202,#4203,#4204,#4205,#4206,
#4207,#4208,#4209,#4210,#4211,#4212,#4213,#4214,#4215,#4216,#4217,#4218,
#4219,#4220,#4221,#4222,#4223,#4224,#4225,#4226,#4227,#4228,#4229,#4230,
#4231,#4232,#4233,#4234,#4235,#4236),.UNSPECIFIED.,.F.,.F.,(4,2,2,2,2,2,
2,2,2,2,2,2,2,2,2,2,2,4),(-11.9803245766439,-11.9373167530931,-11.8585934618904,
-11.7817902230109,-11.7019611013535,-11.6253997279527,-11.5477023803251,
-11.4682254817359,-11.3923417429942,-11.3137849692748,-11.2343306742371,
-11.1577318698951,-11.0781299881721,-11.0011901691327,-10.9236951007982,
-10.8441954672365,-10.7682685365538,-10.7208831151999),.UNSPECIFIED.);
#84=B_SPLINE_CURVE_WITH_KNOTS('',3,(#4237,#4238,#4239,#4240,#4241,#4242,
#4243,#4244,#4245,#4246,#4247,#4248,#4249,#4250,#4251,#4252,#4253,#4254,
#4255,#4256,#4257,#4258,#4259,#4260,#4261,#4262,#4263,#4264,#4265,#4266,
#4267,#4268,#4269,#4270,#4271,#4272),.UNSPECIFIED.,.F.,.F.,(4,2,2,2,2,2,
2,2,2,2,2,2,2,2,2,2,2,4),(-5.6879113601691,-5.62529684161333,-5.54854901162185,
-5.46826362292143,-5.39102857977524,-5.31227247591972,-5.23300989841653,
-5.15664034154526,-5.07678848006062,-4.99838116103412,-4.92183166154852,
-4.84124685797192,-4.7637405229502,-4.68553143909071,-4.6059606559999,-4.52936949203966,
-4.44957633005152,-4.42251287828457),.UNSPECIFIED.);
#85=B_SPLINE_CURVE_WITH_KNOTS('',3,(#4277,#4278,#4279,#4280,#4281,#4282,
#4283,#4284,#4285,#4286,#4287,#4288,#4289,#4290,#4291,#4292,#4293,#4294,
#4295,#4296,#4297,#4298,#4299,#4300,#4301,#4302,#4303,#4304,#4305,#4306,
#4307,#4308,#4309,#4310,#4311,#4312),.UNSPECIFIED.,.F.,.F.,(4,2,2,2,2,2,
2,2,2,2,2,2,2,2,2,2,2,4),(-13.2409568636929,-13.1857973798113,-13.1081455092838,
-13.0307997538635,-12.9503721070074,-12.8741918218951,-12.795946314629,
-12.7163879250462,-12.6402039653457,-12.561110295691,-12.4829974573744,
-12.4059433851361,-12.3258368643218,-12.249533657225,-12.1715840064512,
-12.0920886845932,-12.0161207543943,-11.9803245766439),.UNSPECIFIED.);
#86=B_SPLINE_CURVE_WITH_KNOTS('',3,(#4313,#4314,#4315,#4316,#4317,#4318,
#4319,#4320,#4321,#4322,#4323,#4324,#4325,#4326,#4327,#4328,#4329,#4330,
#4331,#4332,#4333,#4334,#4335,#4336,#4337,#4338,#4339,#4340,#4341,#4342,
#4343,#4344,#4345,#4346,#4347,#4348),.UNSPECIFIED.,.F.,.F.,(4,2,2,2,2,2,
2,2,2,2,2,2,2,2,2,2,2,4),(-4.42251287828457,-4.37105308848007,-4.29475658676344,
-4.2149367917279,-4.13728403482588,-4.05973519783431,-3.97998642459269,
-3.90323717095959,-3.82291167517872,-3.74423079741854,-3.66806093761842,
-3.58829265274099,-3.510477602882,-3.43337898390597,-3.35344313544485,-3.27652653462792,
-3.19699748173497,-3.15840542960694),.UNSPECIFIED.);
#87=B_SPLINE_CURVE_WITH_KNOTS('',3,(#4353,#4354,#4355,#4356,#4357,#4358,
#4359,#4360,#4361,#4362,#4363,#4364,#4365,#4366,#4367,#4368,#4369,#4370,
#4371,#4372,#4373,#4374,#4375,#4376,#4377,#4378,#4379,#4380,#4381,#4382,
#4383,#4384,#4385,#4386,#4387,#4388),.UNSPECIFIED.,.F.,.F.,(4,2,2,2,2,2,
2,2,2,2,2,2,2,2,2,2,2,4),(-14.5013677613806,-14.4340143197835,-14.357337425761,
-14.2796345736176,-14.2001052468701,-14.1241738883576,-14.0456101277613,
-13.9659484009548,-13.8893350084197,-13.8097206417991,-13.7326441155937,
-13.6551329843342,-13.5755730503643,-13.4995748837262,-13.4211982788963,
-13.3416565958452,-13.2652169977317,-13.2409568636929),.UNSPECIFIED.);
#88=B_SPLINE_CURVE_WITH_KNOTS('',3,(#4389,#4390,#4391,#4392,#4393,#4394,
#4395,#4396,#4397,#4398,#4399,#4400,#4401,#4402,#4403,#4404,#4405,#4406,
#4407,#4408,#4409,#4410,#4411,#4412,#4413,#4414,#4415,#4416,#4417,#4418,
#4419,#4420,#4421,#4422,#4423,#4424),.UNSPECIFIED.,.F.,.F.,(4,2,2,2,2,2,
2,2,2,2,2,2,2,2,2,2,2,4),(-3.15840542960694,-3.11810438438716,-3.04194530523324,
-2.96218919644079,-2.88415726256218,-2.80740869673208,-2.72723086835948,
-2.6500962409616,-2.5712724087441,-2.49211926891882,-2.41584052292748,-2.33605445076877,
-2.25775714016015,-2.18123275125624,-2.10076432831839,-2.02336662577393,
-1.94511786786739,-1.89413067066974),.UNSPECIFIED.);
#89=B_SPLINE_CURVE_WITH_KNOTS('',3,(#4429,#4430,#4431,#4432,#4433,#4434,
#4435,#4436,#4437,#4438,#4439,#4440,#4441,#4442,#4443,#4444,#4445,#4446,
#4447,#4448,#4449,#4450,#4451,#4452,#4453,#4454,#4455,#4456,#4457,#4458,
#4459,#4460,#4461,#4462,#4463,#4464),.UNSPECIFIED.,.F.,.F.,(4,2,2,2,2,2,
2,2,2,2,2,2,2,2,2,2,2,4),(-15.7622091439389,-15.6829898523921,-15.6067471990204,
-15.528513438186,-15.4489202057025,-15.3727404748348,-15.2936566676599,
-15.2153833658689,-15.1383330993407,-15.0582339695481,-14.9818408052142,
-14.9038949284596,-14.8243556056916,-14.7483661771305,-14.6695643193714,
-14.5906533835512,-14.5138453351592,-14.5013677613806),.UNSPECIFIED.);
#90=B_SPLINE_CURVE_WITH_KNOTS('',3,(#4465,#4466,#4467,#4468,#4469,#4470,
#4471,#4472,#4473,#4474,#4475,#4476,#4477,#4478,#4479,#4480,#4481,#4482,
#4483,#4484,#4485,#4486,#4487,#4488,#4489,#4490,#4491,#4492,#4493,#4494,
#4495,#4496,#4497,#4498,#4499,#4500),.UNSPECIFIED.,.F.,.F.,(4,2,2,2,2,2,
2,2,2,2,2,2,2,2,2,2,2,4),(-1.89413067066974,-1.86566387854342,-1.78918302276564,
-1.70947059360041,-1.63106398788885,-1.55481869217121,-1.47507701580335,
-1.39754087768896,-1.31998180733374,-1.24035706054127,-1.16372486431469,
-1.08332395037665,-1.00477168783817,-0.928673722312505,-0.848991237615832,
-0.771304718998596,-0.694211484813285,-0.631073530473631),.UNSPECIFIED.);
#91=B_SPLINE_CURVE_WITH_KNOTS('',3,(#4508,#4509,#4510,#4511,#4512,#4513,
#4514,#4515,#4516,#4517),.UNSPECIFIED.,.F.,.F.,(4,3,3,4),(0.0186025420886609,
0.399443095780039,0.791951766276959,0.961843099180382),.UNSPECIFIED.);
#92=B_SPLINE_CURVE_WITH_KNOTS('',3,(#4519,#4520,#4521,#4522,#4523,#4524,
#4525,#4526,#4527,#4528,#4529,#4530,#4531,#4532,#4533,#4534,#4535,#4536),
 .UNSPECIFIED.,.F.,.F.,(4,2,2,2,2,2,2,2,4),(-0.376269306197457,-0.343624542177792,
-0.312421269965175,-0.25987291948725,-0.205012849988066,-0.153112595643002,
-0.0910243275886042,-0.0438944746831949,-1.00000008707024E-6),
 .UNSPECIFIED.);
#93=B_SPLINE_CURVE_WITH_KNOTS('',3,(#4538,#4539,#4540,#4541,#4542,#4543,
#4544,#4545,#4546,#4547,#4548,#4549,#4550,#4551,#4552,#4553,#4554,#4555),
 .UNSPECIFIED.,.F.,.F.,(4,2,2,2,2,2,2,2,4),(-1.05438675280514,-0.870346440875757,
-0.698872384787591,-0.518061896275986,-0.346276386875803,-0.22927416645259,
-0.145876888593318,-0.0688156210803101,0.),.UNSPECIFIED.);
#94=B_SPLINE_CURVE_WITH_KNOTS('',3,(#4563,#4564,#4565,#4566,#4567,#4568,
#4569,#4570,#4571,#4572,#4573,#4574),.UNSPECIFIED.,.F.,.F.,(4,2,2,2,2,4),
(-0.313836142992068,-0.25677177702737,-0.19781608691674,-0.113507480641476,
-0.0353872570075592,-0.0260648083918944),.UNSPECIFIED.);
#95=B_SPLINE_CURVE_WITH_KNOTS('',3,(#4589,#4590,#4591,#4592),
 .UNSPECIFIED.,.F.,.F.,(4,4),(-0.0260648083918944,0.),.UNSPECIFIED.);
#96=B_SPLINE_CURVE_WITH_KNOTS('',3,(#4596,#4597,#4598,#4599,#4600,#4601,
#4602,#4603,#4604,#4605,#4606,#4607,#4608,#4609,#4610,#4611,#4612,#4613,
#4614,#4615),.UNSPECIFIED.,.F.,.F.,(4,2,2,2,2,2,2,2,2,4),(-0.631073530473631,
-0.61441175547036,-0.53762346866716,-0.458031245779653,-0.379277736775302,
-0.303215824772569,-0.223553831976816,-0.145661463287594,-0.0741741268612384,
-1.00000013547596E-6),.UNSPECIFIED.);
#97=B_SPLINE_CURVE_WITH_KNOTS('',3,(#4616,#4617,#4618,#4619,#4620,#4621),
 .UNSPECIFIED.,.F.,.F.,(4,2,4),(-0.113972621579486,-0.0620619568776889,
-0.000408441533670647),.UNSPECIFIED.);
#98=B_SPLINE_CURVE_WITH_KNOTS('',3,(#4622,#4623,#4624,#4625,#4626,#4627,
#4628,#4629,#4630,#4631,#4632,#4633,#4634,#4635,#4636,#4637,#4638,#4639,
#4640,#4641),.UNSPECIFIED.,.F.,.F.,(4,2,2,2,2,2,2,2,2,4),(-16.3669314512571,
-16.2989761330899,-16.2322666274892,-16.1539071068032,-16.0743459352974,
-15.997920071627,-15.9185170450843,-15.8407363969791,-15.7634021047055,
-15.7622091439389),.UNSPECIFIED.);
#99=B_SPLINE_CURVE_WITH_KNOTS('',3,(#7184,#7185,#7186,#7187,#7188,#7189,
#7190,#7191,#7192,#7193,#7194,#7195,#7196,#7197,#7198,#7199,#7200,#7201),
 .UNSPECIFIED.,.F.,.F.,(4,2,2,2,2,2,2,2,4),(0.,0.000446496312049465,0.00089299262409893,
0.00133948893614839,0.00178598524819786,0.00223248156024732,0.00267897787229679,
0.00312547418434625,0.00357196805342217),.UNSPECIFIED.);
#100=B_SPLINE_CURVE_WITH_KNOTS('',3,(#9769,#9770,#9771,#9772,#9773,#9774,
#9775,#9776,#9777,#9778,#9779,#9780,#9781,#9782,#9783,#9784),
 .UNSPECIFIED.,.F.,.F.,(4,2,2,2,2,2,2,4),(2.04424781819707E-8,0.000444285842515272,
0.000888571685030545,0.00177714337006109,0.00222142921257636,0.00266571505509163,
0.00311000089760691,0.00355428674012218),.UNSPECIFIED.);
#101=(
BOUNDED_CURVE()
B_SPLINE_CURVE(2,(#3153,#3154,#3155,#3156,#3157,#3158,#3159,#3160,#3161,
#3162,#3163),.UNSPECIFIED.,.F.,.F.)
B_SPLINE_CURVE_WITH_KNOTS((3,2,2,2,2,3),(0.839018811586759,0.840309935413827,
0.84188650189678,0.843463068379733,0.845039634862686,0.846616201345638),
 .UNSPECIFIED.)
CURVE()
GEOMETRIC_REPRESENTATION_ITEM()
RATIONAL_B_SPLINE_CURVE((0.960270358787523,0.89028195431901,1.,0.866025403784439,
1.,0.866025403784439,1.,0.866025403784439,1.,0.866025403784439,1.))
REPRESENTATION_ITEM('')
);
#102=(
BOUNDED_CURVE()
B_SPLINE_CURVE(2,(#3166,#3167,#3168,#3169,#3170,#3171,#3172,#3173,#3174),
 .UNSPECIFIED.,.F.,.F.)
B_SPLINE_CURVE_WITH_KNOTS((3,2,2,2,3),(0.839084484051456,0.839622641509434,
0.841194968553459,0.842767295597484,0.844339622641509),.UNSPECIFIED.)
CURVE()
GEOMETRIC_REPRESENTATION_ITEM()
RATIONAL_B_SPLINE_CURVE((0.939679100585349,0.954144763707433,1.,0.866025403784439,
1.,0.866025403784439,1.,0.866025403784439,1.))
REPRESENTATION_ITEM('')
);
#103=(
BOUNDED_CURVE()
B_SPLINE_CURVE(2,(#3179,#3180,#3181,#3182,#3183,#3184,#3185,#3186,#3187,
#3188,#3189,#3190,#3191),.UNSPECIFIED.,.F.,.F.)
B_SPLINE_CURVE_WITH_KNOTS((3,2,2,2,2,2,3),(0.846616201345638,0.848192767828591,
0.849769334311544,0.851345900794497,0.852922467277449,0.854499033760402,
0.856075600243355),.UNSPECIFIED.)
CURVE()
GEOMETRIC_REPRESENTATION_ITEM()
RATIONAL_B_SPLINE_CURVE((1.,0.866025403784439,1.,0.866025403784439,1.,0.866025403784439,
1.,0.866025403784439,1.,0.866025403784439,1.,0.866025403784439,1.))
REPRESENTATION_ITEM('')
);
#104=(
BOUNDED_CURVE()
B_SPLINE_CURVE(2,(#3192,#3193,#3194,#3195,#3196,#3197,#3198,#3199,#3200,
#3201,#3202,#3203,#3204),.UNSPECIFIED.,.F.,.F.)
B_SPLINE_CURVE_WITH_KNOTS((3,2,2,2,2,2,3),(0.844339622641509,0.845911949685535,
0.84748427672956,0.849056603773585,0.85062893081761,0.852201257861635,0.85377358490566),
 .UNSPECIFIED.)
CURVE()
GEOMETRIC_REPRESENTATION_ITEM()
RATIONAL_B_SPLINE_CURVE((1.,0.866025403784439,1.,0.866025403784439,1.,0.866025403784439,
1.,0.866025403784439,1.,0.866025403784439,1.,0.866025403784439,1.))
REPRESENTATION_ITEM('')
);
#105=(
BOUNDED_CURVE()
B_SPLINE_CURVE(2,(#3209,#3210,#3211,#3212,#3213,#3214,#3215,#3216,#3217,
#3218,#3219,#3220,#3221),.UNSPECIFIED.,.F.,.F.)
B_SPLINE_CURVE_WITH_KNOTS((3,2,2,2,2,2,3),(0.856075600243355,0.857652166726308,
0.85922873320926,0.860805299692213,0.862381866175166,0.863958432658119,
0.865534999141071),.UNSPECIFIED.)
CURVE()
GEOMETRIC_REPRESENTATION_ITEM()
RATIONAL_B_SPLINE_CURVE((1.,0.866025403784439,1.,0.866025403784439,1.,0.866025403784439,
1.,0.866025403784439,1.,0.866025403784439,1.,0.866025403784439,1.))
REPRESENTATION_ITEM('')
);
#106=(
BOUNDED_CURVE()
B_SPLINE_CURVE(2,(#3222,#3223,#3224,#3225,#3226,#3227,#3228,#3229,#3230,
#3231,#3232,#3233,#3234),.UNSPECIFIED.,.F.,.F.)
B_SPLINE_CURVE_WITH_KNOTS((3,2,2,2,2,2,3),(0.85377358490566,0.855345911949686,
0.856918238993711,0.858490566037736,0.860062893081761,0.861635220125786,
0.863207547169811),.UNSPECIFIED.)
CURVE()
GEOMETRIC_REPRESENTATION_ITEM()
RATIONAL_B_SPLINE_CURVE((1.,0.866025403784439,1.,0.866025403784439,1.,0.866025403784439,
1.,0.866025403784439,1.,0.866025403784439,1.,0.866025403784439,1.))
REPRESENTATION_ITEM('')
);
#107=(
BOUNDED_CURVE()
B_SPLINE_CURVE(2,(#3239,#3240,#3241,#3242,#3243,#3244,#3245,#3246,#3247,
#3248,#3249,#3250,#3251),.UNSPECIFIED.,.F.,.F.)
B_SPLINE_CURVE_WITH_KNOTS((3,2,2,2,2,2,3),(0.865534999141071,0.867111565624024,
0.868688132106977,0.87026469858993,0.871841265072883,0.873417831555835,
0.874994398038788),.UNSPECIFIED.)
CURVE()
GEOMETRIC_REPRESENTATION_ITEM()
RATIONAL_B_SPLINE_CURVE((1.,0.866025403784439,1.,0.866025403784439,1.,0.866025403784439,
1.,0.866025403784439,1.,0.866025403784439,1.,0.866025403784439,1.))
REPRESENTATION_ITEM('')
);
#108=(
BOUNDED_CURVE()
B_SPLINE_CURVE(2,(#3252,#3253,#3254,#3255,#3256,#3257,#3258,#3259,#3260,
#3261,#3262,#3263,#3264),.UNSPECIFIED.,.F.,.F.)
B_SPLINE_CURVE_WITH_KNOTS((3,2,2,2,2,2,3),(0.863207547169811,0.864779874213837,
0.866352201257862,0.867924528301887,0.869496855345912,0.871069182389937,
0.872641509433962),.UNSPECIFIED.)
CURVE()
GEOMETRIC_REPRESENTATION_ITEM()
RATIONAL_B_SPLINE_CURVE((1.,0.866025403784439,1.,0.866025403784439,1.,0.866025403784439,
1.,0.866025403784439,1.,0.866025403784439,1.,0.866025403784439,1.))
REPRESENTATION_ITEM('')
);
#109=(
BOUNDED_CURVE()
B_SPLINE_CURVE(2,(#3269,#3270,#3271,#3272,#3273,#3274,#3275,#3276,#3277,
#3278,#3279,#3280,#3281),.UNSPECIFIED.,.F.,.F.)
B_SPLINE_CURVE_WITH_KNOTS((3,2,2,2,2,2,3),(0.874994398038788,0.876570964521741,
0.878147531004694,0.879724097487646,0.881300663970599,0.882877230453552,
0.884453796936505),.UNSPECIFIED.)
CURVE()
GEOMETRIC_REPRESENTATION_ITEM()
RATIONAL_B_SPLINE_CURVE((1.,0.866025403784439,1.,0.866025403784439,1.,0.866025403784439,
1.,0.866025403784439,1.,0.866025403784439,1.,0.866025403784439,1.))
REPRESENTATION_ITEM('')
);
#110=(
BOUNDED_CURVE()
B_SPLINE_CURVE(2,(#3282,#3283,#3284,#3285,#3286,#3287,#3288,#3289,#3290,
#3291,#3292,#3293,#3294),.UNSPECIFIED.,.F.,.F.)
B_SPLINE_CURVE_WITH_KNOTS((3,2,2,2,2,2,3),(0.872641509433962,0.874213836477987,
0.875786163522013,0.877358490566038,0.878930817610063,0.880503144654088,
0.882075471698113),.UNSPECIFIED.)
CURVE()
GEOMETRIC_REPRESENTATION_ITEM()
RATIONAL_B_SPLINE_CURVE((1.,0.866025403784439,1.,0.866025403784439,1.,0.866025403784439,
1.,0.866025403784439,1.,0.866025403784439,1.,0.866025403784439,1.))
REPRESENTATION_ITEM('')
);
#111=(
BOUNDED_CURVE()
B_SPLINE_CURVE(2,(#3299,#3300,#3301,#3302,#3303,#3304,#3305,#3306,#3307,
#3308,#3309,#3310,#3311),.UNSPECIFIED.,.F.,.F.)
B_SPLINE_CURVE_WITH_KNOTS((3,2,2,2,2,2,3),(0.884453796936505,0.886030363419458,
0.88760692990241,0.889183496385363,0.890760062868316,0.892336629351269,
0.893913195834221),.UNSPECIFIED.)
CURVE()
GEOMETRIC_REPRESENTATION_ITEM()
RATIONAL_B_SPLINE_CURVE((1.,0.866025403784439,1.,0.866025403784439,1.,0.866025403784439,
1.,0.866025403784439,1.,0.866025403784439,1.,0.866025403784439,1.))
REPRESENTATION_ITEM('')
);
#112=(
BOUNDED_CURVE()
B_SPLINE_CURVE(2,(#3312,#3313,#3314,#3315,#3316,#3317,#3318,#3319,#3320,
#3321,#3322,#3323,#3324),.UNSPECIFIED.,.F.,.F.)
B_SPLINE_CURVE_WITH_KNOTS((3,2,2,2,2,2,3),(0.882075471698113,0.883647798742138,
0.885220125786163,0.886792452830189,0.888364779874214,0.889937106918239,
0.891509433962264),.UNSPECIFIED.)
CURVE()
GEOMETRIC_REPRESENTATION_ITEM()
RATIONAL_B_SPLINE_CURVE((1.,0.866025403784439,1.,0.866025403784439,1.,0.866025403784439,
1.,0.866025403784439,1.,0.866025403784439,1.,0.866025403784439,1.))
REPRESENTATION_ITEM('')
);
#113=(
BOUNDED_CURVE()
B_SPLINE_CURVE(2,(#3329,#3330,#3331,#3332,#3333,#3334,#3335,#3336,#3337,
#3338,#3339,#3340,#3341),.UNSPECIFIED.,.F.,.F.)
B_SPLINE_CURVE_WITH_KNOTS((3,2,2,2,2,2,3),(0.893913195834221,0.895489762317174,
0.897066328800127,0.89864289528308,0.900219461766032,0.901796028248985,
0.903372594731938),.UNSPECIFIED.)
CURVE()
GEOMETRIC_REPRESENTATION_ITEM()
RATIONAL_B_SPLINE_CURVE((1.,0.866025403784439,1.,0.866025403784439,1.,0.866025403784439,
1.,0.866025403784439,1.,0.866025403784439,1.,0.866025403784439,1.))
REPRESENTATION_ITEM('')
);
#114=(
BOUNDED_CURVE()
B_SPLINE_CURVE(2,(#3342,#3343,#3344,#3345,#3346,#3347,#3348,#3349,#3350,
#3351,#3352,#3353,#3354),.UNSPECIFIED.,.F.,.F.)
B_SPLINE_CURVE_WITH_KNOTS((3,2,2,2,2,2,3),(0.891509433962264,0.893081761006289,
0.894654088050314,0.89622641509434,0.897798742138365,0.89937106918239,0.900943396226415),
 .UNSPECIFIED.)
CURVE()
GEOMETRIC_REPRESENTATION_ITEM()
RATIONAL_B_SPLINE_CURVE((1.,0.866025403784439,1.,0.866025403784439,1.,0.866025403784439,
1.,0.866025403784439,1.,0.866025403784439,1.,0.866025403784439,1.))
REPRESENTATION_ITEM('')
);
#115=(
BOUNDED_CURVE()
B_SPLINE_CURVE(2,(#3359,#3360,#3361,#3362,#3363,#3364,#3365,#3366,#3367,
#3368,#3369,#3370,#3371),.UNSPECIFIED.,.F.,.F.)
B_SPLINE_CURVE_WITH_KNOTS((3,2,2,2,2,2,3),(0.903372594731938,0.904949161214891,
0.906525727697844,0.908102294180796,0.909678860663749,0.911255427146702,
0.912831993629655),.UNSPECIFIED.)
CURVE()
GEOMETRIC_REPRESENTATION_ITEM()
RATIONAL_B_SPLINE_CURVE((1.,0.866025403784439,1.,0.866025403784439,1.,0.866025403784439,
1.,0.866025403784439,1.,0.866025403784439,1.,0.866025403784439,1.))
REPRESENTATION_ITEM('')
);
#116=(
BOUNDED_CURVE()
B_SPLINE_CURVE(2,(#3372,#3373,#3374,#3375,#3376,#3377,#3378,#3379,#3380,
#3381,#3382,#3383,#3384),.UNSPECIFIED.,.F.,.F.)
B_SPLINE_CURVE_WITH_KNOTS((3,2,2,2,2,2,3),(0.900943396226415,0.90251572327044,
0.904088050314465,0.905660377358491,0.907232704402516,0.908805031446541,
0.910377358490566),.UNSPECIFIED.)
CURVE()
GEOMETRIC_REPRESENTATION_ITEM()
RATIONAL_B_SPLINE_CURVE((1.,0.866025403784439,1.,0.866025403784439,1.,0.866025403784439,
1.,0.866025403784439,1.,0.866025403784439,1.,0.866025403784439,1.))
REPRESENTATION_ITEM('')
);
#117=(
BOUNDED_CURVE()
B_SPLINE_CURVE(2,(#3389,#3390,#3391,#3392,#3393,#3394,#3395,#3396,#3397,
#3398,#3399,#3400,#3401),.UNSPECIFIED.,.F.,.F.)
B_SPLINE_CURVE_WITH_KNOTS((3,2,2,2,2,2,3),(0.912831993629655,0.914408560112607,
0.91598512659556,0.917561693078513,0.919138259561466,0.920714826044419,
0.922291392527371),.UNSPECIFIED.)
CURVE()
GEOMETRIC_REPRESENTATION_ITEM()
RATIONAL_B_SPLINE_CURVE((1.,0.866025403784439,1.,0.866025403784439,1.,0.866025403784439,
1.,0.866025403784439,1.,0.866025403784439,1.,0.866025403784439,1.))
REPRESENTATION_ITEM('')
);
#118=(
BOUNDED_CURVE()
B_SPLINE_CURVE(2,(#3402,#3403,#3404,#3405,#3406,#3407,#3408,#3409,#3410,
#3411,#3412,#3413,#3414),.UNSPECIFIED.,.F.,.F.)
B_SPLINE_CURVE_WITH_KNOTS((3,2,2,2,2,2,3),(0.910377358490566,0.911949685534591,
0.913522012578616,0.915094339622642,0.916666666666667,0.918238993710692,
0.919811320754717),.UNSPECIFIED.)
CURVE()
GEOMETRIC_REPRESENTATION_ITEM()
RATIONAL_B_SPLINE_CURVE((1.,0.866025403784439,1.,0.866025403784439,1.,0.866025403784439,
1.,0.866025403784439,1.,0.866025403784439,1.,0.866025403784439,1.))
REPRESENTATION_ITEM('')
);
#119=(
BOUNDED_CURVE()
B_SPLINE_CURVE(2,(#3419,#3420,#3421,#3422,#3423,#3424,#3425,#3426,#3427,
#3428,#3429,#3430,#3431),.UNSPECIFIED.,.F.,.F.)
B_SPLINE_CURVE_WITH_KNOTS((3,2,2,2,2,2,3),(0.922291392527371,0.923867959010324,
0.925444525493277,0.92702109197623,0.928597658459182,0.930174224942135,
0.931750791425088),.UNSPECIFIED.)
CURVE()
GEOMETRIC_REPRESENTATION_ITEM()
RATIONAL_B_SPLINE_CURVE((1.,0.866025403784439,1.,0.866025403784439,1.,0.866025403784439,
1.,0.866025403784439,1.,0.866025403784439,1.,0.866025403784439,1.))
REPRESENTATION_ITEM('')
);
#120=(
BOUNDED_CURVE()
B_SPLINE_CURVE(2,(#3432,#3433,#3434,#3435,#3436,#3437,#3438,#3439,#3440,
#3441,#3442,#3443,#3444),.UNSPECIFIED.,.F.,.F.)
B_SPLINE_CURVE_WITH_KNOTS((3,2,2,2,2,2,3),(0.919811320754717,0.921383647798742,
0.922955974842767,0.924528301886792,0.926100628930818,0.927672955974843,
0.929245283018868),.UNSPECIFIED.)
CURVE()
GEOMETRIC_REPRESENTATION_ITEM()
RATIONAL_B_SPLINE_CURVE((1.,0.866025403784439,1.,0.866025403784439,1.,0.866025403784439,
1.,0.866025403784439,1.,0.866025403784439,1.,0.866025403784439,1.))
REPRESENTATION_ITEM('')
);
#121=(
BOUNDED_CURVE()
B_SPLINE_CURVE(2,(#3449,#3450,#3451,#3452,#3453,#3454,#3455,#3456,#3457,
#3458,#3459,#3460,#3461),.UNSPECIFIED.,.F.,.F.)
B_SPLINE_CURVE_WITH_KNOTS((3,2,2,2,2,2,3),(0.931750791425088,0.933327357908041,
0.934903924390993,0.936480490873946,0.938057057356899,0.939633623839852,
0.941210190322805),.UNSPECIFIED.)
CURVE()
GEOMETRIC_REPRESENTATION_ITEM()
RATIONAL_B_SPLINE_CURVE((1.,0.866025403784439,1.,0.866025403784439,1.,0.866025403784439,
1.,0.866025403784439,1.,0.866025403784439,1.,0.866025403784439,1.))
REPRESENTATION_ITEM('')
);
#122=(
BOUNDED_CURVE()
B_SPLINE_CURVE(2,(#3462,#3463,#3464,#3465,#3466,#3467,#3468,#3469,#3470,
#3471,#3472,#3473,#3474),.UNSPECIFIED.,.F.,.F.)
B_SPLINE_CURVE_WITH_KNOTS((3,2,2,2,2,2,3),(0.929245283018868,0.930817610062893,
0.932389937106918,0.933962264150943,0.935534591194969,0.937106918238994,
0.938679245283019),.UNSPECIFIED.)
CURVE()
GEOMETRIC_REPRESENTATION_ITEM()
RATIONAL_B_SPLINE_CURVE((1.,0.866025403784439,1.,0.866025403784439,1.,0.866025403784439,
1.,0.866025403784439,1.,0.866025403784439,1.,0.866025403784439,1.))
REPRESENTATION_ITEM('')
);
#123=(
BOUNDED_CURVE()
B_SPLINE_CURVE(2,(#3479,#3480,#3481,#3482,#3483,#3484,#3485,#3486,#3487,
#3488,#3489,#3490,#3491),.UNSPECIFIED.,.F.,.F.)
B_SPLINE_CURVE_WITH_KNOTS((3,2,2,2,2,2,3),(0.941210190322805,0.942786756805757,
0.94436332328871,0.945939889771663,0.947516456254616,0.949093022737568,
0.950669589220521),.UNSPECIFIED.)
CURVE()
GEOMETRIC_REPRESENTATION_ITEM()
RATIONAL_B_SPLINE_CURVE((1.,0.866025403784439,1.,0.866025403784439,1.,0.866025403784439,
1.,0.866025403784439,1.,0.866025403784439,1.,0.866025403784439,1.))
REPRESENTATION_ITEM('')
);
#124=(
BOUNDED_CURVE()
B_SPLINE_CURVE(2,(#3492,#3493,#3494,#3495,#3496,#3497,#3498,#3499,#3500,
#3501,#3502,#3503,#3504),.UNSPECIFIED.,.F.,.F.)
B_SPLINE_CURVE_WITH_KNOTS((3,2,2,2,2,2,3),(0.938679245283019,0.940251572327044,
0.941823899371069,0.943396226415094,0.944968553459119,0.946540880503145,
0.94811320754717),.UNSPECIFIED.)
CURVE()
GEOMETRIC_REPRESENTATION_ITEM()
RATIONAL_B_SPLINE_CURVE((1.,0.866025403784439,1.,0.866025403784439,1.,0.866025403784439,
1.,0.866025403784439,1.,0.866025403784439,1.,0.866025403784439,1.))
REPRESENTATION_ITEM('')
);
#125=(
BOUNDED_CURVE()
B_SPLINE_CURVE(2,(#3509,#3510,#3511,#3512,#3513,#3514,#3515,#3516,#3517,
#3518,#3519,#3520,#3521),.UNSPECIFIED.,.F.,.F.)
B_SPLINE_CURVE_WITH_KNOTS((3,2,2,2,2,2,3),(0.950669589220521,0.952246155703474,
0.953822722186427,0.95539928866938,0.956975855152332,0.958552421635285,
0.960128988118238),.UNSPECIFIED.)
CURVE()
GEOMETRIC_REPRESENTATION_ITEM()
RATIONAL_B_SPLINE_CURVE((1.,0.866025403784439,1.,0.866025403784439,1.,0.866025403784439,
1.,0.866025403784439,1.,0.866025403784439,1.,0.866025403784439,1.))
REPRESENTATION_ITEM('')
);
#126=(
BOUNDED_CURVE()
B_SPLINE_CURVE(2,(#3522,#3523,#3524,#3525,#3526,#3527,#3528,#3529,#3530,
#3531,#3532,#3533,#3534),.UNSPECIFIED.,.F.,.F.)
B_SPLINE_CURVE_WITH_KNOTS((3,2,2,2,2,2,3),(0.94811320754717,0.949685534591195,
0.95125786163522,0.952830188679245,0.95440251572327,0.955974842767296,0.957547169811321),
 .UNSPECIFIED.)
CURVE()
GEOMETRIC_REPRESENTATION_ITEM()
RATIONAL_B_SPLINE_CURVE((1.,0.866025403784439,1.,0.866025403784439,1.,0.866025403784439,
1.,0.866025403784439,1.,0.866025403784439,1.,0.866025403784439,1.))
REPRESENTATION_ITEM('')
);
#127=(
BOUNDED_CURVE()
B_SPLINE_CURVE(2,(#7202,#7203,#7204,#7205,#7206,#7207,#7208,#7209,#7210,
#7211,#7212,#7213,#7214),.UNSPECIFIED.,.F.,.F.)
B_SPLINE_CURVE_WITH_KNOTS((3,2,2,2,2,2,3),(0.957547169811321,0.959119496855346,
0.960691823899371,0.962264150943396,0.963836477987421,0.965408805031447,
0.9665584458795),.UNSPECIFIED.)
CURVE()
GEOMETRIC_REPRESENTATION_ITEM()
RATIONAL_B_SPLINE_CURVE((1.,0.866025403784439,1.,0.866025403784439,1.,0.866025403784439,
1.,0.866025403784439,1.,0.866025403784439,1.,0.902041582890659,0.947331986880629))
REPRESENTATION_ITEM('')
);
#128=(
BOUNDED_CURVE()
B_SPLINE_CURVE(2,(#7216,#7217,#7218,#7219,#7220,#7221,#7222,#7223,#7224,
#7225,#7226),.UNSPECIFIED.,.F.,.F.)
B_SPLINE_CURVE_WITH_KNOTS((3,2,2,2,2,3),(0.960128988118238,0.961705554601191,
0.963282121084143,0.964858687567096,0.966435254050049,0.966840628802582),
 .UNSPECIFIED.)
CURVE()
GEOMETRIC_REPRESENTATION_ITEM()
RATIONAL_B_SPLINE_CURVE((1.,0.866025403784439,1.,0.866025403784439,1.,0.866025403784439,
1.,0.866025403784439,1.,0.965551773823772,0.948818552136593))
REPRESENTATION_ITEM('')
);
#131=CONICAL_SURFACE('',#2266,2.01,0.785398163397453);
#132=CONICAL_SURFACE('',#2278,2.,0.78539816339745);
#133=CONICAL_SURFACE('',#2279,2.01,0.785398163397453);
#141=TOROIDAL_SURFACE('',#2271,2.4,0.4);
#142=TOROIDAL_SURFACE('',#2274,3.9385786437627,0.1);
#149=SHAPE_REPRESENTATION_RELATIONSHIP('SRR','None',#9944,#156);
#156=ADVANCED_BREP_SHAPE_REPRESENTATION('',(#170),#9902);
#163=STYLED_ITEM('',(#9985),#170);
#170=MANIFOLD_SOLID_BREP('Body1',#2028);
#195=FACE_BOUND('',#493,.T.);
#230=PLANE('',#2283);
#231=PLANE('',#2284);
#232=PLANE('',#2285);
#233=PLANE('',#2286);
#234=PLANE('',#2287);
#235=PLANE('',#2288);
#236=PLANE('',#2289);
#237=PLANE('',#2290);
#238=PLANE('',#2291);
#239=PLANE('',#2292);
#240=PLANE('',#2293);
#241=PLANE('',#2294);
#242=PLANE('',#2295);
#243=PLANE('',#2296);
#244=PLANE('',#2297);
#245=PLANE('',#2298);
#246=PLANE('',#2299);
#247=PLANE('',#2300);
#248=PLANE('',#2301);
#249=PLANE('',#2302);
#250=PLANE('',#2303);
#251=PLANE('',#2304);
#313=FACE_OUTER_BOUND('',#455,.T.);
#314=FACE_OUTER_BOUND('',#456,.T.);
#315=FACE_OUTER_BOUND('',#457,.T.);
#316=FACE_OUTER_BOUND('',#458,.T.);
#317=FACE_OUTER_BOUND('',#459,.T.);
#318=FACE_OUTER_BOUND('',#460,.T.);
#319=FACE_OUTER_BOUND('',#461,.T.);
#320=FACE_OUTER_BOUND('',#462,.T.);
#321=FACE_OUTER_BOUND('',#463,.T.);
#322=FACE_OUTER_BOUND('',#464,.T.);
#323=FACE_OUTER_BOUND('',#465,.T.);
#324=FACE_OUTER_BOUND('',#466,.T.);
#325=FACE_OUTER_BOUND('',#467,.T.);
#326=FACE_OUTER_BOUND('',#468,.T.);
#327=FACE_OUTER_BOUND('',#469,.T.);
#328=FACE_OUTER_BOUND('',#470,.T.);
#329=FACE_OUTER_BOUND('',#471,.T.);
#330=FACE_OUTER_BOUND('',#472,.T.);
#331=FACE_OUTER_BOUND('',#473,.T.);
#332=FACE_OUTER_BOUND('',#474,.T.);
#333=FACE_OUTER_BOUND('',#475,.T.);
#334=FACE_OUTER_BOUND('',#476,.T.);
#335=FACE_OUTER_BOUND('',#477,.T.);
#336=FACE_OUTER_BOUND('',#478,.T.);
#337=FACE_OUTER_BOUND('',#479,.T.);
#338=FACE_OUTER_BOUND('',#480,.T.);
#339=FACE_OUTER_BOUND('',#481,.T.);
#340=FACE_OUTER_BOUND('',#482,.T.);
#341=FACE_OUTER_BOUND('',#483,.T.);
#342=FACE_OUTER_BOUND('',#484,.T.);
#343=FACE_OUTER_BOUND('',#485,.T.);
#344=FACE_OUTER_BOUND('',#486,.T.);
#345=FACE_OUTER_BOUND('',#487,.T.);
#346=FACE_OUTER_BOUND('',#488,.T.);
#347=FACE_OUTER_BOUND('',#489,.T.);
#348=FACE_OUTER_BOUND('',#490,.T.);
#349=FACE_OUTER_BOUND('',#491,.T.);
#350=FACE_OUTER_BOUND('',#492,.T.);
#351=FACE_OUTER_BOUND('',#494,.T.);
#352=FACE_OUTER_BOUND('',#495,.T.);
#353=FACE_OUTER_BOUND('',#496,.T.);
#354=FACE_OUTER_BOUND('',#497,.T.);
#355=FACE_OUTER_BOUND('',#498,.T.);
#356=FACE_OUTER_BOUND('',#499,.T.);
#357=FACE_OUTER_BOUND('',#500,.T.);
#358=FACE_OUTER_BOUND('',#501,.T.);
#359=FACE_OUTER_BOUND('',#502,.T.);
#360=FACE_OUTER_BOUND('',#503,.T.);
#361=FACE_OUTER_BOUND('',#504,.T.);
#362=FACE_OUTER_BOUND('',#505,.T.);
#363=FACE_OUTER_BOUND('',#506,.T.);
#364=FACE_OUTER_BOUND('',#507,.T.);
#365=FACE_OUTER_BOUND('',#508,.T.);
#366=FACE_OUTER_BOUND('',#509,.T.);
#367=FACE_OUTER_BOUND('',#510,.T.);
#368=FACE_OUTER_BOUND('',#511,.T.);
#369=FACE_OUTER_BOUND('',#512,.T.);
#455=EDGE_LOOP('',(#1556,#1557,#1558,#1559));
#456=EDGE_LOOP('',(#1560,#1561,#1562,#1563));
#457=EDGE_LOOP('',(#1564,#1565,#1566,#1567));
#458=EDGE_LOOP('',(#1568,#1569,#1570,#1571));
#459=EDGE_LOOP('',(#1572,#1573,#1574,#1575));
#460=EDGE_LOOP('',(#1576,#1577,#1578,#1579));
#461=EDGE_LOOP('',(#1580,#1581,#1582,#1583));
#462=EDGE_LOOP('',(#1584,#1585,#1586,#1587));
#463=EDGE_LOOP('',(#1588,#1589,#1590,#1591));
#464=EDGE_LOOP('',(#1592,#1593,#1594,#1595));
#465=EDGE_LOOP('',(#1596,#1597,#1598,#1599));
#466=EDGE_LOOP('',(#1600,#1601,#1602,#1603));
#467=EDGE_LOOP('',(#1604,#1605,#1606,#1607));
#468=EDGE_LOOP('',(#1608,#1609,#1610,#1611,#1612,#1613,#1614,#1615,#1616));
#469=EDGE_LOOP('',(#1617,#1618,#1619,#1620));
#470=EDGE_LOOP('',(#1621,#1622,#1623,#1624));
#471=EDGE_LOOP('',(#1625,#1626,#1627,#1628));
#472=EDGE_LOOP('',(#1629,#1630,#1631,#1632));
#473=EDGE_LOOP('',(#1633,#1634,#1635,#1636));
#474=EDGE_LOOP('',(#1637,#1638,#1639,#1640));
#475=EDGE_LOOP('',(#1641,#1642,#1643,#1644));
#476=EDGE_LOOP('',(#1645,#1646,#1647,#1648));
#477=EDGE_LOOP('',(#1649,#1650,#1651,#1652));
#478=EDGE_LOOP('',(#1653,#1654,#1655,#1656));
#479=EDGE_LOOP('',(#1657,#1658,#1659,#1660));
#480=EDGE_LOOP('',(#1661,#1662,#1663,#1664));
#481=EDGE_LOOP('',(#1665,#1666,#1667,#1668,#1669,#1670,#1671,#1672,#1673,
#1674,#1675));
#482=EDGE_LOOP('',(#1676,#1677,#1678,#1679,#1680));
#483=EDGE_LOOP('',(#1681,#1682,#1683,#1684));
#484=EDGE_LOOP('',(#1685,#1686,#1687,#1688));
#485=EDGE_LOOP('',(#1689,#1690,#1691));
#486=EDGE_LOOP('',(#1692,#1693,#1694,#1695,#1696,#1697));
#487=EDGE_LOOP('',(#1698,#1699,#1700,#1701,#1702,#1703,#1704,#1705,#1706,
#1707,#1708,#1709,#1710,#1711,#1712,#1713,#1714,#1715,#1716,#1717,#1718,
#1719,#1720,#1721,#1722,#1723,#1724,#1725,#1726,#1727,#1728));
#488=EDGE_LOOP('',(#1729,#1730,#1731,#1732,#1733));
#489=EDGE_LOOP('',(#1734,#1735,#1736,#1737,#1738,#1739,#1740,#1741,#1742,
#1743,#1744,#1745,#1746,#1747,#1748,#1749,#1750,#1751,#1752,#1753,#1754,
#1755,#1756,#1757,#1758,#1759,#1760,#1761,#1762,#1763,#1764,#1765,#1766));
#490=EDGE_LOOP('',(#1767));
#491=EDGE_LOOP('',(#1768,#1769,#1770,#1771,#1772));
#492=EDGE_LOOP('',(#1773));
#493=EDGE_LOOP('',(#1774,#1775,#1776,#1777,#1778,#1779));
#494=EDGE_LOOP('',(#1780,#1781,#1782,#1783));
#495=EDGE_LOOP('',(#1784,#1785,#1786,#1787));
#496=EDGE_LOOP('',(#1788,#1789,#1790,#1791));
#497=EDGE_LOOP('',(#1792,#1793,#1794,#1795));
#498=EDGE_LOOP('',(#1796,#1797,#1798,#1799));
#499=EDGE_LOOP('',(#1800,#1801,#1802,#1803));
#500=EDGE_LOOP('',(#1804,#1805,#1806,#1807));
#501=EDGE_LOOP('',(#1808,#1809,#1810,#1811));
#502=EDGE_LOOP('',(#1812,#1813,#1814,#1815));
#503=EDGE_LOOP('',(#1816,#1817,#1818,#1819));
#504=EDGE_LOOP('',(#1820,#1821,#1822,#1823));
#505=EDGE_LOOP('',(#1824,#1825,#1826,#1827));
#506=EDGE_LOOP('',(#1828,#1829,#1830,#1831));
#507=EDGE_LOOP('',(#1832,#1833,#1834,#1835));
#508=EDGE_LOOP('',(#1836,#1837,#1838,#1839));
#509=EDGE_LOOP('',(#1840,#1841,#1842,#1843));
#510=EDGE_LOOP('',(#1844,#1845,#1846,#1847));
#511=EDGE_LOOP('',(#1848,#1849,#1850,#1851));
#512=EDGE_LOOP('',(#1852,#1853,#1854,#1855,#1856,#1857));
#577=LINE('',#3151,#713);
#578=LINE('',#3178,#714);
#579=LINE('',#3208,#715);
#580=LINE('',#3238,#716);
#581=LINE('',#3268,#717);
#582=LINE('',#3298,#718);
#583=LINE('',#3328,#719);
#584=LINE('',#3358,#720);
#585=LINE('',#3388,#721);
#586=LINE('',#3418,#722);
#587=LINE('',#3448,#723);
#588=LINE('',#3478,#724);
#589=LINE('',#3508,#725);
#590=LINE('',#3538,#726);
#591=LINE('',#3563,#727);
#592=LINE('',#3588,#728);
#593=LINE('',#3664,#729);
#594=LINE('',#3740,#730);
#595=LINE('',#3816,#731);
#596=LINE('',#3892,#732);
#597=LINE('',#3968,#733);
#598=LINE('',#4046,#734);
#599=LINE('',#4124,#735);
#600=LINE('',#4200,#736);
#601=LINE('',#4276,#737);
#602=LINE('',#4352,#738);
#603=LINE('',#4428,#739);
#604=LINE('',#4504,#740);
#605=LINE('',#4559,#741);
#606=LINE('',#4586,#742);
#607=LINE('',#9790,#743);
#608=LINE('',#9792,#744);
#609=LINE('',#9794,#745);
#610=LINE('',#9796,#746);
#611=LINE('',#9798,#747);
#612=LINE('',#9799,#748);
#613=LINE('',#9803,#749);
#614=LINE('',#9805,#750);
#615=LINE('',#9807,#751);
#616=LINE('',#9808,#752);
#617=LINE('',#9812,#753);
#618=LINE('',#9813,#754);
#619=LINE('',#9814,#755);
#620=LINE('',#9818,#756);
#621=LINE('',#9819,#757);
#622=LINE('',#9820,#758);
#623=LINE('',#9824,#759);
#624=LINE('',#9825,#760);
#625=LINE('',#9826,#761);
#626=LINE('',#9830,#762);
#627=LINE('',#9831,#763);
#628=LINE('',#9832,#764);
#629=LINE('',#9834,#765);
#630=LINE('',#9835,#766);
#631=LINE('',#9837,#767);
#632=LINE('',#9838,#768);
#633=LINE('',#9840,#769);
#634=LINE('',#9842,#770);
#635=LINE('',#9844,#771);
#636=LINE('',#9846,#772);
#637=LINE('',#9850,#773);
#638=LINE('',#9852,#774);
#639=LINE('',#9853,#775);
#640=LINE('',#9856,#776);
#641=LINE('',#9857,#777);
#642=LINE('',#9860,#778);
#643=LINE('',#9861,#779);
#644=LINE('',#9864,#780);
#645=LINE('',#9865,#781);
#646=LINE('',#9868,#782);
#647=LINE('',#9869,#783);
#648=LINE('',#9871,#784);
#713=VECTOR('',#2640,1.6211138875);
#714=VECTOR('',#2645,1.6211138875);
#715=VECTOR('',#2648,1.6211138875);
#716=VECTOR('',#2651,1.6211138875);
#717=VECTOR('',#2654,1.6211138875);
#718=VECTOR('',#2657,1.6211138875);
#719=VECTOR('',#2660,1.6211138875);
#720=VECTOR('',#2663,1.6211138875);
#721=VECTOR('',#2666,1.6211138875);
#722=VECTOR('',#2669,1.6211138875);
#723=VECTOR('',#2672,1.6211138875);
#724=VECTOR('',#2675,1.6211138875);
#725=VECTOR('',#2678,1.6211138875);
#726=VECTOR('',#2681,2.);
#727=VECTOR('',#2684,2.);
#728=VECTOR('',#2693,2.);
#729=VECTOR('',#2696,2.);
#730=VECTOR('',#2699,2.);
#731=VECTOR('',#2702,2.);
#732=VECTOR('',#2705,2.);
#733=VECTOR('',#2708,2.);
#734=VECTOR('',#2711,2.);
#735=VECTOR('',#2714,2.);
#736=VECTOR('',#2717,2.);
#737=VECTOR('',#2720,2.);
#738=VECTOR('',#2723,2.);
#739=VECTOR('',#2726,2.);
#740=VECTOR('',#2729,2.01);
#741=VECTOR('',#2734,2.01);
#742=VECTOR('',#2755,2.);
#743=VECTOR('',#2770,1000.);
#744=VECTOR('',#2771,1000.);
#745=VECTOR('',#2772,1000.);
#746=VECTOR('',#2773,1000.);
#747=VECTOR('',#2774,1000.);
#748=VECTOR('',#2775,1000.);
#749=VECTOR('',#2778,1000.);
#750=VECTOR('',#2779,1000.);
#751=VECTOR('',#2780,1000.);
#752=VECTOR('',#2781,1000.);
#753=VECTOR('',#2784,1000.);
#754=VECTOR('',#2785,1000.);
#755=VECTOR('',#2786,1000.);
#756=VECTOR('',#2789,1000.);
#757=VECTOR('',#2790,1000.);
#758=VECTOR('',#2791,1000.);
#759=VECTOR('',#2794,1000.);
#760=VECTOR('',#2795,1000.);
#761=VECTOR('',#2796,1000.);
#762=VECTOR('',#2799,1000.);
#763=VECTOR('',#2800,1000.);
#764=VECTOR('',#2801,1000.);
#765=VECTOR('',#2804,1000.);
#766=VECTOR('',#2805,1000.);
#767=VECTOR('',#2808,1000.);
#768=VECTOR('',#2809,1000.);
#769=VECTOR('',#2812,1000.);
#770=VECTOR('',#2815,1000.);
#771=VECTOR('',#2818,1000.);
#772=VECTOR('',#2821,1000.);
#773=VECTOR('',#2826,1000.);
#774=VECTOR('',#2827,1000.);
#775=VECTOR('',#2828,1000.);
#776=VECTOR('',#2831,1000.);
#777=VECTOR('',#2832,1000.);
#778=VECTOR('',#2835,1000.);
#779=VECTOR('',#2836,1000.);
#780=VECTOR('',#2839,1000.);
#781=VECTOR('',#2840,1000.);
#782=VECTOR('',#2843,1000.);
#783=VECTOR('',#2844,1000.);
#784=VECTOR('',#2847,1000.);
#844=CIRCLE('',#2236,1.6211138875);
#845=CIRCLE('',#2250,2.);
#846=CIRCLE('',#2251,2.);
#847=CIRCLE('',#2252,2.);
#848=CIRCLE('',#2253,2.);
#849=CIRCLE('',#2267,2.);
#850=CIRCLE('',#2268,1.6211138875);
#851=CIRCLE('',#2269,1.55999999999999);
#852=CIRCLE('',#2270,1.6211138875);
#853=CIRCLE('',#2272,2.11715728752538);
#854=CIRCLE('',#2273,0.4);
#855=CIRCLE('',#2275,3.9385786437627);
#856=CIRCLE('',#2276,0.1);
#857=CIRCLE('',#2277,4.00928932188135);
#858=CIRCLE('',#2280,2.);
#939=VERTEX_POINT('',#3149);
#940=VERTEX_POINT('',#3150);
#941=VERTEX_POINT('',#3152);
#942=VERTEX_POINT('',#3164);
#943=VERTEX_POINT('',#3176);
#944=VERTEX_POINT('',#3177);
#945=VERTEX_POINT('',#3206);
#946=VERTEX_POINT('',#3207);
#947=VERTEX_POINT('',#3236);
#948=VERTEX_POINT('',#3237);
#949=VERTEX_POINT('',#3266);
#950=VERTEX_POINT('',#3267);
#951=VERTEX_POINT('',#3296);
#952=VERTEX_POINT('',#3297);
#953=VERTEX_POINT('',#3326);
#954=VERTEX_POINT('',#3327);
#955=VERTEX_POINT('',#3356);
#956=VERTEX_POINT('',#3357);
#957=VERTEX_POINT('',#3386);
#958=VERTEX_POINT('',#3387);
#959=VERTEX_POINT('',#3416);
#960=VERTEX_POINT('',#3417);
#961=VERTEX_POINT('',#3446);
#962=VERTEX_POINT('',#3447);
#963=VERTEX_POINT('',#3476);
#964=VERTEX_POINT('',#3477);
#965=VERTEX_POINT('',#3506);
#966=VERTEX_POINT('',#3507);
#967=VERTEX_POINT('',#3536);
#968=VERTEX_POINT('',#3537);
#969=VERTEX_POINT('',#3539);
#970=VERTEX_POINT('',#3560);
#971=VERTEX_POINT('',#3562);
#972=VERTEX_POINT('',#3564);
#973=VERTEX_POINT('',#3567);
#974=VERTEX_POINT('',#3586);
#975=VERTEX_POINT('',#3587);
#976=VERTEX_POINT('',#3662);
#977=VERTEX_POINT('',#3663);
#978=VERTEX_POINT('',#3738);
#979=VERTEX_POINT('',#3739);
#980=VERTEX_POINT('',#3814);
#981=VERTEX_POINT('',#3815);
#982=VERTEX_POINT('',#3890);
#983=VERTEX_POINT('',#3891);
#984=VERTEX_POINT('',#3966);
#985=VERTEX_POINT('',#3967);
#986=VERTEX_POINT('',#4044);
#987=VERTEX_POINT('',#4045);
#988=VERTEX_POINT('',#4122);
#989=VERTEX_POINT('',#4123);
#990=VERTEX_POINT('',#4198);
#991=VERTEX_POINT('',#4199);
#992=VERTEX_POINT('',#4274);
#993=VERTEX_POINT('',#4275);
#994=VERTEX_POINT('',#4350);
#995=VERTEX_POINT('',#4351);
#996=VERTEX_POINT('',#4426);
#997=VERTEX_POINT('',#4427);
#998=VERTEX_POINT('',#4502);
#999=VERTEX_POINT('',#4503);
#1000=VERTEX_POINT('',#4505);
#1001=VERTEX_POINT('',#4507);
#1002=VERTEX_POINT('',#4518);
#1003=VERTEX_POINT('',#4537);
#1004=VERTEX_POINT('',#4556);
#1005=VERTEX_POINT('',#4558);
#1006=VERTEX_POINT('',#4561);
#1007=VERTEX_POINT('',#4576);
#1008=VERTEX_POINT('',#4580);
#1009=VERTEX_POINT('',#4582);
#1010=VERTEX_POINT('',#4588);
#1011=VERTEX_POINT('',#4595);
#1012=VERTEX_POINT('',#9788);
#1013=VERTEX_POINT('',#9789);
#1014=VERTEX_POINT('',#9791);
#1015=VERTEX_POINT('',#9793);
#1016=VERTEX_POINT('',#9795);
#1017=VERTEX_POINT('',#9797);
#1018=VERTEX_POINT('',#9801);
#1019=VERTEX_POINT('',#9802);
#1020=VERTEX_POINT('',#9804);
#1021=VERTEX_POINT('',#9806);
#1022=VERTEX_POINT('',#9810);
#1023=VERTEX_POINT('',#9811);
#1024=VERTEX_POINT('',#9816);
#1025=VERTEX_POINT('',#9817);
#1026=VERTEX_POINT('',#9822);
#1027=VERTEX_POINT('',#9823);
#1028=VERTEX_POINT('',#9828);
#1029=VERTEX_POINT('',#9829);
#1030=VERTEX_POINT('',#9849);
#1031=VERTEX_POINT('',#9851);
#1032=VERTEX_POINT('',#9855);
#1033=VERTEX_POINT('',#9859);
#1034=VERTEX_POINT('',#9863);
#1035=VERTEX_POINT('',#9867);
#1159=EDGE_CURVE('',#939,#940,#577,.T.);
#1160=EDGE_CURVE('',#941,#939,#101,.T.);
#1161=EDGE_CURVE('',#941,#942,#844,.T.);
#1162=EDGE_CURVE('',#942,#940,#102,.T.);
#1163=EDGE_CURVE('',#943,#944,#578,.T.);
#1164=EDGE_CURVE('',#939,#943,#103,.T.);
#1165=EDGE_CURVE('',#940,#944,#104,.T.);
#1166=EDGE_CURVE('',#945,#946,#579,.T.);
#1167=EDGE_CURVE('',#943,#945,#105,.T.);
#1168=EDGE_CURVE('',#944,#946,#106,.T.);
#1169=EDGE_CURVE('',#947,#948,#580,.T.);
#1170=EDGE_CURVE('',#945,#947,#107,.T.);
#1171=EDGE_CURVE('',#946,#948,#108,.T.);
#1172=EDGE_CURVE('',#949,#950,#581,.T.);
#1173=EDGE_CURVE('',#947,#949,#109,.T.);
#1174=EDGE_CURVE('',#948,#950,#110,.T.);
#1175=EDGE_CURVE('',#951,#952,#582,.T.);
#1176=EDGE_CURVE('',#949,#951,#111,.T.);
#1177=EDGE_CURVE('',#950,#952,#112,.T.);
#1178=EDGE_CURVE('',#953,#954,#583,.T.);
#1179=EDGE_CURVE('',#951,#953,#113,.T.);
#1180=EDGE_CURVE('',#952,#954,#114,.T.);
#1181=EDGE_CURVE('',#955,#956,#584,.T.);
#1182=EDGE_CURVE('',#953,#955,#115,.T.);
#1183=EDGE_CURVE('',#954,#956,#116,.T.);
#1184=EDGE_CURVE('',#957,#958,#585,.T.);
#1185=EDGE_CURVE('',#955,#957,#117,.T.);
#1186=EDGE_CURVE('',#956,#958,#118,.T.);
#1187=EDGE_CURVE('',#959,#960,#586,.T.);
#1188=EDGE_CURVE('',#957,#959,#119,.T.);
#1189=EDGE_CURVE('',#958,#960,#120,.T.);
#1190=EDGE_CURVE('',#961,#962,#587,.T.);
#1191=EDGE_CURVE('',#959,#961,#121,.T.);
#1192=EDGE_CURVE('',#960,#962,#122,.T.);
#1193=EDGE_CURVE('',#963,#964,#588,.T.);
#1194=EDGE_CURVE('',#961,#963,#123,.T.);
#1195=EDGE_CURVE('',#962,#964,#124,.T.);
#1196=EDGE_CURVE('',#965,#966,#589,.T.);
#1197=EDGE_CURVE('',#963,#965,#125,.T.);
#1198=EDGE_CURVE('',#964,#966,#126,.T.);
#1199=EDGE_CURVE('',#967,#968,#590,.T.);
#1200=EDGE_CURVE('',#969,#967,#65,.F.);
#1201=EDGE_CURVE('',#969,#970,#845,.T.);
#1202=EDGE_CURVE('',#970,#971,#591,.T.);
#1203=EDGE_CURVE('',#971,#972,#846,.T.);
#1204=EDGE_CURVE('',#972,#971,#847,.T.);
#1205=EDGE_CURVE('',#970,#973,#848,.T.);
#1206=EDGE_CURVE('',#973,#968,#66,.T.);
#1207=EDGE_CURVE('',#974,#975,#592,.T.);
#1208=EDGE_CURVE('',#967,#974,#67,.F.);
#1209=EDGE_CURVE('',#968,#975,#68,.T.);
#1210=EDGE_CURVE('',#976,#977,#593,.T.);
#1211=EDGE_CURVE('',#974,#976,#69,.F.);
#1212=EDGE_CURVE('',#975,#977,#70,.T.);
#1213=EDGE_CURVE('',#978,#979,#594,.T.);
#1214=EDGE_CURVE('',#976,#978,#71,.F.);
#1215=EDGE_CURVE('',#977,#979,#72,.T.);
#1216=EDGE_CURVE('',#980,#981,#595,.T.);
#1217=EDGE_CURVE('',#978,#980,#73,.F.);
#1218=EDGE_CURVE('',#979,#981,#74,.T.);
#1219=EDGE_CURVE('',#982,#983,#596,.T.);
#1220=EDGE_CURVE('',#980,#982,#75,.F.);
#1221=EDGE_CURVE('',#981,#983,#76,.T.);
#1222=EDGE_CURVE('',#984,#985,#597,.T.);
#1223=EDGE_CURVE('',#982,#984,#77,.F.);
#1224=EDGE_CURVE('',#983,#985,#78,.T.);
#1225=EDGE_CURVE('',#986,#987,#598,.T.);
#1226=EDGE_CURVE('',#984,#986,#79,.F.);
#1227=EDGE_CURVE('',#985,#987,#80,.T.);
#1228=EDGE_CURVE('',#988,#989,#599,.T.);
#1229=EDGE_CURVE('',#986,#988,#81,.F.);
#1230=EDGE_CURVE('',#987,#989,#82,.T.);
#1231=EDGE_CURVE('',#990,#991,#600,.T.);
#1232=EDGE_CURVE('',#988,#990,#83,.F.);
#1233=EDGE_CURVE('',#989,#991,#84,.T.);
#1234=EDGE_CURVE('',#992,#993,#601,.T.);
#1235=EDGE_CURVE('',#990,#992,#85,.F.);
#1236=EDGE_CURVE('',#991,#993,#86,.T.);
#1237=EDGE_CURVE('',#994,#995,#602,.T.);
#1238=EDGE_CURVE('',#992,#994,#87,.F.);
#1239=EDGE_CURVE('',#993,#995,#88,.T.);
#1240=EDGE_CURVE('',#996,#997,#603,.T.);
#1241=EDGE_CURVE('',#994,#996,#89,.F.);
#1242=EDGE_CURVE('',#995,#997,#90,.T.);
#1243=EDGE_CURVE('',#998,#999,#604,.T.);
#1244=EDGE_CURVE('',#1000,#998,#849,.T.);
#1245=EDGE_CURVE('',#1000,#1001,#91,.T.);
#1246=EDGE_CURVE('',#1001,#1002,#92,.T.);
#1247=EDGE_CURVE('',#1002,#1003,#93,.T.);
#1248=EDGE_CURVE('',#1003,#1004,#850,.T.);
#1249=EDGE_CURVE('',#1004,#1005,#605,.T.);
#1250=EDGE_CURVE('',#1005,#1005,#851,.T.);
#1251=EDGE_CURVE('',#1004,#1006,#852,.T.);
#1252=EDGE_CURVE('',#1006,#999,#94,.T.);
#1253=EDGE_CURVE('',#1007,#1007,#853,.T.);
#1254=EDGE_CURVE('',#1007,#972,#854,.T.);
#1255=EDGE_CURVE('',#1008,#1008,#855,.T.);
#1256=EDGE_CURVE('',#1008,#1009,#856,.T.);
#1257=EDGE_CURVE('',#1009,#1009,#857,.T.);
#1258=EDGE_CURVE('',#1009,#1007,#606,.T.);
#1259=EDGE_CURVE('',#999,#1010,#95,.T.);
#1260=EDGE_CURVE('',#998,#1010,#858,.T.);
#1261=EDGE_CURVE('',#997,#1011,#96,.T.);
#1262=EDGE_CURVE('',#1011,#1000,#97,.T.);
#1263=EDGE_CURVE('',#996,#1010,#98,.F.);
#1264=EDGE_CURVE('',#942,#969,#99,.T.);
#1265=EDGE_CURVE('',#966,#1006,#127,.T.);
#1266=EDGE_CURVE('',#965,#1003,#128,.T.);
#1267=EDGE_CURVE('',#973,#941,#100,.T.);
#1268=EDGE_CURVE('',#1012,#1013,#607,.T.);
#1269=EDGE_CURVE('',#1013,#1014,#608,.T.);
#1270=EDGE_CURVE('',#1014,#1015,#609,.T.);
#1271=EDGE_CURVE('',#1015,#1016,#610,.T.);
#1272=EDGE_CURVE('',#1016,#1017,#611,.T.);
#1273=EDGE_CURVE('',#1017,#1012,#612,.T.);
#1274=EDGE_CURVE('',#1018,#1019,#613,.T.);
#1275=EDGE_CURVE('',#1019,#1020,#614,.T.);
#1276=EDGE_CURVE('',#1021,#1020,#615,.T.);
#1277=EDGE_CURVE('',#1018,#1021,#616,.T.);
#1278=EDGE_CURVE('',#1022,#1023,#617,.T.);
#1279=EDGE_CURVE('',#1023,#1019,#618,.T.);
#1280=EDGE_CURVE('',#1022,#1018,#619,.T.);
#1281=EDGE_CURVE('',#1024,#1025,#620,.T.);
#1282=EDGE_CURVE('',#1025,#1023,#621,.T.);
#1283=EDGE_CURVE('',#1024,#1022,#622,.T.);
#1284=EDGE_CURVE('',#1026,#1027,#623,.T.);
#1285=EDGE_CURVE('',#1027,#1025,#624,.T.);
#1286=EDGE_CURVE('',#1026,#1024,#625,.T.);
#1287=EDGE_CURVE('',#1028,#1029,#626,.T.);
#1288=EDGE_CURVE('',#1029,#1027,#627,.T.);
#1289=EDGE_CURVE('',#1028,#1026,#628,.T.);
#1290=EDGE_CURVE('',#1020,#1029,#629,.T.);
#1291=EDGE_CURVE('',#1021,#1028,#630,.T.);
#1292=EDGE_CURVE('',#1017,#1023,#631,.T.);
#1293=EDGE_CURVE('',#1019,#1016,#632,.T.);
#1294=EDGE_CURVE('',#1020,#1015,#633,.T.);
#1295=EDGE_CURVE('',#1012,#1025,#634,.T.);
#1296=EDGE_CURVE('',#1029,#1014,#635,.T.);
#1297=EDGE_CURVE('',#1013,#1027,#636,.T.);
#1298=EDGE_CURVE('',#1030,#1021,#637,.T.);
#1299=EDGE_CURVE('',#1031,#1030,#638,.T.);
#1300=EDGE_CURVE('',#1031,#1018,#639,.T.);
#1301=EDGE_CURVE('',#1032,#1031,#640,.T.);
#1302=EDGE_CURVE('',#1032,#1022,#641,.T.);
#1303=EDGE_CURVE('',#1033,#1032,#642,.T.);
#1304=EDGE_CURVE('',#1033,#1024,#643,.T.);
#1305=EDGE_CURVE('',#1034,#1033,#644,.T.);
#1306=EDGE_CURVE('',#1034,#1026,#645,.T.);
#1307=EDGE_CURVE('',#1035,#1034,#646,.T.);
#1308=EDGE_CURVE('',#1035,#1028,#647,.T.);
#1309=EDGE_CURVE('',#1030,#1035,#648,.T.);
#1556=ORIENTED_EDGE('',*,*,#1159,.F.);
#1557=ORIENTED_EDGE('',*,*,#1160,.F.);
#1558=ORIENTED_EDGE('',*,*,#1161,.T.);
#1559=ORIENTED_EDGE('',*,*,#1162,.T.);
#1560=ORIENTED_EDGE('',*,*,#1163,.F.);
#1561=ORIENTED_EDGE('',*,*,#1164,.F.);
#1562=ORIENTED_EDGE('',*,*,#1159,.T.);
#1563=ORIENTED_EDGE('',*,*,#1165,.T.);
#1564=ORIENTED_EDGE('',*,*,#1166,.F.);
#1565=ORIENTED_EDGE('',*,*,#1167,.F.);
#1566=ORIENTED_EDGE('',*,*,#1163,.T.);
#1567=ORIENTED_EDGE('',*,*,#1168,.T.);
#1568=ORIENTED_EDGE('',*,*,#1169,.F.);
#1569=ORIENTED_EDGE('',*,*,#1170,.F.);
#1570=ORIENTED_EDGE('',*,*,#1166,.T.);
#1571=ORIENTED_EDGE('',*,*,#1171,.T.);
#1572=ORIENTED_EDGE('',*,*,#1172,.F.);
#1573=ORIENTED_EDGE('',*,*,#1173,.F.);
#1574=ORIENTED_EDGE('',*,*,#1169,.T.);
#1575=ORIENTED_EDGE('',*,*,#1174,.T.);
#1576=ORIENTED_EDGE('',*,*,#1175,.F.);
#1577=ORIENTED_EDGE('',*,*,#1176,.F.);
#1578=ORIENTED_EDGE('',*,*,#1172,.T.);
#1579=ORIENTED_EDGE('',*,*,#1177,.T.);
#1580=ORIENTED_EDGE('',*,*,#1178,.F.);
#1581=ORIENTED_EDGE('',*,*,#1179,.F.);
#1582=ORIENTED_EDGE('',*,*,#1175,.T.);
#1583=ORIENTED_EDGE('',*,*,#1180,.T.);
#1584=ORIENTED_EDGE('',*,*,#1181,.F.);
#1585=ORIENTED_EDGE('',*,*,#1182,.F.);
#1586=ORIENTED_EDGE('',*,*,#1178,.T.);
#1587=ORIENTED_EDGE('',*,*,#1183,.T.);
#1588=ORIENTED_EDGE('',*,*,#1184,.F.);
#1589=ORIENTED_EDGE('',*,*,#1185,.F.);
#1590=ORIENTED_EDGE('',*,*,#1181,.T.);
#1591=ORIENTED_EDGE('',*,*,#1186,.T.);
#1592=ORIENTED_EDGE('',*,*,#1187,.F.);
#1593=ORIENTED_EDGE('',*,*,#1188,.F.);
#1594=ORIENTED_EDGE('',*,*,#1184,.T.);
#1595=ORIENTED_EDGE('',*,*,#1189,.T.);
#1596=ORIENTED_EDGE('',*,*,#1190,.F.);
#1597=ORIENTED_EDGE('',*,*,#1191,.F.);
#1598=ORIENTED_EDGE('',*,*,#1187,.T.);
#1599=ORIENTED_EDGE('',*,*,#1192,.T.);
#1600=ORIENTED_EDGE('',*,*,#1193,.F.);
#1601=ORIENTED_EDGE('',*,*,#1194,.F.);
#1602=ORIENTED_EDGE('',*,*,#1190,.T.);
#1603=ORIENTED_EDGE('',*,*,#1195,.T.);
#1604=ORIENTED_EDGE('',*,*,#1196,.F.);
#1605=ORIENTED_EDGE('',*,*,#1197,.F.);
#1606=ORIENTED_EDGE('',*,*,#1193,.T.);
#1607=ORIENTED_EDGE('',*,*,#1198,.T.);
#1608=ORIENTED_EDGE('',*,*,#1199,.F.);
#1609=ORIENTED_EDGE('',*,*,#1200,.F.);
#1610=ORIENTED_EDGE('',*,*,#1201,.T.);
#1611=ORIENTED_EDGE('',*,*,#1202,.T.);
#1612=ORIENTED_EDGE('',*,*,#1203,.T.);
#1613=ORIENTED_EDGE('',*,*,#1204,.T.);
#1614=ORIENTED_EDGE('',*,*,#1202,.F.);
#1615=ORIENTED_EDGE('',*,*,#1205,.T.);
#1616=ORIENTED_EDGE('',*,*,#1206,.T.);
#1617=ORIENTED_EDGE('',*,*,#1207,.F.);
#1618=ORIENTED_EDGE('',*,*,#1208,.F.);
#1619=ORIENTED_EDGE('',*,*,#1199,.T.);
#1620=ORIENTED_EDGE('',*,*,#1209,.T.);
#1621=ORIENTED_EDGE('',*,*,#1210,.F.);
#1622=ORIENTED_EDGE('',*,*,#1211,.F.);
#1623=ORIENTED_EDGE('',*,*,#1207,.T.);
#1624=ORIENTED_EDGE('',*,*,#1212,.T.);
#1625=ORIENTED_EDGE('',*,*,#1213,.F.);
#1626=ORIENTED_EDGE('',*,*,#1214,.F.);
#1627=ORIENTED_EDGE('',*,*,#1210,.T.);
#1628=ORIENTED_EDGE('',*,*,#1215,.T.);
#1629=ORIENTED_EDGE('',*,*,#1216,.F.);
#1630=ORIENTED_EDGE('',*,*,#1217,.F.);
#1631=ORIENTED_EDGE('',*,*,#1213,.T.);
#1632=ORIENTED_EDGE('',*,*,#1218,.T.);
#1633=ORIENTED_EDGE('',*,*,#1219,.F.);
#1634=ORIENTED_EDGE('',*,*,#1220,.F.);
#1635=ORIENTED_EDGE('',*,*,#1216,.T.);
#1636=ORIENTED_EDGE('',*,*,#1221,.T.);
#1637=ORIENTED_EDGE('',*,*,#1222,.F.);
#1638=ORIENTED_EDGE('',*,*,#1223,.F.);
#1639=ORIENTED_EDGE('',*,*,#1219,.T.);
#1640=ORIENTED_EDGE('',*,*,#1224,.T.);
#1641=ORIENTED_EDGE('',*,*,#1225,.F.);
#1642=ORIENTED_EDGE('',*,*,#1226,.F.);
#1643=ORIENTED_EDGE('',*,*,#1222,.T.);
#1644=ORIENTED_EDGE('',*,*,#1227,.T.);
#1645=ORIENTED_EDGE('',*,*,#1228,.F.);
#1646=ORIENTED_EDGE('',*,*,#1229,.F.);
#1647=ORIENTED_EDGE('',*,*,#1225,.T.);
#1648=ORIENTED_EDGE('',*,*,#1230,.T.);
#1649=ORIENTED_EDGE('',*,*,#1231,.F.);
#1650=ORIENTED_EDGE('',*,*,#1232,.F.);
#1651=ORIENTED_EDGE('',*,*,#1228,.T.);
#1652=ORIENTED_EDGE('',*,*,#1233,.T.);
#1653=ORIENTED_EDGE('',*,*,#1234,.F.);
#1654=ORIENTED_EDGE('',*,*,#1235,.F.);
#1655=ORIENTED_EDGE('',*,*,#1231,.T.);
#1656=ORIENTED_EDGE('',*,*,#1236,.T.);
#1657=ORIENTED_EDGE('',*,*,#1237,.F.);
#1658=ORIENTED_EDGE('',*,*,#1238,.F.);
#1659=ORIENTED_EDGE('',*,*,#1234,.T.);
#1660=ORIENTED_EDGE('',*,*,#1239,.T.);
#1661=ORIENTED_EDGE('',*,*,#1240,.F.);
#1662=ORIENTED_EDGE('',*,*,#1241,.F.);
#1663=ORIENTED_EDGE('',*,*,#1237,.T.);
#1664=ORIENTED_EDGE('',*,*,#1242,.T.);
#1665=ORIENTED_EDGE('',*,*,#1243,.F.);
#1666=ORIENTED_EDGE('',*,*,#1244,.F.);
#1667=ORIENTED_EDGE('',*,*,#1245,.T.);
#1668=ORIENTED_EDGE('',*,*,#1246,.T.);
#1669=ORIENTED_EDGE('',*,*,#1247,.T.);
#1670=ORIENTED_EDGE('',*,*,#1248,.T.);
#1671=ORIENTED_EDGE('',*,*,#1249,.T.);
#1672=ORIENTED_EDGE('',*,*,#1250,.F.);
#1673=ORIENTED_EDGE('',*,*,#1249,.F.);
#1674=ORIENTED_EDGE('',*,*,#1251,.T.);
#1675=ORIENTED_EDGE('',*,*,#1252,.T.);
#1676=ORIENTED_EDGE('',*,*,#1253,.F.);
#1677=ORIENTED_EDGE('',*,*,#1254,.T.);
#1678=ORIENTED_EDGE('',*,*,#1203,.F.);
#1679=ORIENTED_EDGE('',*,*,#1204,.F.);
#1680=ORIENTED_EDGE('',*,*,#1254,.F.);
#1681=ORIENTED_EDGE('',*,*,#1255,.F.);
#1682=ORIENTED_EDGE('',*,*,#1256,.T.);
#1683=ORIENTED_EDGE('',*,*,#1257,.F.);
#1684=ORIENTED_EDGE('',*,*,#1256,.F.);
#1685=ORIENTED_EDGE('',*,*,#1257,.T.);
#1686=ORIENTED_EDGE('',*,*,#1258,.T.);
#1687=ORIENTED_EDGE('',*,*,#1253,.T.);
#1688=ORIENTED_EDGE('',*,*,#1258,.F.);
#1689=ORIENTED_EDGE('',*,*,#1243,.T.);
#1690=ORIENTED_EDGE('',*,*,#1259,.T.);
#1691=ORIENTED_EDGE('',*,*,#1260,.F.);
#1692=ORIENTED_EDGE('',*,*,#1240,.T.);
#1693=ORIENTED_EDGE('',*,*,#1261,.T.);
#1694=ORIENTED_EDGE('',*,*,#1262,.T.);
#1695=ORIENTED_EDGE('',*,*,#1244,.T.);
#1696=ORIENTED_EDGE('',*,*,#1260,.T.);
#1697=ORIENTED_EDGE('',*,*,#1263,.F.);
#1698=ORIENTED_EDGE('',*,*,#1162,.F.);
#1699=ORIENTED_EDGE('',*,*,#1264,.T.);
#1700=ORIENTED_EDGE('',*,*,#1200,.T.);
#1701=ORIENTED_EDGE('',*,*,#1208,.T.);
#1702=ORIENTED_EDGE('',*,*,#1211,.T.);
#1703=ORIENTED_EDGE('',*,*,#1214,.T.);
#1704=ORIENTED_EDGE('',*,*,#1217,.T.);
#1705=ORIENTED_EDGE('',*,*,#1220,.T.);
#1706=ORIENTED_EDGE('',*,*,#1223,.T.);
#1707=ORIENTED_EDGE('',*,*,#1226,.T.);
#1708=ORIENTED_EDGE('',*,*,#1229,.T.);
#1709=ORIENTED_EDGE('',*,*,#1232,.T.);
#1710=ORIENTED_EDGE('',*,*,#1235,.T.);
#1711=ORIENTED_EDGE('',*,*,#1238,.T.);
#1712=ORIENTED_EDGE('',*,*,#1241,.T.);
#1713=ORIENTED_EDGE('',*,*,#1263,.T.);
#1714=ORIENTED_EDGE('',*,*,#1259,.F.);
#1715=ORIENTED_EDGE('',*,*,#1252,.F.);
#1716=ORIENTED_EDGE('',*,*,#1265,.F.);
#1717=ORIENTED_EDGE('',*,*,#1198,.F.);
#1718=ORIENTED_EDGE('',*,*,#1195,.F.);
#1719=ORIENTED_EDGE('',*,*,#1192,.F.);
#1720=ORIENTED_EDGE('',*,*,#1189,.F.);
#1721=ORIENTED_EDGE('',*,*,#1186,.F.);
#1722=ORIENTED_EDGE('',*,*,#1183,.F.);
#1723=ORIENTED_EDGE('',*,*,#1180,.F.);
#1724=ORIENTED_EDGE('',*,*,#1177,.F.);
#1725=ORIENTED_EDGE('',*,*,#1174,.F.);
#1726=ORIENTED_EDGE('',*,*,#1171,.F.);
#1727=ORIENTED_EDGE('',*,*,#1168,.F.);
#1728=ORIENTED_EDGE('',*,*,#1165,.F.);
#1729=ORIENTED_EDGE('',*,*,#1196,.T.);
#1730=ORIENTED_EDGE('',*,*,#1265,.T.);
#1731=ORIENTED_EDGE('',*,*,#1251,.F.);
#1732=ORIENTED_EDGE('',*,*,#1248,.F.);
#1733=ORIENTED_EDGE('',*,*,#1266,.F.);
#1734=ORIENTED_EDGE('',*,*,#1206,.F.);
#1735=ORIENTED_EDGE('',*,*,#1267,.T.);
#1736=ORIENTED_EDGE('',*,*,#1160,.T.);
#1737=ORIENTED_EDGE('',*,*,#1164,.T.);
#1738=ORIENTED_EDGE('',*,*,#1167,.T.);
#1739=ORIENTED_EDGE('',*,*,#1170,.T.);
#1740=ORIENTED_EDGE('',*,*,#1173,.T.);
#1741=ORIENTED_EDGE('',*,*,#1176,.T.);
#1742=ORIENTED_EDGE('',*,*,#1179,.T.);
#1743=ORIENTED_EDGE('',*,*,#1182,.T.);
#1744=ORIENTED_EDGE('',*,*,#1185,.T.);
#1745=ORIENTED_EDGE('',*,*,#1188,.T.);
#1746=ORIENTED_EDGE('',*,*,#1191,.T.);
#1747=ORIENTED_EDGE('',*,*,#1194,.T.);
#1748=ORIENTED_EDGE('',*,*,#1197,.T.);
#1749=ORIENTED_EDGE('',*,*,#1266,.T.);
#1750=ORIENTED_EDGE('',*,*,#1247,.F.);
#1751=ORIENTED_EDGE('',*,*,#1246,.F.);
#1752=ORIENTED_EDGE('',*,*,#1245,.F.);
#1753=ORIENTED_EDGE('',*,*,#1262,.F.);
#1754=ORIENTED_EDGE('',*,*,#1261,.F.);
#1755=ORIENTED_EDGE('',*,*,#1242,.F.);
#1756=ORIENTED_EDGE('',*,*,#1239,.F.);
#1757=ORIENTED_EDGE('',*,*,#1236,.F.);
#1758=ORIENTED_EDGE('',*,*,#1233,.F.);
#1759=ORIENTED_EDGE('',*,*,#1230,.F.);
#1760=ORIENTED_EDGE('',*,*,#1227,.F.);
#1761=ORIENTED_EDGE('',*,*,#1224,.F.);
#1762=ORIENTED_EDGE('',*,*,#1221,.F.);
#1763=ORIENTED_EDGE('',*,*,#1218,.F.);
#1764=ORIENTED_EDGE('',*,*,#1215,.F.);
#1765=ORIENTED_EDGE('',*,*,#1212,.F.);
#1766=ORIENTED_EDGE('',*,*,#1209,.F.);
#1767=ORIENTED_EDGE('',*,*,#1250,.T.);
#1768=ORIENTED_EDGE('',*,*,#1264,.F.);
#1769=ORIENTED_EDGE('',*,*,#1161,.F.);
#1770=ORIENTED_EDGE('',*,*,#1267,.F.);
#1771=ORIENTED_EDGE('',*,*,#1205,.F.);
#1772=ORIENTED_EDGE('',*,*,#1201,.F.);
#1773=ORIENTED_EDGE('',*,*,#1255,.T.);
#1774=ORIENTED_EDGE('',*,*,#1268,.T.);
#1775=ORIENTED_EDGE('',*,*,#1269,.T.);
#1776=ORIENTED_EDGE('',*,*,#1270,.T.);
#1777=ORIENTED_EDGE('',*,*,#1271,.T.);
#1778=ORIENTED_EDGE('',*,*,#1272,.T.);
#1779=ORIENTED_EDGE('',*,*,#1273,.T.);
#1780=ORIENTED_EDGE('',*,*,#1274,.T.);
#1781=ORIENTED_EDGE('',*,*,#1275,.T.);
#1782=ORIENTED_EDGE('',*,*,#1276,.F.);
#1783=ORIENTED_EDGE('',*,*,#1277,.F.);
#1784=ORIENTED_EDGE('',*,*,#1278,.T.);
#1785=ORIENTED_EDGE('',*,*,#1279,.T.);
#1786=ORIENTED_EDGE('',*,*,#1274,.F.);
#1787=ORIENTED_EDGE('',*,*,#1280,.F.);
#1788=ORIENTED_EDGE('',*,*,#1281,.T.);
#1789=ORIENTED_EDGE('',*,*,#1282,.T.);
#1790=ORIENTED_EDGE('',*,*,#1278,.F.);
#1791=ORIENTED_EDGE('',*,*,#1283,.F.);
#1792=ORIENTED_EDGE('',*,*,#1284,.T.);
#1793=ORIENTED_EDGE('',*,*,#1285,.T.);
#1794=ORIENTED_EDGE('',*,*,#1281,.F.);
#1795=ORIENTED_EDGE('',*,*,#1286,.F.);
#1796=ORIENTED_EDGE('',*,*,#1287,.T.);
#1797=ORIENTED_EDGE('',*,*,#1288,.T.);
#1798=ORIENTED_EDGE('',*,*,#1284,.F.);
#1799=ORIENTED_EDGE('',*,*,#1289,.F.);
#1800=ORIENTED_EDGE('',*,*,#1276,.T.);
#1801=ORIENTED_EDGE('',*,*,#1290,.T.);
#1802=ORIENTED_EDGE('',*,*,#1287,.F.);
#1803=ORIENTED_EDGE('',*,*,#1291,.F.);
#1804=ORIENTED_EDGE('',*,*,#1292,.F.);
#1805=ORIENTED_EDGE('',*,*,#1272,.F.);
#1806=ORIENTED_EDGE('',*,*,#1293,.F.);
#1807=ORIENTED_EDGE('',*,*,#1279,.F.);
#1808=ORIENTED_EDGE('',*,*,#1293,.T.);
#1809=ORIENTED_EDGE('',*,*,#1271,.F.);
#1810=ORIENTED_EDGE('',*,*,#1294,.F.);
#1811=ORIENTED_EDGE('',*,*,#1275,.F.);
#1812=ORIENTED_EDGE('',*,*,#1292,.T.);
#1813=ORIENTED_EDGE('',*,*,#1282,.F.);
#1814=ORIENTED_EDGE('',*,*,#1295,.F.);
#1815=ORIENTED_EDGE('',*,*,#1273,.F.);
#1816=ORIENTED_EDGE('',*,*,#1294,.T.);
#1817=ORIENTED_EDGE('',*,*,#1270,.F.);
#1818=ORIENTED_EDGE('',*,*,#1296,.F.);
#1819=ORIENTED_EDGE('',*,*,#1290,.F.);
#1820=ORIENTED_EDGE('',*,*,#1295,.T.);
#1821=ORIENTED_EDGE('',*,*,#1285,.F.);
#1822=ORIENTED_EDGE('',*,*,#1297,.F.);
#1823=ORIENTED_EDGE('',*,*,#1268,.F.);
#1824=ORIENTED_EDGE('',*,*,#1296,.T.);
#1825=ORIENTED_EDGE('',*,*,#1269,.F.);
#1826=ORIENTED_EDGE('',*,*,#1297,.T.);
#1827=ORIENTED_EDGE('',*,*,#1288,.F.);
#1828=ORIENTED_EDGE('',*,*,#1277,.T.);
#1829=ORIENTED_EDGE('',*,*,#1298,.F.);
#1830=ORIENTED_EDGE('',*,*,#1299,.F.);
#1831=ORIENTED_EDGE('',*,*,#1300,.T.);
#1832=ORIENTED_EDGE('',*,*,#1280,.T.);
#1833=ORIENTED_EDGE('',*,*,#1300,.F.);
#1834=ORIENTED_EDGE('',*,*,#1301,.F.);
#1835=ORIENTED_EDGE('',*,*,#1302,.T.);
#1836=ORIENTED_EDGE('',*,*,#1283,.T.);
#1837=ORIENTED_EDGE('',*,*,#1302,.F.);
#1838=ORIENTED_EDGE('',*,*,#1303,.F.);
#1839=ORIENTED_EDGE('',*,*,#1304,.T.);
#1840=ORIENTED_EDGE('',*,*,#1286,.T.);
#1841=ORIENTED_EDGE('',*,*,#1304,.F.);
#1842=ORIENTED_EDGE('',*,*,#1305,.F.);
#1843=ORIENTED_EDGE('',*,*,#1306,.T.);
#1844=ORIENTED_EDGE('',*,*,#1289,.T.);
#1845=ORIENTED_EDGE('',*,*,#1306,.F.);
#1846=ORIENTED_EDGE('',*,*,#1307,.F.);
#1847=ORIENTED_EDGE('',*,*,#1308,.T.);
#1848=ORIENTED_EDGE('',*,*,#1291,.T.);
#1849=ORIENTED_EDGE('',*,*,#1308,.F.);
#1850=ORIENTED_EDGE('',*,*,#1309,.F.);
#1851=ORIENTED_EDGE('',*,*,#1298,.T.);
#1852=ORIENTED_EDGE('',*,*,#1299,.T.);
#1853=ORIENTED_EDGE('',*,*,#1309,.T.);
#1854=ORIENTED_EDGE('',*,*,#1307,.T.);
#1855=ORIENTED_EDGE('',*,*,#1305,.T.);
#1856=ORIENTED_EDGE('',*,*,#1303,.T.);
#1857=ORIENTED_EDGE('',*,*,#1301,.T.);
#1876=CYLINDRICAL_SURFACE('',#2235,1.6211138875);
#1877=CYLINDRICAL_SURFACE('',#2237,1.6211138875);
#1878=CYLINDRICAL_SURFACE('',#2238,1.6211138875);
#1879=CYLINDRICAL_SURFACE('',#2239,1.6211138875);
#1880=CYLINDRICAL_SURFACE('',#2240,1.6211138875);
#1881=CYLINDRICAL_SURFACE('',#2241,1.6211138875);
#1882=CYLINDRICAL_SURFACE('',#2242,1.6211138875);
#1883=CYLINDRICAL_SURFACE('',#2243,1.6211138875);
#1884=CYLINDRICAL_SURFACE('',#2244,1.6211138875);
#1885=CYLINDRICAL_SURFACE('',#2245,1.6211138875);
#1886=CYLINDRICAL_SURFACE('',#2246,1.6211138875);
#1887=CYLINDRICAL_SURFACE('',#2247,1.6211138875);
#1888=CYLINDRICAL_SURFACE('',#2248,1.6211138875);
#1889=CYLINDRICAL_SURFACE('',#2249,2.);
#1890=CYLINDRICAL_SURFACE('',#2254,2.);
#1891=CYLINDRICAL_SURFACE('',#2255,2.);
#1892=CYLINDRICAL_SURFACE('',#2256,2.);
#1893=CYLINDRICAL_SURFACE('',#2257,2.);
#1894=CYLINDRICAL_SURFACE('',#2258,2.);
#1895=CYLINDRICAL_SURFACE('',#2259,2.);
#1896=CYLINDRICAL_SURFACE('',#2260,2.);
#1897=CYLINDRICAL_SURFACE('',#2261,2.);
#1898=CYLINDRICAL_SURFACE('',#2262,2.);
#1899=CYLINDRICAL_SURFACE('',#2263,2.);
#1900=CYLINDRICAL_SURFACE('',#2264,2.);
#1901=CYLINDRICAL_SURFACE('',#2265,2.);
#1902=CYLINDRICAL_SURFACE('',#2281,2.);
#1903=CYLINDRICAL_SURFACE('',#2282,1.6211138875);
#1965=ADVANCED_FACE('',(#313),#1876,.T.);
#1966=ADVANCED_FACE('',(#314),#1877,.T.);
#1967=ADVANCED_FACE('',(#315),#1878,.T.);
#1968=ADVANCED_FACE('',(#316),#1879,.T.);
#1969=ADVANCED_FACE('',(#317),#1880,.T.);
#1970=ADVANCED_FACE('',(#318),#1881,.T.);
#1971=ADVANCED_FACE('',(#319),#1882,.T.);
#1972=ADVANCED_FACE('',(#320),#1883,.T.);
#1973=ADVANCED_FACE('',(#321),#1884,.T.);
#1974=ADVANCED_FACE('',(#322),#1885,.T.);
#1975=ADVANCED_FACE('',(#323),#1886,.T.);
#1976=ADVANCED_FACE('',(#324),#1887,.T.);
#1977=ADVANCED_FACE('',(#325),#1888,.T.);
#1978=ADVANCED_FACE('',(#326),#1889,.T.);
#1979=ADVANCED_FACE('',(#327),#1890,.T.);
#1980=ADVANCED_FACE('',(#328),#1891,.T.);
#1981=ADVANCED_FACE('',(#329),#1892,.T.);
#1982=ADVANCED_FACE('',(#330),#1893,.T.);
#1983=ADVANCED_FACE('',(#331),#1894,.T.);
#1984=ADVANCED_FACE('',(#332),#1895,.T.);
#1985=ADVANCED_FACE('',(#333),#1896,.T.);
#1986=ADVANCED_FACE('',(#334),#1897,.T.);
#1987=ADVANCED_FACE('',(#335),#1898,.T.);
#1988=ADVANCED_FACE('',(#336),#1899,.T.);
#1989=ADVANCED_FACE('',(#337),#1900,.T.);
#1990=ADVANCED_FACE('',(#338),#1901,.T.);
#1991=ADVANCED_FACE('',(#339),#131,.T.);
#1992=ADVANCED_FACE('',(#340),#141,.F.);
#1993=ADVANCED_FACE('',(#341),#142,.T.);
#1994=ADVANCED_FACE('',(#342),#132,.T.);
#1995=ADVANCED_FACE('',(#343),#133,.T.);
#1996=ADVANCED_FACE('',(#344),#1902,.T.);
#1997=ADVANCED_FACE('',(#345),#63,.T.);
#1998=ADVANCED_FACE('',(#346),#1903,.T.);
#1999=ADVANCED_FACE('',(#347),#64,.T.);
#2000=ADVANCED_FACE('',(#348),#230,.F.);
#2001=ADVANCED_FACE('',(#349),#231,.F.);
#2002=ADVANCED_FACE('',(#350,#195),#232,.T.);
#2003=ADVANCED_FACE('',(#351),#233,.F.);
#2004=ADVANCED_FACE('',(#352),#234,.F.);
#2005=ADVANCED_FACE('',(#353),#235,.F.);
#2006=ADVANCED_FACE('',(#354),#236,.F.);
#2007=ADVANCED_FACE('',(#355),#237,.F.);
#2008=ADVANCED_FACE('',(#356),#238,.F.);
#2009=ADVANCED_FACE('',(#357),#239,.T.);
#2010=ADVANCED_FACE('',(#358),#240,.T.);
#2011=ADVANCED_FACE('',(#359),#241,.T.);
#2012=ADVANCED_FACE('',(#360),#242,.T.);
#2013=ADVANCED_FACE('',(#361),#243,.T.);
#2014=ADVANCED_FACE('',(#362),#244,.T.);
#2015=ADVANCED_FACE('',(#363),#245,.F.);
#2016=ADVANCED_FACE('',(#364),#246,.F.);
#2017=ADVANCED_FACE('',(#365),#247,.F.);
#2018=ADVANCED_FACE('',(#366),#248,.F.);
#2019=ADVANCED_FACE('',(#367),#249,.F.);
#2020=ADVANCED_FACE('',(#368),#250,.F.);
#2021=ADVANCED_FACE('',(#369),#251,.T.);
#2028=CLOSED_SHELL('',(#1965,#1966,#1967,#1968,#1969,#1970,#1971,#1972,
#1973,#1974,#1975,#1976,#1977,#1978,#1979,#1980,#1981,#1982,#1983,#1984,
#1985,#1986,#1987,#1988,#1989,#1990,#1991,#1992,#1993,#1994,#1995,#1996,
#1997,#1998,#1999,#2000,#2001,#2002,#2003,#2004,#2005,#2006,#2007,#2008,
#2009,#2010,#2011,#2012,#2013,#2014,#2015,#2016,#2017,#2018,#2019,#2020,
#2021));
#2234=AXIS2_PLACEMENT_3D('',#3147,#2636,#2637);
#2235=AXIS2_PLACEMENT_3D('',#3148,#2638,#2639);
#2236=AXIS2_PLACEMENT_3D('',#3165,#2641,#2642);
#2237=AXIS2_PLACEMENT_3D('',#3175,#2643,#2644);
#2238=AXIS2_PLACEMENT_3D('',#3205,#2646,#2647);
#2239=AXIS2_PLACEMENT_3D('',#3235,#2649,#2650);
#2240=AXIS2_PLACEMENT_3D('',#3265,#2652,#2653);
#2241=AXIS2_PLACEMENT_3D('',#3295,#2655,#2656);
#2242=AXIS2_PLACEMENT_3D('',#3325,#2658,#2659);
#2243=AXIS2_PLACEMENT_3D('',#3355,#2661,#2662);
#2244=AXIS2_PLACEMENT_3D('',#3385,#2664,#2665);
#2245=AXIS2_PLACEMENT_3D('',#3415,#2667,#2668);
#2246=AXIS2_PLACEMENT_3D('',#3445,#2670,#2671);
#2247=AXIS2_PLACEMENT_3D('',#3475,#2673,#2674);
#2248=AXIS2_PLACEMENT_3D('',#3505,#2676,#2677);
#2249=AXIS2_PLACEMENT_3D('',#3535,#2679,#2680);
#2250=AXIS2_PLACEMENT_3D('',#3561,#2682,#2683);
#2251=AXIS2_PLACEMENT_3D('',#3565,#2685,#2686);
#2252=AXIS2_PLACEMENT_3D('',#3566,#2687,#2688);
#2253=AXIS2_PLACEMENT_3D('',#3568,#2689,#2690);
#2254=AXIS2_PLACEMENT_3D('',#3585,#2691,#2692);
#2255=AXIS2_PLACEMENT_3D('',#3661,#2694,#2695);
#2256=AXIS2_PLACEMENT_3D('',#3737,#2697,#2698);
#2257=AXIS2_PLACEMENT_3D('',#3813,#2700,#2701);
#2258=AXIS2_PLACEMENT_3D('',#3889,#2703,#2704);
#2259=AXIS2_PLACEMENT_3D('',#3965,#2706,#2707);
#2260=AXIS2_PLACEMENT_3D('',#4043,#2709,#2710);
#2261=AXIS2_PLACEMENT_3D('',#4121,#2712,#2713);
#2262=AXIS2_PLACEMENT_3D('',#4197,#2715,#2716);
#2263=AXIS2_PLACEMENT_3D('',#4273,#2718,#2719);
#2264=AXIS2_PLACEMENT_3D('',#4349,#2721,#2722);
#2265=AXIS2_PLACEMENT_3D('',#4425,#2724,#2725);
#2266=AXIS2_PLACEMENT_3D('',#4501,#2727,#2728);
#2267=AXIS2_PLACEMENT_3D('',#4506,#2730,#2731);
#2268=AXIS2_PLACEMENT_3D('',#4557,#2732,#2733);
#2269=AXIS2_PLACEMENT_3D('',#4560,#2735,#2736);
#2270=AXIS2_PLACEMENT_3D('',#4562,#2737,#2738);
#2271=AXIS2_PLACEMENT_3D('',#4575,#2739,#2740);
#2272=AXIS2_PLACEMENT_3D('',#4577,#2741,#2742);
#2273=AXIS2_PLACEMENT_3D('',#4578,#2743,#2744);
#2274=AXIS2_PLACEMENT_3D('',#4579,#2745,#2746);
#2275=AXIS2_PLACEMENT_3D('',#4581,#2747,#2748);
#2276=AXIS2_PLACEMENT_3D('',#4583,#2749,#2750);
#2277=AXIS2_PLACEMENT_3D('',#4584,#2751,#2752);
#2278=AXIS2_PLACEMENT_3D('',#4585,#2753,#2754);
#2279=AXIS2_PLACEMENT_3D('',#4587,#2756,#2757);
#2280=AXIS2_PLACEMENT_3D('',#4593,#2758,#2759);
#2281=AXIS2_PLACEMENT_3D('',#4594,#2760,#2761);
#2282=AXIS2_PLACEMENT_3D('',#7215,#2762,#2763);
#2283=AXIS2_PLACEMENT_3D('',#9785,#2764,#2765);
#2284=AXIS2_PLACEMENT_3D('',#9786,#2766,#2767);
#2285=AXIS2_PLACEMENT_3D('',#9787,#2768,#2769);
#2286=AXIS2_PLACEMENT_3D('',#9800,#2776,#2777);
#2287=AXIS2_PLACEMENT_3D('',#9809,#2782,#2783);
#2288=AXIS2_PLACEMENT_3D('',#9815,#2787,#2788);
#2289=AXIS2_PLACEMENT_3D('',#9821,#2792,#2793);
#2290=AXIS2_PLACEMENT_3D('',#9827,#2797,#2798);
#2291=AXIS2_PLACEMENT_3D('',#9833,#2802,#2803);
#2292=AXIS2_PLACEMENT_3D('',#9836,#2806,#2807);
#2293=AXIS2_PLACEMENT_3D('',#9839,#2810,#2811);
#2294=AXIS2_PLACEMENT_3D('',#9841,#2813,#2814);
#2295=AXIS2_PLACEMENT_3D('',#9843,#2816,#2817);
#2296=AXIS2_PLACEMENT_3D('',#9845,#2819,#2820);
#2297=AXIS2_PLACEMENT_3D('',#9847,#2822,#2823);
#2298=AXIS2_PLACEMENT_3D('',#9848,#2824,#2825);
#2299=AXIS2_PLACEMENT_3D('',#9854,#2829,#2830);
#2300=AXIS2_PLACEMENT_3D('',#9858,#2833,#2834);
#2301=AXIS2_PLACEMENT_3D('',#9862,#2837,#2838);
#2302=AXIS2_PLACEMENT_3D('',#9866,#2841,#2842);
#2303=AXIS2_PLACEMENT_3D('',#9870,#2845,#2846);
#2304=AXIS2_PLACEMENT_3D('',#9872,#2848,#2849);
#2636=DIRECTION('axis',(0.,0.,1.));
#2637=DIRECTION('refdir',(1.,0.,0.));
#2638=DIRECTION('center_axis',(0.,-1.,0.));
#2639=DIRECTION('ref_axis',(-1.,0.,1.28409742660487E-16));
#2640=DIRECTION('',(0.,1.,0.));
#2641=DIRECTION('center_axis',(0.,-1.,0.));
#2642=DIRECTION('ref_axis',(-1.,0.,1.28409742660487E-16));
#2643=DIRECTION('center_axis',(0.,-1.,0.));
#2644=DIRECTION('ref_axis',(-1.,0.,1.28409742660487E-16));
#2645=DIRECTION('',(0.,1.,0.));
#2646=DIRECTION('center_axis',(0.,-1.,0.));
#2647=DIRECTION('ref_axis',(-1.,0.,1.28409742660487E-16));
#2648=DIRECTION('',(0.,1.,0.));
#2649=DIRECTION('center_axis',(0.,-1.,0.));
#2650=DIRECTION('ref_axis',(-1.,0.,1.28409742660487E-16));
#2651=DIRECTION('',(0.,1.,0.));
#2652=DIRECTION('center_axis',(0.,-1.,0.));
#2653=DIRECTION('ref_axis',(-1.,0.,1.28409742660487E-16));
#2654=DIRECTION('',(0.,1.,0.));
#2655=DIRECTION('center_axis',(0.,-1.,0.));
#2656=DIRECTION('ref_axis',(-1.,0.,1.28409742660487E-16));
#2657=DIRECTION('',(0.,1.,0.));
#2658=DIRECTION('center_axis',(0.,-1.,0.));
#2659=DIRECTION('ref_axis',(-1.,0.,1.28409742660487E-16));
#2660=DIRECTION('',(0.,1.,0.));
#2661=DIRECTION('center_axis',(0.,-1.,0.));
#2662=DIRECTION('ref_axis',(-1.,0.,1.28409742660487E-16));
#2663=DIRECTION('',(0.,1.,0.));
#2664=DIRECTION('center_axis',(0.,-1.,0.));
#2665=DIRECTION('ref_axis',(-1.,0.,1.28409742660487E-16));
#2666=DIRECTION('',(0.,1.,0.));
#2667=DIRECTION('center_axis',(0.,-1.,0.));
#2668=DIRECTION('ref_axis',(-1.,0.,1.28409742660487E-16));
#2669=DIRECTION('',(0.,1.,0.));
#2670=DIRECTION('center_axis',(0.,-1.,0.));
#2671=DIRECTION('ref_axis',(-1.,0.,1.28409742660487E-16));
#2672=DIRECTION('',(0.,1.,0.));
#2673=DIRECTION('center_axis',(0.,-1.,0.));
#2674=DIRECTION('ref_axis',(-1.,0.,1.28409742660487E-16));
#2675=DIRECTION('',(0.,1.,0.));
#2676=DIRECTION('center_axis',(0.,-1.,0.));
#2677=DIRECTION('ref_axis',(-1.,0.,1.28409742660487E-16));
#2678=DIRECTION('',(0.,1.,0.));
#2679=DIRECTION('center_axis',(0.,-1.,0.));
#2680=DIRECTION('ref_axis',(0.,0.,-1.));
#2681=DIRECTION('',(0.,1.,0.));
#2682=DIRECTION('center_axis',(0.,1.,0.));
#2683=DIRECTION('ref_axis',(0.,0.,1.));
#2684=DIRECTION('',(0.,1.,0.));
#2685=DIRECTION('center_axis',(0.,-1.,0.));
#2686=DIRECTION('ref_axis',(0.,0.,1.));
#2687=DIRECTION('center_axis',(0.,-1.,0.));
#2688=DIRECTION('ref_axis',(0.,0.,1.));
#2689=DIRECTION('center_axis',(0.,1.,0.));
#2690=DIRECTION('ref_axis',(0.,0.,1.));
#2691=DIRECTION('center_axis',(0.,-1.,0.));
#2692=DIRECTION('ref_axis',(0.,0.,-1.));
#2693=DIRECTION('',(0.,1.,0.));
#2694=DIRECTION('center_axis',(0.,-1.,0.));
#2695=DIRECTION('ref_axis',(0.,0.,-1.));
#2696=DIRECTION('',(0.,1.,0.));
#2697=DIRECTION('center_axis',(0.,-1.,0.));
#2698=DIRECTION('ref_axis',(0.,0.,-1.));
#2699=DIRECTION('',(0.,1.,0.));
#2700=DIRECTION('center_axis',(0.,-1.,0.));
#2701=DIRECTION('ref_axis',(0.,0.,-1.));
#2702=DIRECTION('',(0.,1.,0.));
#2703=DIRECTION('center_axis',(0.,-1.,0.));
#2704=DIRECTION('ref_axis',(0.,0.,-1.));
#2705=DIRECTION('',(0.,1.,0.));
#2706=DIRECTION('center_axis',(0.,-1.,0.));
#2707=DIRECTION('ref_axis',(0.,0.,-1.));
#2708=DIRECTION('',(0.,1.,0.));
#2709=DIRECTION('center_axis',(0.,-1.,0.));
#2710=DIRECTION('ref_axis',(0.,0.,-1.));
#2711=DIRECTION('',(0.,1.,0.));
#2712=DIRECTION('center_axis',(0.,-1.,0.));
#2713=DIRECTION('ref_axis',(0.,0.,-1.));
#2714=DIRECTION('',(0.,1.,0.));
#2715=DIRECTION('center_axis',(0.,-1.,0.));
#2716=DIRECTION('ref_axis',(0.,0.,-1.));
#2717=DIRECTION('',(0.,1.,0.));
#2718=DIRECTION('center_axis',(0.,-1.,0.));
#2719=DIRECTION('ref_axis',(0.,0.,-1.));
#2720=DIRECTION('',(0.,1.,0.));
#2721=DIRECTION('center_axis',(0.,-1.,0.));
#2722=DIRECTION('ref_axis',(0.,0.,-1.));
#2723=DIRECTION('',(0.,1.,0.));
#2724=DIRECTION('center_axis',(0.,-1.,0.));
#2725=DIRECTION('ref_axis',(0.,0.,-1.));
#2726=DIRECTION('',(0.,1.,0.));
#2727=DIRECTION('center_axis',(0.,1.,0.));
#2728=DIRECTION('ref_axis',(0.,0.,1.));
#2729=DIRECTION('',(8.65956056235498E-17,-0.707106781186544,0.707106781186551));
#2730=DIRECTION('center_axis',(0.,1.,0.));
#2731=DIRECTION('ref_axis',(0.,0.,1.));
#2732=DIRECTION('center_axis',(-8.64437306947178E-16,-1.,-1.44797790076548E-15));
#2733=DIRECTION('ref_axis',(0.961856708765554,-4.33382881479145E-16,-0.273553782285489));
#2734=DIRECTION('',(8.65956056235498E-17,-0.707106781186544,0.707106781186551));
#2735=DIRECTION('center_axis',(0.,-1.,0.));
#2736=DIRECTION('ref_axis',(0.,0.,-1.));
#2737=DIRECTION('center_axis',(-8.64437306947178E-16,-1.,-1.44797790076548E-15));
#2738=DIRECTION('ref_axis',(0.961856708765554,-4.33382881479145E-16,-0.273553782285489));
#2739=DIRECTION('center_axis',(0.,1.,0.));
#2740=DIRECTION('ref_axis',(0.,0.,1.));
#2741=DIRECTION('center_axis',(0.,1.,0.));
#2742=DIRECTION('ref_axis',(0.,0.,1.));
#2743=DIRECTION('center_axis',(1.,0.,-1.22464679914735E-16));
#2744=DIRECTION('ref_axis',(-1.22464679914735E-16,0.,-1.));
#2745=DIRECTION('center_axis',(0.,1.,0.));
#2746=DIRECTION('ref_axis',(0.,0.,1.));
#2747=DIRECTION('center_axis',(0.,1.,0.));
#2748=DIRECTION('ref_axis',(0.,0.,1.));
#2749=DIRECTION('center_axis',(-1.,0.,1.22464679914735E-16));
#2750=DIRECTION('ref_axis',(-1.22464679914735E-16,0.,-1.));
#2751=DIRECTION('center_axis',(0.,-1.,0.));
#2752=DIRECTION('ref_axis',(0.,0.,1.));
#2753=DIRECTION('center_axis',(0.,1.,0.));
#2754=DIRECTION('ref_axis',(0.,0.,1.));
#2755=DIRECTION('',(8.65956056235495E-17,-0.707106781186546,0.707106781186549));
#2756=DIRECTION('center_axis',(0.,1.,0.));
#2757=DIRECTION('ref_axis',(0.,0.,1.));
#2758=DIRECTION('center_axis',(0.,1.,0.));
#2759=DIRECTION('ref_axis',(0.,0.,1.));
#2760=DIRECTION('center_axis',(0.,-1.,0.));
#2761=DIRECTION('ref_axis',(0.,0.,-1.));
#2762=DIRECTION('center_axis',(0.,-1.,0.));
#2763=DIRECTION('ref_axis',(-1.,0.,1.28409742660487E-16));
#2764=DIRECTION('center_axis',(0.,1.,0.));
#2765=DIRECTION('ref_axis',(0.,0.,1.));
#2766=DIRECTION('center_axis',(0.,1.,0.));
#2767=DIRECTION('ref_axis',(0.,0.,1.));
#2768=DIRECTION('center_axis',(0.,1.,0.));
#2769=DIRECTION('ref_axis',(0.,0.,1.));
#2770=DIRECTION('',(-0.866025403784438,0.,-0.5));
#2771=DIRECTION('',(0.,0.,-1.));
#2772=DIRECTION('',(0.866025403784439,0.,-0.5));
#2773=DIRECTION('',(0.866025403784438,0.,0.5));
#2774=DIRECTION('',(1.50231459873716E-16,0.,1.));
#2775=DIRECTION('',(-0.866025403784439,0.,0.5));
#2776=DIRECTION('center_axis',(0.5,0.,-0.866025403784439));
#2777=DIRECTION('ref_axis',(-0.866025403784439,0.,-0.5));
#2778=DIRECTION('',(0.,1.,0.));
#2779=DIRECTION('',(-0.866025403784439,0.,-0.5));
#2780=DIRECTION('',(0.,1.,0.));
#2781=DIRECTION('',(-0.866025403784439,0.,-0.5));
#2782=DIRECTION('center_axis',(1.,0.,-1.50231459873716E-16));
#2783=DIRECTION('ref_axis',(-1.50231459873716E-16,0.,-1.));
#2784=DIRECTION('',(0.,1.,0.));
#2785=DIRECTION('',(-1.50231459873716E-16,0.,-1.));
#2786=DIRECTION('',(-1.50231459873716E-16,0.,-1.));
#2787=DIRECTION('center_axis',(0.5,0.,0.866025403784439));
#2788=DIRECTION('ref_axis',(0.866025403784439,0.,-0.5));
#2789=DIRECTION('',(0.,1.,0.));
#2790=DIRECTION('',(0.866025403784439,0.,-0.5));
#2791=DIRECTION('',(0.866025403784439,0.,-0.5));
#2792=DIRECTION('center_axis',(-0.5,0.,0.866025403784439));
#2793=DIRECTION('ref_axis',(0.866025403784439,0.,0.5));
#2794=DIRECTION('',(0.,1.,0.));
#2795=DIRECTION('',(0.866025403784438,0.,0.5));
#2796=DIRECTION('',(0.866025403784438,0.,0.5));
#2797=DIRECTION('center_axis',(-1.,0.,0.));
#2798=DIRECTION('ref_axis',(0.,0.,1.));
#2799=DIRECTION('',(0.,1.,0.));
#2800=DIRECTION('',(0.,0.,1.));
#2801=DIRECTION('',(0.,0.,1.));
#2802=DIRECTION('center_axis',(-0.5,0.,-0.866025403784439));
#2803=DIRECTION('ref_axis',(-0.866025403784439,0.,0.5));
#2804=DIRECTION('',(-0.866025403784439,0.,0.5));
#2805=DIRECTION('',(-0.866025403784439,0.,0.5));
#2806=DIRECTION('center_axis',(-0.70710678118655,0.707106781186545,1.0622968402426E-16));
#2807=DIRECTION('ref_axis',(1.50231459873716E-16,2.12845086949137E-34,1.));
#2808=DIRECTION('',(-0.654653670707975,-0.65465367070798,-0.377964473009225));
#2809=DIRECTION('',(0.654653670707975,0.65465367070798,-0.377964473009227));
#2810=DIRECTION('center_axis',(-0.353553390593275,0.707106781186545,0.612372435695797));
#2811=DIRECTION('ref_axis',(0.866025403784439,1.12179404366126E-17,0.5));
#2812=DIRECTION('',(4.73877874074079E-16,0.65465367070798,-0.755928946018452));
#2813=DIRECTION('center_axis',(-0.353553390593275,0.707106781186544,-0.612372435695797));
#2814=DIRECTION('ref_axis',(-0.866025403784439,-2.22179676214442E-17,0.5));
#2815=DIRECTION('',(2.46349614890202E-15,-0.65465367070798,-0.755928946018452));
#2816=DIRECTION('center_axis',(0.353553390593275,0.707106781186545,0.612372435695797));
#2817=DIRECTION('ref_axis',(0.866025403784439,6.5167186869869E-18,-0.5));
#2818=DIRECTION('',(-0.654653670707975,0.65465367070798,-0.377964473009226));
#2819=DIRECTION('center_axis',(0.353553390593275,0.707106781186546,-0.612372435695796));
#2820=DIRECTION('ref_axis',(-0.866025403784439,3.51850444550808E-18,-0.5));
#2821=DIRECTION('',(0.654653670707975,-0.654653670707979,-0.377964473009227));
#2822=DIRECTION('center_axis',(0.70710678118655,0.707106781186545,0.));
#2823=DIRECTION('ref_axis',(0.,0.,-1.));
#2824=DIRECTION('center_axis',(0.249999999999997,-0.86602540378444,-0.433012701892219));
#2825=DIRECTION('ref_axis',(1.15617626223753E-17,0.447213595499957,-0.894427190999916));
#2826=DIRECTION('',(-3.0099126994645E-15,0.447213595499957,-0.894427190999917));
#2827=DIRECTION('',(-0.866025403784441,0.,-0.499999999999995));
#2828=DIRECTION('',(0.77459666924148,0.447213595499957,-0.447213595499965));
#2829=DIRECTION('center_axis',(0.499999999999998,-0.86602540378444,-5.25810109558002E-15));
#2830=DIRECTION('ref_axis',(0.86602540378444,0.499999999999998,-1.39303110180435E-31));
#2831=DIRECTION('',(-1.05162021911601E-14,0.,-1.));
#2832=DIRECTION('',(0.774596669241488,0.447213595499956,0.447213595499951));
#2833=DIRECTION('center_axis',(0.250000000000003,-0.86602540378444,0.433012701892216));
#2834=DIRECTION('ref_axis',(-1.269494574772E-17,-0.447213595499954,-0.894427190999918));
#2835=DIRECTION('',(0.866025403784434,0.,-0.500000000000007));
#2836=DIRECTION('',(6.32081666887542E-15,0.447213595499956,0.894427190999917));
#2837=DIRECTION('center_axis',(-0.249999999999996,-0.86602540378444,0.433012701892219));
#2838=DIRECTION('ref_axis',(7.449066610202E-18,-0.447213595499957,-0.894427190999916));
#2839=DIRECTION('',(0.866025403784442,0.,0.499999999999995));
#2840=DIRECTION('',(-0.774596669241482,0.447213595499956,0.447213595499962));
#2841=DIRECTION('center_axis',(-0.499999999999998,-0.86602540378444,1.65254605861087E-15));
#2842=DIRECTION('ref_axis',(0.86602540378444,-0.499999999999998,-1.10237170434595E-32));
#2843=DIRECTION('',(3.30509211722174E-15,0.,1.));
#2844=DIRECTION('',(-0.774596669241485,0.447213595499956,-0.447213595499957));
#2845=DIRECTION('center_axis',(-0.249999999999999,-0.86602540378444,-0.433012701892217));
#2846=DIRECTION('ref_axis',(-8.79687280792217E-19,0.447213595499956,-0.894427190999917));
#2847=DIRECTION('',(-0.866025403784438,0.,0.500000000000001));
#2848=DIRECTION('center_axis',(0.,1.,0.));
#2849=DIRECTION('ref_axis',(0.,0.,1.));
#3147=CARTESIAN_POINT('',(0.,0.,0.));
#3148=CARTESIAN_POINT('Origin',(-2.77555756156289E-16,71.6937500009559,
-2.08166817117217E-16));
#3149=CARTESIAN_POINT('',(1.6211138875,8.95625000095593,-2.08166817117217E-16));
#3150=CARTESIAN_POINT('',(1.6211138875,9.13125000095592,-2.08166817117217E-16));
#3151=CARTESIAN_POINT('',(1.6211138875,71.6937500009559,-2.17804440896414E-16));
#3152=CARTESIAN_POINT('',(0.538440894222362,9.51999998211971,1.52908195976357));
#3153=CARTESIAN_POINT('Ctrl Pts',(0.538440894222362,9.51999996467551,1.52908195976357));
#3154=CARTESIAN_POINT('Ctrl Pts',(-0.164839976619388,9.46938696606746,1.77673067379592));
#3155=CARTESIAN_POINT('Ctrl Pts',(-0.810556943749999,9.42291666762259,1.40392580900275));
#3156=CARTESIAN_POINT('Ctrl Pts',(-1.6211138875,9.36458333428926,0.935950539335167));
#3157=CARTESIAN_POINT('Ctrl Pts',(-1.6211138875,9.30625000095593,0.));
#3158=CARTESIAN_POINT('Ctrl Pts',(-1.6211138875,9.24791666762259,-0.935950539335166));
#3159=CARTESIAN_POINT('Ctrl Pts',(-0.81055694375,9.18958333428926,-1.40392580900275));
#3160=CARTESIAN_POINT('Ctrl Pts',(-1.14620883215705E-16,9.13125000095592,
-1.87190107867033));
#3161=CARTESIAN_POINT('Ctrl Pts',(0.81055694375,9.0729166676226,-1.40392580900275));
#3162=CARTESIAN_POINT('Ctrl Pts',(1.6211138875,9.01458333428926,-0.935950539335166));
#3163=CARTESIAN_POINT('Ctrl Pts',(1.6211138875,8.95625000095593,-1.9852919333802E-16));
#3164=CARTESIAN_POINT('',(-1.52006374725761,9.52000000000001,0.563397231550268));
#3165=CARTESIAN_POINT('Origin',(-2.77555756156289E-16,9.52000000000001,
-2.08166817117217E-16));
#3166=CARTESIAN_POINT('Ctrl Pts',(-1.52006374725761,9.52000000000001,0.563397231550268));
#3167=CARTESIAN_POINT('Ctrl Pts',(-1.6211138875,9.49937173003197,0.290760721755766));
#3168=CARTESIAN_POINT('Ctrl Pts',(-1.6211138875,9.48125000095592,0.));
#3169=CARTESIAN_POINT('Ctrl Pts',(-1.6211138875,9.42291666762259,-0.935950539335166));
#3170=CARTESIAN_POINT('Ctrl Pts',(-0.81055694375,9.36458333428925,-1.40392580900275));
#3171=CARTESIAN_POINT('Ctrl Pts',(-1.14620883215705E-16,9.30625000095592,
-1.87190107867033));
#3172=CARTESIAN_POINT('Ctrl Pts',(0.81055694375,9.24791666762259,-1.40392580900275));
#3173=CARTESIAN_POINT('Ctrl Pts',(1.6211138875,9.18958333428925,-0.935950539335166));
#3174=CARTESIAN_POINT('Ctrl Pts',(1.6211138875,9.13125000095592,-1.9852919333802E-16));
#3175=CARTESIAN_POINT('Origin',(-2.77555756156289E-16,71.6937500009559,
-2.08166817117217E-16));
#3176=CARTESIAN_POINT('',(1.6211138875,8.25625000095592,-2.08166817117217E-16));
#3177=CARTESIAN_POINT('',(1.6211138875,8.43125000095592,-2.08166817117217E-16));
#3178=CARTESIAN_POINT('',(1.6211138875,71.6937500009559,-2.17804440896414E-16));
#3179=CARTESIAN_POINT('Ctrl Pts',(1.6211138875,8.95625000095593,-1.9852919333802E-16));
#3180=CARTESIAN_POINT('Ctrl Pts',(1.6211138875,8.89791666762259,0.935950539335165));
#3181=CARTESIAN_POINT('Ctrl Pts',(0.810556943750001,8.83958333428926,1.40392580900275));
#3182=CARTESIAN_POINT('Ctrl Pts',(3.43862649647115E-16,8.78125000095592,
1.87190107867033));
#3183=CARTESIAN_POINT('Ctrl Pts',(-0.810556943749999,8.72291666762259,1.40392580900275));
#3184=CARTESIAN_POINT('Ctrl Pts',(-1.6211138875,8.66458333428927,0.935950539335167));
#3185=CARTESIAN_POINT('Ctrl Pts',(-1.6211138875,8.60625000095593,0.));
#3186=CARTESIAN_POINT('Ctrl Pts',(-1.6211138875,8.5479166676226,-0.935950539335166));
#3187=CARTESIAN_POINT('Ctrl Pts',(-0.81055694375,8.48958333428926,-1.40392580900275));
#3188=CARTESIAN_POINT('Ctrl Pts',(-1.14620883215705E-16,8.43125000095593,
-1.87190107867033));
#3189=CARTESIAN_POINT('Ctrl Pts',(0.81055694375,8.37291666762259,-1.40392580900275));
#3190=CARTESIAN_POINT('Ctrl Pts',(1.6211138875,8.31458333428926,-0.935950539335166));
#3191=CARTESIAN_POINT('Ctrl Pts',(1.6211138875,8.25625000095592,-1.9852919333802E-16));
#3192=CARTESIAN_POINT('Ctrl Pts',(1.6211138875,9.13125000095592,-1.9852919333802E-16));
#3193=CARTESIAN_POINT('Ctrl Pts',(1.6211138875,9.07291666762258,0.935950539335165));
#3194=CARTESIAN_POINT('Ctrl Pts',(0.810556943750001,9.01458333428926,1.40392580900275));
#3195=CARTESIAN_POINT('Ctrl Pts',(3.43862649647115E-16,8.95625000095592,
1.87190107867033));
#3196=CARTESIAN_POINT('Ctrl Pts',(-0.810556943749999,8.89791666762259,1.40392580900275));
#3197=CARTESIAN_POINT('Ctrl Pts',(-1.6211138875,8.83958333428926,0.935950539335167));
#3198=CARTESIAN_POINT('Ctrl Pts',(-1.6211138875,8.78125000095592,0.));
#3199=CARTESIAN_POINT('Ctrl Pts',(-1.6211138875,8.72291666762259,-0.935950539335166));
#3200=CARTESIAN_POINT('Ctrl Pts',(-0.81055694375,8.66458333428925,-1.40392580900275));
#3201=CARTESIAN_POINT('Ctrl Pts',(-1.14620883215705E-16,8.60625000095593,
-1.87190107867033));
#3202=CARTESIAN_POINT('Ctrl Pts',(0.81055694375,8.54791666762259,-1.40392580900275));
#3203=CARTESIAN_POINT('Ctrl Pts',(1.6211138875,8.48958333428926,-0.935950539335166));
#3204=CARTESIAN_POINT('Ctrl Pts',(1.6211138875,8.43125000095592,-1.9852919333802E-16));
#3205=CARTESIAN_POINT('Origin',(-2.77555756156289E-16,71.6937500009559,
-2.08166817117217E-16));
#3206=CARTESIAN_POINT('',(1.6211138875,7.55625000095593,-2.08166817117217E-16));
#3207=CARTESIAN_POINT('',(1.6211138875,7.73125000095592,-2.08166817117217E-16));
#3208=CARTESIAN_POINT('',(1.6211138875,71.6937500009559,-2.17804440896414E-16));
#3209=CARTESIAN_POINT('Ctrl Pts',(1.6211138875,8.25625000095592,-1.9852919333802E-16));
#3210=CARTESIAN_POINT('Ctrl Pts',(1.6211138875,8.1979166676226,0.935950539335165));
#3211=CARTESIAN_POINT('Ctrl Pts',(0.810556943750001,8.13958333428925,1.40392580900275));
#3212=CARTESIAN_POINT('Ctrl Pts',(3.43862649647115E-16,8.08125000095593,
1.87190107867033));
#3213=CARTESIAN_POINT('Ctrl Pts',(-0.810556943749999,8.02291666762259,1.40392580900275));
#3214=CARTESIAN_POINT('Ctrl Pts',(-1.6211138875,7.96458333428926,0.935950539335167));
#3215=CARTESIAN_POINT('Ctrl Pts',(-1.6211138875,7.90625000095593,0.));
#3216=CARTESIAN_POINT('Ctrl Pts',(-1.6211138875,7.84791666762259,-0.935950539335166));
#3217=CARTESIAN_POINT('Ctrl Pts',(-0.81055694375,7.78958333428927,-1.40392580900275));
#3218=CARTESIAN_POINT('Ctrl Pts',(-1.14620883215705E-16,7.73125000095592,
-1.87190107867033));
#3219=CARTESIAN_POINT('Ctrl Pts',(0.81055694375,7.6729166676226,-1.40392580900275));
#3220=CARTESIAN_POINT('Ctrl Pts',(1.6211138875,7.61458333428926,-0.935950539335166));
#3221=CARTESIAN_POINT('Ctrl Pts',(1.6211138875,7.55625000095593,-1.9852919333802E-16));
#3222=CARTESIAN_POINT('Ctrl Pts',(1.6211138875,8.43125000095592,-1.9852919333802E-16));
#3223=CARTESIAN_POINT('Ctrl Pts',(1.6211138875,8.37291666762259,0.935950539335165));
#3224=CARTESIAN_POINT('Ctrl Pts',(0.810556943750001,8.31458333428925,1.40392580900275));
#3225=CARTESIAN_POINT('Ctrl Pts',(3.43862649647115E-16,8.25625000095592,
1.87190107867033));
#3226=CARTESIAN_POINT('Ctrl Pts',(-0.810556943749999,8.19791666762258,1.40392580900275));
#3227=CARTESIAN_POINT('Ctrl Pts',(-1.6211138875,8.13958333428925,0.935950539335167));
#3228=CARTESIAN_POINT('Ctrl Pts',(-1.6211138875,8.08125000095593,0.));
#3229=CARTESIAN_POINT('Ctrl Pts',(-1.6211138875,8.02291666762259,-0.935950539335166));
#3230=CARTESIAN_POINT('Ctrl Pts',(-0.81055694375,7.96458333428926,-1.40392580900275));
#3231=CARTESIAN_POINT('Ctrl Pts',(-1.14620883215705E-16,7.90625000095592,
-1.87190107867033));
#3232=CARTESIAN_POINT('Ctrl Pts',(0.81055694375,7.84791666762259,-1.40392580900275));
#3233=CARTESIAN_POINT('Ctrl Pts',(1.6211138875,7.78958333428925,-0.935950539335166));
#3234=CARTESIAN_POINT('Ctrl Pts',(1.6211138875,7.73125000095592,-1.9852919333802E-16));
#3235=CARTESIAN_POINT('Origin',(-2.77555756156289E-16,71.6937500009559,
-2.08166817117217E-16));
#3236=CARTESIAN_POINT('',(1.6211138875,6.85625000095592,-2.08166817117217E-16));
#3237=CARTESIAN_POINT('',(1.6211138875,7.03125000095592,-2.08166817117217E-16));
#3238=CARTESIAN_POINT('',(1.6211138875,71.6937500009559,-2.17804440896414E-16));
#3239=CARTESIAN_POINT('Ctrl Pts',(1.6211138875,7.55625000095593,-1.9852919333802E-16));
#3240=CARTESIAN_POINT('Ctrl Pts',(1.6211138875,7.49791666762259,0.935950539335165));
#3241=CARTESIAN_POINT('Ctrl Pts',(0.810556943750001,7.43958333428926,1.40392580900275));
#3242=CARTESIAN_POINT('Ctrl Pts',(3.43862649647115E-16,7.38125000095592,
1.87190107867033));
#3243=CARTESIAN_POINT('Ctrl Pts',(-0.810556943749999,7.3229166676226,1.40392580900275));
#3244=CARTESIAN_POINT('Ctrl Pts',(-1.6211138875,7.26458333428925,0.935950539335167));
#3245=CARTESIAN_POINT('Ctrl Pts',(-1.6211138875,7.20625000095593,0.));
#3246=CARTESIAN_POINT('Ctrl Pts',(-1.6211138875,7.1479166676226,-0.935950539335166));
#3247=CARTESIAN_POINT('Ctrl Pts',(-0.81055694375,7.08958333428926,-1.40392580900275));
#3248=CARTESIAN_POINT('Ctrl Pts',(-1.14620883215705E-16,7.03125000095593,
-1.87190107867033));
#3249=CARTESIAN_POINT('Ctrl Pts',(0.81055694375,6.97291666762259,-1.40392580900275));
#3250=CARTESIAN_POINT('Ctrl Pts',(1.6211138875,6.91458333428927,-0.935950539335166));
#3251=CARTESIAN_POINT('Ctrl Pts',(1.6211138875,6.85625000095592,-1.9852919333802E-16));
#3252=CARTESIAN_POINT('Ctrl Pts',(1.6211138875,7.73125000095592,-1.9852919333802E-16));
#3253=CARTESIAN_POINT('Ctrl Pts',(1.6211138875,7.67291666762258,0.935950539335165));
#3254=CARTESIAN_POINT('Ctrl Pts',(0.810556943750001,7.61458333428926,1.40392580900275));
#3255=CARTESIAN_POINT('Ctrl Pts',(3.43862649647115E-16,7.55625000095592,
1.87190107867033));
#3256=CARTESIAN_POINT('Ctrl Pts',(-0.810556943749999,7.49791666762259,1.40392580900275));
#3257=CARTESIAN_POINT('Ctrl Pts',(-1.6211138875,7.43958333428925,0.935950539335167));
#3258=CARTESIAN_POINT('Ctrl Pts',(-1.6211138875,7.38125000095592,0.));
#3259=CARTESIAN_POINT('Ctrl Pts',(-1.6211138875,7.3229166676226,-0.935950539335166));
#3260=CARTESIAN_POINT('Ctrl Pts',(-0.81055694375,7.26458333428925,-1.40392580900275));
#3261=CARTESIAN_POINT('Ctrl Pts',(-1.14620883215705E-16,7.20625000095593,
-1.87190107867033));
#3262=CARTESIAN_POINT('Ctrl Pts',(0.81055694375,7.14791666762259,-1.40392580900275));
#3263=CARTESIAN_POINT('Ctrl Pts',(1.6211138875,7.08958333428926,-0.935950539335166));
#3264=CARTESIAN_POINT('Ctrl Pts',(1.6211138875,7.03125000095592,-1.9852919333802E-16));
#3265=CARTESIAN_POINT('Origin',(-2.77555756156289E-16,71.6937500009559,
-2.08166817117217E-16));
#3266=CARTESIAN_POINT('',(1.6211138875,6.15625000095593,-2.08166817117217E-16));
#3267=CARTESIAN_POINT('',(1.6211138875,6.33125000095593,-2.08166817117217E-16));
#3268=CARTESIAN_POINT('',(1.6211138875,71.6937500009559,-2.17804440896414E-16));
#3269=CARTESIAN_POINT('Ctrl Pts',(1.6211138875,6.85625000095592,-1.9852919333802E-16));
#3270=CARTESIAN_POINT('Ctrl Pts',(1.6211138875,6.7979166676226,0.935950539335165));
#3271=CARTESIAN_POINT('Ctrl Pts',(0.810556943750001,6.73958333428926,1.40392580900275));
#3272=CARTESIAN_POINT('Ctrl Pts',(3.43862649647115E-16,6.68125000095593,
1.87190107867033));
#3273=CARTESIAN_POINT('Ctrl Pts',(-0.810556943749999,6.62291666762259,1.40392580900275));
#3274=CARTESIAN_POINT('Ctrl Pts',(-1.6211138875,6.56458333428926,0.935950539335167));
#3275=CARTESIAN_POINT('Ctrl Pts',(-1.6211138875,6.50625000095592,0.));
#3276=CARTESIAN_POINT('Ctrl Pts',(-1.6211138875,6.44791666762259,-0.935950539335166));
#3277=CARTESIAN_POINT('Ctrl Pts',(-0.81055694375,6.38958333428925,-1.40392580900275));
#3278=CARTESIAN_POINT('Ctrl Pts',(-1.14620883215705E-16,6.33125000095593,
-1.87190107867033));
#3279=CARTESIAN_POINT('Ctrl Pts',(0.81055694375,6.2729166676226,-1.40392580900275));
#3280=CARTESIAN_POINT('Ctrl Pts',(1.6211138875,6.21458333428926,-0.935950539335166));
#3281=CARTESIAN_POINT('Ctrl Pts',(1.6211138875,6.15625000095593,-1.9852919333802E-16));
#3282=CARTESIAN_POINT('Ctrl Pts',(1.6211138875,7.03125000095592,-1.9852919333802E-16));
#3283=CARTESIAN_POINT('Ctrl Pts',(1.6211138875,6.97291666762259,0.935950539335165));
#3284=CARTESIAN_POINT('Ctrl Pts',(0.810556943750001,6.91458333428925,1.40392580900275));
#3285=CARTESIAN_POINT('Ctrl Pts',(3.43862649647115E-16,6.85625000095592,
1.87190107867033));
#3286=CARTESIAN_POINT('Ctrl Pts',(-0.810556943749999,6.79791666762258,1.40392580900275));
#3287=CARTESIAN_POINT('Ctrl Pts',(-1.6211138875,6.73958333428926,0.935950539335167));
#3288=CARTESIAN_POINT('Ctrl Pts',(-1.6211138875,6.68125000095592,0.));
#3289=CARTESIAN_POINT('Ctrl Pts',(-1.6211138875,6.62291666762259,-0.935950539335166));
#3290=CARTESIAN_POINT('Ctrl Pts',(-0.81055694375,6.56458333428925,-1.40392580900275));
#3291=CARTESIAN_POINT('Ctrl Pts',(-1.14620883215705E-16,6.50625000095592,
-1.87190107867033));
#3292=CARTESIAN_POINT('Ctrl Pts',(0.81055694375,6.44791666762259,-1.40392580900275));
#3293=CARTESIAN_POINT('Ctrl Pts',(1.6211138875,6.38958333428925,-0.935950539335166));
#3294=CARTESIAN_POINT('Ctrl Pts',(1.6211138875,6.33125000095593,-1.9852919333802E-16));
#3295=CARTESIAN_POINT('Origin',(-2.77555756156289E-16,71.6937500009559,
-2.08166817117217E-16));
#3296=CARTESIAN_POINT('',(1.6211138875,5.45625000095593,-2.08166817117217E-16));
#3297=CARTESIAN_POINT('',(1.6211138875,5.63125000095592,-2.08166817117217E-16));
#3298=CARTESIAN_POINT('',(1.6211138875,71.6937500009559,-2.17804440896414E-16));
#3299=CARTESIAN_POINT('Ctrl Pts',(1.6211138875,6.15625000095593,-1.9852919333802E-16));
#3300=CARTESIAN_POINT('Ctrl Pts',(1.6211138875,6.09791666762259,0.935950539335165));
#3301=CARTESIAN_POINT('Ctrl Pts',(0.810556943750001,6.03958333428927,1.40392580900275));
#3302=CARTESIAN_POINT('Ctrl Pts',(3.43862649647115E-16,5.98125000095592,
1.87190107867033));
#3303=CARTESIAN_POINT('Ctrl Pts',(-0.810556943749999,5.9229166676226,1.40392580900275));
#3304=CARTESIAN_POINT('Ctrl Pts',(-1.6211138875,5.86458333428926,0.935950539335167));
#3305=CARTESIAN_POINT('Ctrl Pts',(-1.6211138875,5.80625000095593,0.));
#3306=CARTESIAN_POINT('Ctrl Pts',(-1.6211138875,5.74791666762259,-0.935950539335166));
#3307=CARTESIAN_POINT('Ctrl Pts',(-0.81055694375,5.68958333428926,-1.40392580900275));
#3308=CARTESIAN_POINT('Ctrl Pts',(-1.14620883215705E-16,5.63125000095592,
-1.87190107867033));
#3309=CARTESIAN_POINT('Ctrl Pts',(0.81055694375,5.57291666762259,-1.40392580900275));
#3310=CARTESIAN_POINT('Ctrl Pts',(1.6211138875,5.51458333428927,-0.935950539335166));
#3311=CARTESIAN_POINT('Ctrl Pts',(1.6211138875,5.45625000095593,-1.9852919333802E-16));
#3312=CARTESIAN_POINT('Ctrl Pts',(1.6211138875,6.33125000095593,-1.9852919333802E-16));
#3313=CARTESIAN_POINT('Ctrl Pts',(1.6211138875,6.27291666762259,0.935950539335165));
#3314=CARTESIAN_POINT('Ctrl Pts',(0.810556943750001,6.21458333428926,1.40392580900275));
#3315=CARTESIAN_POINT('Ctrl Pts',(3.43862649647115E-16,6.15625000095592,
1.87190107867033));
#3316=CARTESIAN_POINT('Ctrl Pts',(-0.810556943749999,6.09791666762259,1.40392580900275));
#3317=CARTESIAN_POINT('Ctrl Pts',(-1.6211138875,6.03958333428925,0.935950539335167));
#3318=CARTESIAN_POINT('Ctrl Pts',(-1.6211138875,5.98125000095592,0.));
#3319=CARTESIAN_POINT('Ctrl Pts',(-1.6211138875,5.92291666762258,-0.935950539335166));
#3320=CARTESIAN_POINT('Ctrl Pts',(-0.81055694375,5.86458333428926,-1.40392580900275));
#3321=CARTESIAN_POINT('Ctrl Pts',(-1.14620883215705E-16,5.80625000095591,
-1.87190107867033));
#3322=CARTESIAN_POINT('Ctrl Pts',(0.81055694375,5.74791666762259,-1.40392580900275));
#3323=CARTESIAN_POINT('Ctrl Pts',(1.6211138875,5.68958333428926,-0.935950539335166));
#3324=CARTESIAN_POINT('Ctrl Pts',(1.6211138875,5.63125000095592,-1.9852919333802E-16));
#3325=CARTESIAN_POINT('Origin',(-2.77555756156289E-16,71.6937500009559,
-2.08166817117217E-16));
#3326=CARTESIAN_POINT('',(1.6211138875,4.75625000095593,-2.08166817117217E-16));
#3327=CARTESIAN_POINT('',(1.6211138875,4.93125000095593,-2.08166817117217E-16));
#3328=CARTESIAN_POINT('',(1.6211138875,71.6937500009559,-2.17804440896414E-16));
#3329=CARTESIAN_POINT('Ctrl Pts',(1.6211138875,5.45625000095593,-1.9852919333802E-16));
#3330=CARTESIAN_POINT('Ctrl Pts',(1.6211138875,5.3979166676226,0.935950539335165));
#3331=CARTESIAN_POINT('Ctrl Pts',(0.810556943750001,5.33958333428926,1.40392580900275));
#3332=CARTESIAN_POINT('Ctrl Pts',(3.43862649647115E-16,5.28125000095593,
1.87190107867033));
#3333=CARTESIAN_POINT('Ctrl Pts',(-0.810556943749999,5.22291666762259,1.40392580900275));
#3334=CARTESIAN_POINT('Ctrl Pts',(-1.6211138875,5.16458333428926,0.935950539335167));
#3335=CARTESIAN_POINT('Ctrl Pts',(-1.6211138875,5.10625000095592,0.));
#3336=CARTESIAN_POINT('Ctrl Pts',(-1.6211138875,5.0479166676226,-0.935950539335166));
#3337=CARTESIAN_POINT('Ctrl Pts',(-0.81055694375,4.98958333428925,-1.40392580900275));
#3338=CARTESIAN_POINT('Ctrl Pts',(-1.14620883215705E-16,4.93125000095593,
-1.87190107867033));
#3339=CARTESIAN_POINT('Ctrl Pts',(0.81055694375,4.87291666762259,-1.40392580900275));
#3340=CARTESIAN_POINT('Ctrl Pts',(1.6211138875,4.81458333428926,-0.935950539335166));
#3341=CARTESIAN_POINT('Ctrl Pts',(1.6211138875,4.75625000095593,-1.9852919333802E-16));
#3342=CARTESIAN_POINT('Ctrl Pts',(1.6211138875,5.63125000095592,-1.9852919333802E-16));
#3343=CARTESIAN_POINT('Ctrl Pts',(1.6211138875,5.57291666762259,0.935950539335165));
#3344=CARTESIAN_POINT('Ctrl Pts',(0.810556943750001,5.51458333428925,1.40392580900275));
#3345=CARTESIAN_POINT('Ctrl Pts',(3.43862649647115E-16,5.45625000095593,
1.87190107867033));
#3346=CARTESIAN_POINT('Ctrl Pts',(-0.810556943749999,5.39791666762259,1.40392580900275));
#3347=CARTESIAN_POINT('Ctrl Pts',(-1.6211138875,5.33958333428926,0.935950539335167));
#3348=CARTESIAN_POINT('Ctrl Pts',(-1.6211138875,5.28125000095592,0.));
#3349=CARTESIAN_POINT('Ctrl Pts',(-1.6211138875,5.22291666762259,-0.935950539335166));
#3350=CARTESIAN_POINT('Ctrl Pts',(-0.81055694375,5.16458333428925,-1.40392580900275));
#3351=CARTESIAN_POINT('Ctrl Pts',(-1.14620883215705E-16,5.10625000095592,
-1.87190107867033));
#3352=CARTESIAN_POINT('Ctrl Pts',(0.81055694375,5.04791666762258,-1.40392580900275));
#3353=CARTESIAN_POINT('Ctrl Pts',(1.6211138875,4.98958333428925,-0.935950539335166));
#3354=CARTESIAN_POINT('Ctrl Pts',(1.6211138875,4.93125000095593,-1.9852919333802E-16));
#3355=CARTESIAN_POINT('Origin',(-2.77555756156289E-16,71.6937500009559,
-2.08166817117217E-16));
#3356=CARTESIAN_POINT('',(1.6211138875,4.05625000095593,-2.08166817117217E-16));
#3357=CARTESIAN_POINT('',(1.6211138875,4.23125000095592,-2.08166817117217E-16));
#3358=CARTESIAN_POINT('',(1.6211138875,71.6937500009559,-2.17804440896414E-16));
#3359=CARTESIAN_POINT('Ctrl Pts',(1.6211138875,4.75625000095593,-1.9852919333802E-16));
#3360=CARTESIAN_POINT('Ctrl Pts',(1.6211138875,4.69791666762259,0.935950539335165));
#3361=CARTESIAN_POINT('Ctrl Pts',(0.810556943750001,4.63958333428927,1.40392580900275));
#3362=CARTESIAN_POINT('Ctrl Pts',(3.43862649647115E-16,4.58125000095593,
1.87190107867033));
#3363=CARTESIAN_POINT('Ctrl Pts',(-0.810556943749999,4.5229166676226,1.40392580900275));
#3364=CARTESIAN_POINT('Ctrl Pts',(-1.6211138875,4.46458333428926,0.935950539335167));
#3365=CARTESIAN_POINT('Ctrl Pts',(-1.6211138875,4.40625000095593,0.));
#3366=CARTESIAN_POINT('Ctrl Pts',(-1.6211138875,4.34791666762259,-0.935950539335166));
#3367=CARTESIAN_POINT('Ctrl Pts',(-0.81055694375,4.28958333428926,-1.40392580900275));
#3368=CARTESIAN_POINT('Ctrl Pts',(-1.14620883215705E-16,4.23125000095592,
-1.87190107867033));
#3369=CARTESIAN_POINT('Ctrl Pts',(0.81055694375,4.17291666762259,-1.40392580900275));
#3370=CARTESIAN_POINT('Ctrl Pts',(1.6211138875,4.11458333428925,-0.935950539335166));
#3371=CARTESIAN_POINT('Ctrl Pts',(1.6211138875,4.05625000095593,-1.9852919333802E-16));
#3372=CARTESIAN_POINT('Ctrl Pts',(1.6211138875,4.93125000095593,-1.9852919333802E-16));
#3373=CARTESIAN_POINT('Ctrl Pts',(1.6211138875,4.87291666762259,0.935950539335165));
#3374=CARTESIAN_POINT('Ctrl Pts',(0.810556943750001,4.81458333428926,1.40392580900275));
#3375=CARTESIAN_POINT('Ctrl Pts',(3.43862649647115E-16,4.75625000095592,
1.87190107867033));
#3376=CARTESIAN_POINT('Ctrl Pts',(-0.810556943749999,4.69791666762259,1.40392580900275));
#3377=CARTESIAN_POINT('Ctrl Pts',(-1.6211138875,4.63958333428925,0.935950539335167));
#3378=CARTESIAN_POINT('Ctrl Pts',(-1.6211138875,4.58125000095593,0.));
#3379=CARTESIAN_POINT('Ctrl Pts',(-1.6211138875,4.52291666762258,-0.935950539335166));
#3380=CARTESIAN_POINT('Ctrl Pts',(-0.81055694375,4.46458333428926,-1.40392580900275));
#3381=CARTESIAN_POINT('Ctrl Pts',(-1.14620883215705E-16,4.40625000095592,
-1.87190107867033));
#3382=CARTESIAN_POINT('Ctrl Pts',(0.81055694375,4.34791666762259,-1.40392580900275));
#3383=CARTESIAN_POINT('Ctrl Pts',(1.6211138875,4.28958333428925,-0.935950539335166));
#3384=CARTESIAN_POINT('Ctrl Pts',(1.6211138875,4.23125000095592,-1.9852919333802E-16));
#3385=CARTESIAN_POINT('Origin',(-2.77555756156289E-16,71.6937500009559,
-2.08166817117217E-16));
#3386=CARTESIAN_POINT('',(1.6211138875,3.35625000095592,-2.08166817117217E-16));
#3387=CARTESIAN_POINT('',(1.6211138875,3.53125000095592,-2.08166817117217E-16));
#3388=CARTESIAN_POINT('',(1.6211138875,71.6937500009559,-2.17804440896414E-16));
#3389=CARTESIAN_POINT('Ctrl Pts',(1.6211138875,4.05625000095593,-1.9852919333802E-16));
#3390=CARTESIAN_POINT('Ctrl Pts',(1.6211138875,3.9979166676226,0.935950539335165));
#3391=CARTESIAN_POINT('Ctrl Pts',(0.810556943750001,3.93958333428926,1.40392580900275));
#3392=CARTESIAN_POINT('Ctrl Pts',(3.43862649647115E-16,3.88125000095593,
1.87190107867033));
#3393=CARTESIAN_POINT('Ctrl Pts',(-0.810556943749999,3.82291666762259,1.40392580900275));
#3394=CARTESIAN_POINT('Ctrl Pts',(-1.6211138875,3.76458333428926,0.935950539335167));
#3395=CARTESIAN_POINT('Ctrl Pts',(-1.6211138875,3.70625000095592,0.));
#3396=CARTESIAN_POINT('Ctrl Pts',(-1.6211138875,3.6479166676226,-0.935950539335166));
#3397=CARTESIAN_POINT('Ctrl Pts',(-0.81055694375,3.58958333428926,-1.40392580900275));
#3398=CARTESIAN_POINT('Ctrl Pts',(-1.14620883215705E-16,3.53125000095593,
-1.87190107867033));
#3399=CARTESIAN_POINT('Ctrl Pts',(0.81055694375,3.47291666762259,-1.40392580900275));
#3400=CARTESIAN_POINT('Ctrl Pts',(1.6211138875,3.41458333428926,-0.935950539335166));
#3401=CARTESIAN_POINT('Ctrl Pts',(1.6211138875,3.35625000095592,-1.9852919333802E-16));
#3402=CARTESIAN_POINT('Ctrl Pts',(1.6211138875,4.23125000095592,-1.9852919333802E-16));
#3403=CARTESIAN_POINT('Ctrl Pts',(1.6211138875,4.17291666762259,0.935950539335165));
#3404=CARTESIAN_POINT('Ctrl Pts',(0.810556943750001,4.11458333428925,1.40392580900275));
#3405=CARTESIAN_POINT('Ctrl Pts',(3.43862649647115E-16,4.05625000095593,
1.87190107867033));
#3406=CARTESIAN_POINT('Ctrl Pts',(-0.810556943749999,3.99791666762259,1.40392580900275));
#3407=CARTESIAN_POINT('Ctrl Pts',(-1.6211138875,3.93958333428926,0.935950539335167));
#3408=CARTESIAN_POINT('Ctrl Pts',(-1.6211138875,3.88125000095592,0.));
#3409=CARTESIAN_POINT('Ctrl Pts',(-1.6211138875,3.82291666762259,-0.935950539335166));
#3410=CARTESIAN_POINT('Ctrl Pts',(-0.81055694375,3.76458333428925,-1.40392580900275));
#3411=CARTESIAN_POINT('Ctrl Pts',(-1.14620883215705E-16,3.70625000095592,
-1.87190107867033));
#3412=CARTESIAN_POINT('Ctrl Pts',(0.81055694375,3.64791666762258,-1.40392580900275));
#3413=CARTESIAN_POINT('Ctrl Pts',(1.6211138875,3.58958333428926,-0.935950539335166));
#3414=CARTESIAN_POINT('Ctrl Pts',(1.6211138875,3.53125000095592,-1.9852919333802E-16));
#3415=CARTESIAN_POINT('Origin',(-2.77555756156289E-16,71.6937500009559,
-2.08166817117217E-16));
#3416=CARTESIAN_POINT('',(1.6211138875,2.65625000095593,-2.08166817117217E-16));
#3417=CARTESIAN_POINT('',(1.6211138875,2.83125000095592,-2.08166817117217E-16));
#3418=CARTESIAN_POINT('',(1.6211138875,71.6937500009559,-2.17804440896414E-16));
#3419=CARTESIAN_POINT('Ctrl Pts',(1.6211138875,3.35625000095592,-1.9852919333802E-16));
#3420=CARTESIAN_POINT('Ctrl Pts',(1.6211138875,3.29791666762259,0.935950539335165));
#3421=CARTESIAN_POINT('Ctrl Pts',(0.810556943750001,3.23958333428925,1.40392580900275));
#3422=CARTESIAN_POINT('Ctrl Pts',(3.43862649647115E-16,3.18125000095593,
1.87190107867033));
#3423=CARTESIAN_POINT('Ctrl Pts',(-0.810556943749999,3.1229166676226,1.40392580900275));
#3424=CARTESIAN_POINT('Ctrl Pts',(-1.6211138875,3.06458333428926,0.935950539335167));
#3425=CARTESIAN_POINT('Ctrl Pts',(-1.6211138875,3.00625000095593,0.));
#3426=CARTESIAN_POINT('Ctrl Pts',(-1.6211138875,2.94791666762259,-0.935950539335166));
#3427=CARTESIAN_POINT('Ctrl Pts',(-0.81055694375,2.88958333428926,-1.40392580900275));
#3428=CARTESIAN_POINT('Ctrl Pts',(-1.14620883215705E-16,2.83125000095592,
-1.87190107867033));
#3429=CARTESIAN_POINT('Ctrl Pts',(0.81055694375,2.7729166676226,-1.40392580900275));
#3430=CARTESIAN_POINT('Ctrl Pts',(1.6211138875,2.71458333428926,-0.935950539335166));
#3431=CARTESIAN_POINT('Ctrl Pts',(1.6211138875,2.65625000095593,-1.9852919333802E-16));
#3432=CARTESIAN_POINT('Ctrl Pts',(1.6211138875,3.53125000095592,-1.9852919333802E-16));
#3433=CARTESIAN_POINT('Ctrl Pts',(1.6211138875,3.47291666762259,0.935950539335165));
#3434=CARTESIAN_POINT('Ctrl Pts',(0.810556943750001,3.41458333428925,1.40392580900275));
#3435=CARTESIAN_POINT('Ctrl Pts',(3.43862649647115E-16,3.35625000095592,
1.87190107867033));
#3436=CARTESIAN_POINT('Ctrl Pts',(-0.810556943749999,3.29791666762259,1.40392580900275));
#3437=CARTESIAN_POINT('Ctrl Pts',(-1.6211138875,3.23958333428925,0.935950539335167));
#3438=CARTESIAN_POINT('Ctrl Pts',(-1.6211138875,3.18125000095593,0.));
#3439=CARTESIAN_POINT('Ctrl Pts',(-1.6211138875,3.12291666762259,-0.935950539335166));
#3440=CARTESIAN_POINT('Ctrl Pts',(-0.81055694375,3.06458333428926,-1.40392580900275));
#3441=CARTESIAN_POINT('Ctrl Pts',(-1.14620883215705E-16,3.00625000095592,
-1.87190107867033));
#3442=CARTESIAN_POINT('Ctrl Pts',(0.81055694375,2.94791666762259,-1.40392580900275));
#3443=CARTESIAN_POINT('Ctrl Pts',(1.6211138875,2.88958333428925,-0.935950539335166));
#3444=CARTESIAN_POINT('Ctrl Pts',(1.6211138875,2.83125000095592,-1.9852919333802E-16));
#3445=CARTESIAN_POINT('Origin',(-2.77555756156289E-16,71.6937500009559,
-2.08166817117217E-16));
#3446=CARTESIAN_POINT('',(1.6211138875,1.95625000095592,-2.08166817117217E-16));
#3447=CARTESIAN_POINT('',(1.6211138875,2.13125000095592,-2.08166817117217E-16));
#3448=CARTESIAN_POINT('',(1.6211138875,71.6937500009559,-2.17804440896414E-16));
#3449=CARTESIAN_POINT('Ctrl Pts',(1.6211138875,2.65625000095593,-1.9852919333802E-16));
#3450=CARTESIAN_POINT('Ctrl Pts',(1.6211138875,2.59791666762259,0.935950539335165));
#3451=CARTESIAN_POINT('Ctrl Pts',(0.810556943750001,2.53958333428926,1.40392580900275));
#3452=CARTESIAN_POINT('Ctrl Pts',(3.43862649647115E-16,2.48125000095592,
1.87190107867033));
#3453=CARTESIAN_POINT('Ctrl Pts',(-0.810556943749999,2.42291666762259,1.40392580900275));
#3454=CARTESIAN_POINT('Ctrl Pts',(-1.6211138875,2.36458333428927,0.935950539335167));
#3455=CARTESIAN_POINT('Ctrl Pts',(-1.6211138875,2.30625000095593,0.));
#3456=CARTESIAN_POINT('Ctrl Pts',(-1.6211138875,2.2479166676226,-0.935950539335166));
#3457=CARTESIAN_POINT('Ctrl Pts',(-0.81055694375,2.18958333428926,-1.40392580900275));
#3458=CARTESIAN_POINT('Ctrl Pts',(-1.14620883215705E-16,2.13125000095593,
-1.87190107867033));
#3459=CARTESIAN_POINT('Ctrl Pts',(0.81055694375,2.07291666762259,-1.40392580900275));
#3460=CARTESIAN_POINT('Ctrl Pts',(1.6211138875,2.01458333428926,-0.935950539335166));
#3461=CARTESIAN_POINT('Ctrl Pts',(1.6211138875,1.95625000095592,-1.9852919333802E-16));
#3462=CARTESIAN_POINT('Ctrl Pts',(1.6211138875,2.83125000095592,-1.9852919333802E-16));
#3463=CARTESIAN_POINT('Ctrl Pts',(1.6211138875,2.77291666762258,0.935950539335165));
#3464=CARTESIAN_POINT('Ctrl Pts',(0.810556943750001,2.71458333428926,1.40392580900275));
#3465=CARTESIAN_POINT('Ctrl Pts',(3.43862649647115E-16,2.65625000095591,
1.87190107867033));
#3466=CARTESIAN_POINT('Ctrl Pts',(-0.810556943749999,2.59791666762259,1.40392580900275));
#3467=CARTESIAN_POINT('Ctrl Pts',(-1.6211138875,2.53958333428926,0.935950539335167));
#3468=CARTESIAN_POINT('Ctrl Pts',(-1.6211138875,2.48125000095592,0.));
#3469=CARTESIAN_POINT('Ctrl Pts',(-1.6211138875,2.42291666762259,-0.935950539335166));
#3470=CARTESIAN_POINT('Ctrl Pts',(-0.81055694375,2.36458333428925,-1.40392580900275));
#3471=CARTESIAN_POINT('Ctrl Pts',(-1.14620883215705E-16,2.30625000095593,
-1.87190107867033));
#3472=CARTESIAN_POINT('Ctrl Pts',(0.81055694375,2.24791666762258,-1.40392580900275));
#3473=CARTESIAN_POINT('Ctrl Pts',(1.6211138875,2.18958333428926,-0.935950539335166));
#3474=CARTESIAN_POINT('Ctrl Pts',(1.6211138875,2.13125000095592,-1.9852919333802E-16));
#3475=CARTESIAN_POINT('Origin',(-2.77555756156289E-16,71.6937500009559,
-2.08166817117217E-16));
#3476=CARTESIAN_POINT('',(1.6211138875,1.25625000095593,-2.08166817117217E-16));
#3477=CARTESIAN_POINT('',(1.6211138875,1.43125000095592,-2.08166817117217E-16));
#3478=CARTESIAN_POINT('',(1.6211138875,71.6937500009559,-2.17804440896414E-16));
#3479=CARTESIAN_POINT('Ctrl Pts',(1.6211138875,1.95625000095592,-1.9852919333802E-16));
#3480=CARTESIAN_POINT('Ctrl Pts',(1.6211138875,1.8979166676226,0.935950539335165));
#3481=CARTESIAN_POINT('Ctrl Pts',(0.810556943750001,1.83958333428925,1.40392580900275));
#3482=CARTESIAN_POINT('Ctrl Pts',(3.43862649647115E-16,1.78125000095593,
1.87190107867033));
#3483=CARTESIAN_POINT('Ctrl Pts',(-0.810556943749999,1.72291666762259,1.40392580900275));
#3484=CARTESIAN_POINT('Ctrl Pts',(-1.6211138875,1.66458333428926,0.935950539335167));
#3485=CARTESIAN_POINT('Ctrl Pts',(-1.6211138875,1.60625000095593,0.));
#3486=CARTESIAN_POINT('Ctrl Pts',(-1.6211138875,1.54791666762259,-0.935950539335166));
#3487=CARTESIAN_POINT('Ctrl Pts',(-0.81055694375,1.48958333428927,-1.40392580900275));
#3488=CARTESIAN_POINT('Ctrl Pts',(-1.14620883215705E-16,1.43125000095592,
-1.87190107867033));
#3489=CARTESIAN_POINT('Ctrl Pts',(0.81055694375,1.3729166676226,-1.40392580900275));
#3490=CARTESIAN_POINT('Ctrl Pts',(1.6211138875,1.31458333428926,-0.935950539335166));
#3491=CARTESIAN_POINT('Ctrl Pts',(1.6211138875,1.25625000095593,-1.9852919333802E-16));
#3492=CARTESIAN_POINT('Ctrl Pts',(1.6211138875,2.13125000095592,-1.9852919333802E-16));
#3493=CARTESIAN_POINT('Ctrl Pts',(1.6211138875,2.07291666762259,0.935950539335165));
#3494=CARTESIAN_POINT('Ctrl Pts',(0.810556943750001,2.01458333428925,1.40392580900275));
#3495=CARTESIAN_POINT('Ctrl Pts',(3.43862649647115E-16,1.95625000095592,
1.87190107867033));
#3496=CARTESIAN_POINT('Ctrl Pts',(-0.810556943749999,1.89791666762258,1.40392580900275));
#3497=CARTESIAN_POINT('Ctrl Pts',(-1.6211138875,1.83958333428925,0.935950539335167));
#3498=CARTESIAN_POINT('Ctrl Pts',(-1.6211138875,1.78125000095593,0.));
#3499=CARTESIAN_POINT('Ctrl Pts',(-1.6211138875,1.72291666762259,-0.935950539335166));
#3500=CARTESIAN_POINT('Ctrl Pts',(-0.81055694375,1.66458333428926,-1.40392580900275));
#3501=CARTESIAN_POINT('Ctrl Pts',(-1.14620883215705E-16,1.60625000095592,
-1.87190107867033));
#3502=CARTESIAN_POINT('Ctrl Pts',(0.81055694375,1.54791666762259,-1.40392580900275));
#3503=CARTESIAN_POINT('Ctrl Pts',(1.6211138875,1.48958333428925,-0.935950539335166));
#3504=CARTESIAN_POINT('Ctrl Pts',(1.6211138875,1.43125000095592,-1.9852919333802E-16));
#3505=CARTESIAN_POINT('Origin',(-2.77555756156289E-16,71.6937500009559,
-2.08166817117217E-16));
#3506=CARTESIAN_POINT('',(1.6211138875,0.556250000955924,-2.08166817117217E-16));
#3507=CARTESIAN_POINT('',(1.6211138875,0.731250000955919,-2.08166817117217E-16));
#3508=CARTESIAN_POINT('',(1.6211138875,71.6937500009559,-2.17804440896414E-16));
#3509=CARTESIAN_POINT('Ctrl Pts',(1.6211138875,1.25625000095593,-1.9852919333802E-16));
#3510=CARTESIAN_POINT('Ctrl Pts',(1.6211138875,1.19791666762259,0.935950539335165));
#3511=CARTESIAN_POINT('Ctrl Pts',(0.810556943750001,1.13958333428926,1.40392580900275));
#3512=CARTESIAN_POINT('Ctrl Pts',(3.43862649647115E-16,1.08125000095592,
1.87190107867033));
#3513=CARTESIAN_POINT('Ctrl Pts',(-0.810556943749999,1.02291666762259,1.40392580900275));
#3514=CARTESIAN_POINT('Ctrl Pts',(-1.6211138875,0.964583334289254,0.935950539335167));
#3515=CARTESIAN_POINT('Ctrl Pts',(-1.6211138875,0.906250000955927,0.));
#3516=CARTESIAN_POINT('Ctrl Pts',(-1.6211138875,0.8479166676226,-0.935950539335166));
#3517=CARTESIAN_POINT('Ctrl Pts',(-0.81055694375,0.789583334289259,-1.40392580900275));
#3518=CARTESIAN_POINT('Ctrl Pts',(-1.14620883215705E-16,0.731250000955933,
-1.87190107867033));
#3519=CARTESIAN_POINT('Ctrl Pts',(0.81055694375,0.672916667622592,-1.40392580900275));
#3520=CARTESIAN_POINT('Ctrl Pts',(1.6211138875,0.614583334289265,-0.935950539335166));
#3521=CARTESIAN_POINT('Ctrl Pts',(1.6211138875,0.556250000955924,-1.9852919333802E-16));
#3522=CARTESIAN_POINT('Ctrl Pts',(1.6211138875,1.43125000095592,-1.9852919333802E-16));
#3523=CARTESIAN_POINT('Ctrl Pts',(1.6211138875,1.37291666762258,0.935950539335165));
#3524=CARTESIAN_POINT('Ctrl Pts',(0.810556943750001,1.31458333428926,1.40392580900275));
#3525=CARTESIAN_POINT('Ctrl Pts',(3.43862649647115E-16,1.25625000095592,
1.87190107867033));
#3526=CARTESIAN_POINT('Ctrl Pts',(-0.810556943749999,1.19791666762259,1.40392580900275));
#3527=CARTESIAN_POINT('Ctrl Pts',(-1.6211138875,1.13958333428925,0.935950539335167));
#3528=CARTESIAN_POINT('Ctrl Pts',(-1.6211138875,1.08125000095592,0.));
#3529=CARTESIAN_POINT('Ctrl Pts',(-1.6211138875,1.02291666762259,-0.935950539335166));
#3530=CARTESIAN_POINT('Ctrl Pts',(-0.81055694375,0.964583334289254,-1.40392580900275));
#3531=CARTESIAN_POINT('Ctrl Pts',(-1.14620883215705E-16,0.906250000955927,
-1.87190107867033));
#3532=CARTESIAN_POINT('Ctrl Pts',(0.81055694375,0.847916667622586,-1.40392580900275));
#3533=CARTESIAN_POINT('Ctrl Pts',(1.6211138875,0.789583334289259,-0.935950539335166));
#3534=CARTESIAN_POINT('Ctrl Pts',(1.6211138875,0.731250000955919,-1.9852919333802E-16));
#3535=CARTESIAN_POINT('Origin',(0.,70.,0.));
#3536=CARTESIAN_POINT('',(9.45320890747724E-15,9.17500000000001,2.));
#3537=CARTESIAN_POINT('',(1.59948180381188E-6,9.26250009520725,1.9999999999842));
#3538=CARTESIAN_POINT('',(-2.44929359829471E-16,70.,2.));
#3539=CARTESIAN_POINT('',(0.0859174328513604,9.52000000000001,-1.99815344810835));
#3540=CARTESIAN_POINT('Ctrl Pts',(7.0652298666267E-16,9.17500000000001,
2.));
#3541=CARTESIAN_POINT('Ctrl Pts',(0.0654772424788999,9.17881950581128,2.));
#3542=CARTESIAN_POINT('Ctrl Pts',(0.131032570471315,9.18264356661088,1.99678463284646));
#3543=CARTESIAN_POINT('Ctrl Pts',(0.450361646577216,9.20127109605039,1.96526945131892));
#3544=CARTESIAN_POINT('Ctrl Pts',(0.697209761447221,9.2156705694178,1.89183809047694));
#3545=CARTESIAN_POINT('Ctrl Pts',(1.1599092090385,9.2426613705273,1.65093392830596));
#3546=CARTESIAN_POINT('Ctrl Pts',(1.36930582965127,9.25674167404953,1.48190465126004));
#3547=CARTESIAN_POINT('Ctrl Pts',(1.7065994308231,9.28712492813149,1.07520874818695));
#3548=CARTESIAN_POINT('Ctrl Pts',(1.83255618803444,9.30253994528419,0.842791711206109));
#3549=CARTESIAN_POINT('Ctrl Pts',(1.9852210179839,9.33184741278064,0.35079538907281));
#3550=CARTESIAN_POINT('Ctrl Pts',(2.01363857356743,9.3447081787264,0.0968766608571719));
#3551=CARTESIAN_POINT('Ctrl Pts',(1.97330694803748,9.3719962043763,-0.420000685587666));
#3552=CARTESIAN_POINT('Ctrl Pts',(1.90028788275951,9.38714172438564,-0.677646653316077));
#3553=CARTESIAN_POINT('Ctrl Pts',(1.66096748133944,9.41766878114948,-1.14375396451092));
#3554=CARTESIAN_POINT('Ctrl Pts',(1.4991644205791,9.43275134166329,-1.34889419374688));
#3555=CARTESIAN_POINT('Ctrl Pts',(1.13680344977255,9.4590353597047,-1.65997361456257));
#3556=CARTESIAN_POINT('Ctrl Pts',(0.948658523269392,9.46966158614263,-1.77422571002165));
#3557=CARTESIAN_POINT('Ctrl Pts',(0.535425634758868,9.49376683797241,-1.94028063464073));
#3558=CARTESIAN_POINT('Ctrl Pts',(0.312304096132736,9.50678226105893,-1.98841950664599));
#3559=CARTESIAN_POINT('Ctrl Pts',(0.0859167558215111,9.51998818924375,-1.99815372558498));
#3560=CARTESIAN_POINT('',(-2.44929359829471E-16,9.52000000000001,2.));
#3561=CARTESIAN_POINT('Origin',(0.,9.52000000000001,0.));
#3562=CARTESIAN_POINT('',(2.44929359829471E-16,9.65431457505077,2.));
#3563=CARTESIAN_POINT('',(-2.44929359829471E-16,70.,2.));
#3564=CARTESIAN_POINT('',(-2.44929359829471E-16,9.65431457505077,-2.));
#3565=CARTESIAN_POINT('Origin',(0.,9.65431457505077,0.));
#3566=CARTESIAN_POINT('Origin',(0.,9.65431457505077,0.));
#3567=CARTESIAN_POINT('',(1.48658736561886,9.52000000000002,-1.33792828622799));
#3568=CARTESIAN_POINT('Origin',(0.,9.52000000000001,0.));
#3569=CARTESIAN_POINT('Ctrl Pts',(1.48734101297985,9.52000000000002,-1.33709263370496));
#3570=CARTESIAN_POINT('Ctrl Pts',(1.63791501835166,9.50714677517763,-1.169598708428));
#3571=CARTESIAN_POINT('Ctrl Pts',(1.75911955738823,9.49392572967888,-0.977867352719137));
#3572=CARTESIAN_POINT('Ctrl Pts',(1.93092564010499,9.46810888677228,-0.566018685335447));
#3573=CARTESIAN_POINT('Ctrl Pts',(1.98163283227066,9.45568175477737,-0.349301079153031));
#3574=CARTESIAN_POINT('Ctrl Pts',(2.01214704636104,9.43088073657671,0.124014372304799));
#3575=CARTESIAN_POINT('Ctrl Pts',(1.98031191750013,9.41785399914761,0.37752308269164));
#3576=CARTESIAN_POINT('Ctrl Pts',(1.82071231212849,9.3884011807903,0.868392811035422));
#3577=CARTESIAN_POINT('Ctrl Pts',(1.69094028902841,9.372919972832,1.09991733862416));
#3578=CARTESIAN_POINT('Ctrl Pts',(1.35539802709022,9.34330775640548,1.49236179051775));
#3579=CARTESIAN_POINT('Ctrl Pts',(1.15560569732876,9.32991033425602,1.65189509908556));
#3580=CARTESIAN_POINT('Ctrl Pts',(0.790412681009631,9.30860740830407,1.84408113448345));
#3581=CARTESIAN_POINT('Ctrl Pts',(0.641067231556676,9.29989559041931,1.90115935094908));
#3582=CARTESIAN_POINT('Ctrl Pts',(0.327456843583413,9.28160165112087,1.97981779131892));
#3583=CARTESIAN_POINT('Ctrl Pts',(0.164054865481099,9.2720698690649,1.99999671982436));
#3584=CARTESIAN_POINT('Ctrl Pts',(3.99936387195099E-5,9.2625023348741,1.99999999960013));
#3585=CARTESIAN_POINT('Origin',(0.,70.,0.));
#3586=CARTESIAN_POINT('',(-8.37541161687439E-15,8.475,2.));
#3587=CARTESIAN_POINT('',(1.48308516830053E-14,8.56250000191184,2.));
#3588=CARTESIAN_POINT('',(-2.44929359829471E-16,70.,2.));
#3589=CARTESIAN_POINT('Ctrl Pts',(7.59808882477842E-15,8.47500000000001,
2.));
#3590=CARTESIAN_POINT('Ctrl Pts',(0.105462367466573,8.48115197143556,2.));
#3591=CARTESIAN_POINT('Ctrl Pts',(0.211002460351238,8.48730847685385,1.99165844030807));
#3592=CARTESIAN_POINT('Ctrl Pts',(0.566317225824197,8.50803517150644,1.93487381835091));
#3593=CARTESIAN_POINT('Ctrl Pts',(0.807005156353637,8.52187416873751,1.84745781454963));
#3594=CARTESIAN_POINT('Ctrl Pts',(1.25252964810262,8.54829920549905,1.58160142821606));
#3595=CARTESIAN_POINT('Ctrl Pts',(1.4508881784191,8.56316568976568,1.40184370960763));
#3596=CARTESIAN_POINT('Ctrl Pts',(1.7631873502528,8.59362166091542,0.979277841388434));
#3597=CARTESIAN_POINT('Ctrl Pts',(1.87558951753305,8.60890636078586,0.741614671450395));
#3598=CARTESIAN_POINT('Ctrl Pts',(2.00138276505221,8.63777309815185,0.242828228006081));
#3599=CARTESIAN_POINT('Ctrl Pts',(2.01601583216441,8.65018696662936,-0.012947724454868));
#3600=CARTESIAN_POINT('Ctrl Pts',(1.94699225367654,8.67831894957769,-0.529965786082098));
#3601=CARTESIAN_POINT('Ctrl Pts',(1.85867649225116,8.69380137912261,-0.785449281408499));
#3602=CARTESIAN_POINT('Ctrl Pts',(1.59200912501479,8.7244228066855,-1.23763587188446));
#3603=CARTESIAN_POINT('Ctrl Pts',(1.41968985468868,8.73926989008554,-1.43204332669598));
#3604=CARTESIAN_POINT('Ctrl Pts',(1.00937069646563,8.76709572606385,-1.74595415512816));
#3605=CARTESIAN_POINT('Ctrl Pts',(0.774881221579688,8.77979859540789,-1.86192286742975));
#3606=CARTESIAN_POINT('Ctrl Pts',(0.269671873081754,8.80926914073694,-1.99928612004507));
#3607=CARTESIAN_POINT('Ctrl Pts',(0.00338211962886355,8.82480270968836,
-2.01738559898112));
#3608=CARTESIAN_POINT('Ctrl Pts',(-0.510960934847595,8.85480605453282,-1.95029153797676));
#3609=CARTESIAN_POINT('Ctrl Pts',(-0.754687604120902,8.86902344357376,-1.86954848788297));
#3610=CARTESIAN_POINT('Ctrl Pts',(-1.20800875702901,8.8954671774934,-1.61584007525765));
#3611=CARTESIAN_POINT('Ctrl Pts',(-1.41133074637823,8.90999891019387,-1.44169119402485));
#3612=CARTESIAN_POINT('Ctrl Pts',(-1.73576755166978,8.94039724159011,-1.02727396296809));
#3613=CARTESIAN_POINT('Ctrl Pts',(-1.85492262965682,8.95575220708085,-0.792118689280096));
#3614=CARTESIAN_POINT('Ctrl Pts',(-1.99405667036303,8.98484046001804,-0.296649685242302));
#3615=CARTESIAN_POINT('Ctrl Pts',(-2.01556246576001,8.99743240884776,-0.0418401299621862));
#3616=CARTESIAN_POINT('Ctrl Pts',(-1.96104169758539,9.02508165764329,0.473995475055345));
#3617=CARTESIAN_POINT('Ctrl Pts',(-1.88096840075696,9.04032842551777,0.729572868260019));
#3618=CARTESIAN_POINT('Ctrl Pts',(-1.62924249842628,9.07084754148429,1.18836067314294));
#3619=CARTESIAN_POINT('Ctrl Pts',(-1.46241462989662,9.08582531086932,1.38852550186937));
#3620=CARTESIAN_POINT('Ctrl Pts',(-1.06248382247422,9.11392601041099,1.71387493493997));
#3621=CARTESIAN_POINT('Ctrl Pts',(-0.833398741972677,9.12638507338498,1.83621648971916));
#3622=CARTESIAN_POINT('Ctrl Pts',(-0.396706359840074,9.15185879567604,1.97038257217702));
#3623=CARTESIAN_POINT('Ctrl Pts',(-0.198712772962524,9.16340842157719,2.));
#3624=CARTESIAN_POINT('Ctrl Pts',(-8.53483950180589E-15,9.17500000000001,
2.));
#3625=CARTESIAN_POINT('Ctrl Pts',(1.90566659674651E-11,9.26250000191294,
2.00000000000002));
#3626=CARTESIAN_POINT('Ctrl Pts',(-0.257304108099317,9.24749059560743,2.00000000000006));
#3627=CARTESIAN_POINT('Ctrl Pts',(-0.512236880529356,9.23261951721429,1.95034594378667));
#3628=CARTESIAN_POINT('Ctrl Pts',(-0.981276227019413,9.20525888866904,1.76038092822654));
#3629=CARTESIAN_POINT('Ctrl Pts',(-1.19231374107119,9.19314353837047,1.62488180827426));
#3630=CARTESIAN_POINT('Ctrl Pts',(-1.5622316908883,9.16470757636485,1.27556796811243));
#3631=CARTESIAN_POINT('Ctrl Pts',(-1.71468144646498,9.14946372091359,1.06183479387747));
#3632=CARTESIAN_POINT('Ctrl Pts',(-1.93127233317037,9.11898066356148,0.583475553719287));
#3633=CARTESIAN_POINT('Ctrl Pts',(-1.99153619176926,9.10404547537348,0.322628854278394));
#3634=CARTESIAN_POINT('Ctrl Pts',(-2.00646871390316,9.07742145493661,-0.19576877688697));
#3635=CARTESIAN_POINT('Ctrl Pts',(-1.96554314136245,9.06384851194789,-0.448284406729788));
#3636=CARTESIAN_POINT('Ctrl Pts',(-1.78817028005374,9.03415566366629,-0.933644101450979));
#3637=CARTESIAN_POINT('Ctrl Pts',(-1.64995028952709,9.01866059682148,-1.16056553033455));
#3638=CARTESIAN_POINT('Ctrl Pts',(-1.29415730903856,8.98874903328475,-1.54724376046733));
#3639=CARTESIAN_POINT('Ctrl Pts',(-1.08034993983026,8.97552041506857,-1.70341423900341));
#3640=CARTESIAN_POINT('Ctrl Pts',(-0.609968446726665,8.94808149463753,-1.92189375954845));
#3641=CARTESIAN_POINT('Ctrl Pts',(-0.358856680588314,8.93343330827946,-1.98416774025015));
#3642=CARTESIAN_POINT('Ctrl Pts',(0.163198666704829,8.90298007968736,-2.0110569238483));
#3643=CARTESIAN_POINT('Ctrl Pts',(0.42937403919576,8.88745318295873,-1.97145826744264));
#3644=CARTESIAN_POINT('Ctrl Pts',(0.92000150326077,8.85883324755494,-1.79408447591622));
#3645=CARTESIAN_POINT('Ctrl Pts',(1.14116649734624,8.84652018704735,-1.66219224268598));
#3646=CARTESIAN_POINT('Ctrl Pts',(1.5251146797244,8.81801352796414,-1.3195793218663));
#3647=CARTESIAN_POINT('Ctrl Pts',(1.68318697174025,8.80286160175781,-1.1109120476771));
#3648=CARTESIAN_POINT('Ctrl Pts',(1.91338699615764,8.77234334845276,-0.639713347655176));
#3649=CARTESIAN_POINT('Ctrl Pts',(1.98126220145905,8.75727847929295,-0.380694043773767));
#3650=CARTESIAN_POINT('Ctrl Pts',(2.01131636650622,8.7302565099176,0.136850448845239));
#3651=CARTESIAN_POINT('Ctrl Pts',(1.97786148928562,8.71714353473363,0.390171872482263));
#3652=CARTESIAN_POINT('Ctrl Pts',(1.81527538666286,8.68767894754209,0.879550308535442));
#3653=CARTESIAN_POINT('Ctrl Pts',(1.68436773280673,8.67222716163985,1.10983677648947));
#3654=CARTESIAN_POINT('Ctrl Pts',(1.33956700707109,8.64202942504695,1.50852614526927));
#3655=CARTESIAN_POINT('Ctrl Pts',(1.12839208065064,8.62832287328311,1.67235528110575));
#3656=CARTESIAN_POINT('Ctrl Pts',(0.662588073022141,8.60115097283811,1.90430099781709));
#3657=CARTESIAN_POINT('Ctrl Pts',(0.413980559775339,8.58664886789871,1.97331305372972));
#3658=CARTESIAN_POINT('Ctrl Pts',(0.106132978563006,8.56869109232799,1.99789044226144));
#3659=CARTESIAN_POINT('Ctrl Pts',(0.0530358871513877,8.56559376199567,2.));
#3660=CARTESIAN_POINT('Ctrl Pts',(7.41933818794109E-16,8.56250000191184,
2.));
#3661=CARTESIAN_POINT('Origin',(0.,70.,0.));
#3662=CARTESIAN_POINT('',(1.33173054502156E-14,7.77500000000001,2.));
#3663=CARTESIAN_POINT('',(2.75550483792952E-14,7.86250000191184,2.));
#3664=CARTESIAN_POINT('',(-2.44929359829471E-16,70.,2.));
#3665=CARTESIAN_POINT('Ctrl Pts',(5.86336534880161E-15,7.77500000000001,
2.));
#3666=CARTESIAN_POINT('Ctrl Pts',(0.144710179754815,7.78344142715237,2.));
#3667=CARTESIAN_POINT('Ctrl Pts',(0.289338759461054,7.79187809430192,1.98429396284856));
#3668=CARTESIAN_POINT('Ctrl Pts',(0.678641071003376,7.81458739580856,1.89831552691932));
#3669=CARTESIAN_POINT('Ctrl Pts',(0.913286535675115,7.827511604482,1.79722711026655));
#3670=CARTESIAN_POINT('Ctrl Pts',(1.34230244411645,7.8547280067094,1.50617451526789));
#3671=CARTESIAN_POINT('Ctrl Pts',(1.52994621267493,7.86985230922693,1.31512714824939));
#3672=CARTESIAN_POINT('Ctrl Pts',(1.81638341917427,7.90037819173438,0.876245981398777));
#3673=CARTESIAN_POINT('Ctrl Pts',(1.91447157603324,7.91548006520074,0.633937637928994));
#3674=CARTESIAN_POINT('Ctrl Pts',(2.01219327080911,7.943863981205,0.128501460288878));
#3675=CARTESIAN_POINT('Ctrl Pts',(2.01212313264796,7.95619331976415,-0.12959523102893));
#3676=CARTESIAN_POINT('Ctrl Pts',(1.91277780465302,7.98497332866613,-0.641934609574077));
#3677=CARTESIAN_POINT('Ctrl Pts',(1.81050911014114,8.00050874900382,-0.890411320888694));
#3678=CARTESIAN_POINT('Ctrl Pts',(1.5203852399451,8.03089334619851,-1.3243672675752));
#3679=CARTESIAN_POINT('Ctrl Pts',(1.33856236024206,8.04546904366245,-1.5079157626145));
#3680=CARTESIAN_POINT('Ctrl Pts',(0.909424776687682,8.07277395533603,-1.80065014111363));
#3681=CARTESIAN_POINT('Ctrl Pts',(0.66460770222988,8.08623121736996,-1.90466015281606));
#3682=CARTESIAN_POINT('Ctrl Pts',(0.149343889657557,8.11628827310334,-2.01164976474229));
#3683=CARTESIAN_POINT('Ctrl Pts',(-0.11594189746457,8.13176327735213,-2.01385064625415));
#3684=CARTESIAN_POINT('Ctrl Pts',(-0.623007461315161,8.16134210191008,-1.91731213129782));
#3685=CARTESIAN_POINT('Ctrl Pts',(-0.86061755342047,8.17467105579428,-1.8230469408812));
#3686=CARTESIAN_POINT('Ctrl Pts',(-1.29795031623099,8.2014956207513,-1.54455245039818));
#3687=CARTESIAN_POINT('Ctrl Pts',(-1.49103788648041,8.21649747918302,-1.35907182806801));
#3688=CARTESIAN_POINT('Ctrl Pts',(-1.79052008750211,8.24700149799274,-0.928154981291581));
#3689=CARTESIAN_POINT('Ctrl Pts',(-1.89578969583597,8.26220076216339,-0.688065014786461));
#3690=CARTESIAN_POINT('Ctrl Pts',(-2.00756828407403,8.29082923214331,-0.185903675101916));
#3691=CARTESIAN_POINT('Ctrl Pts',(-2.01490631812433,8.30315113975425,0.0709825571365514));
#3692=CARTESIAN_POINT('Ctrl Pts',(-1.93082980082602,8.33160909865332,0.585762450874943));
#3693=CARTESIAN_POINT('Ctrl Pts',(-1.83553236798457,8.3471242386706,0.837862575759251));
#3694=CARTESIAN_POINT('Ctrl Pts',(-1.55708628702896,8.37763996900972,1.28115646027813));
#3695=CARTESIAN_POINT('Ctrl Pts',(-1.37997141252304,8.39235776994509,1.47023604261329));
#3696=CARTESIAN_POINT('Ctrl Pts',(-0.960303803133177,8.41992859304112,1.7737015943198));
#3697=CARTESIAN_POINT('Ctrl Pts',(-0.720770852159437,8.43295503362406,1.88380283908764));
#3698=CARTESIAN_POINT('Ctrl Pts',(-0.313547604702796,8.45670972305903,1.98154568112522));
#3699=CARTESIAN_POINT('Ctrl Pts',(-0.15685977517984,8.46584984644785,2.));
#3700=CARTESIAN_POINT('Ctrl Pts',(2.04697370165263E-14,8.47500000000001,
2.));
#3701=CARTESIAN_POINT('Ctrl Pts',(-6.34908792207511E-15,8.56250000191184,
2.));
#3702=CARTESIAN_POINT('Ctrl Pts',(-0.211791443364041,8.55014550104893,2.));
#3703=CARTESIAN_POINT('Ctrl Pts',(-0.422606866547989,8.53784793469652,1.9663553689863));
#3704=CARTESIAN_POINT('Ctrl Pts',(-0.868081090589095,8.51186193829412,1.81994308052866));
#3705=CARTESIAN_POINT('Ctrl Pts',(-1.09398569432927,8.49949294438145,1.69379772754904));
#3706=CARTESIAN_POINT('Ctrl Pts',(-1.48760806966432,8.4712296434194,1.36158744612626));
#3707=CARTESIAN_POINT('Ctrl Pts',(-1.65102289478909,8.45617923347963,1.15801418579668));
#3708=CARTESIAN_POINT('Ctrl Pts',(-1.89430688679977,8.42565217494147,0.694195219573794));
#3709=CARTESIAN_POINT('Ctrl Pts',(-1.96957247437605,8.41047322719565,0.437184584522383));
#3710=CARTESIAN_POINT('Ctrl Pts',(-2.01441005981556,8.38306971268874,-0.0793773312476014));
#3711=CARTESIAN_POINT('Ctrl Pts',(-1.98819231399505,8.37030423910157,-0.333570656303743));
#3712=CARTESIAN_POINT('Ctrl Pts',(-1.83984508919913,8.34106611245623,-0.82668715605278));
#3713=CARTESIAN_POINT('Ctrl Pts',(-1.71605288881846,8.32566902073102,-1.05999906906072));
#3714=CARTESIAN_POINT('Ctrl Pts',(-1.38205991004181,8.29520673661087,-1.47016497640736));
#3715=CARTESIAN_POINT('Ctrl Pts',(-1.1734417375009,8.2809507699327,-1.64147268846638));
#3716=CARTESIAN_POINT('Ctrl Pts',(-0.712101744651061,8.2540392703498,-1.88625652499066));
#3717=CARTESIAN_POINT('Ctrl Pts',(-0.466038132703796,8.23968555965287,-1.96158530310034));
#3718=CARTESIAN_POINT('Ctrl Pts',(0.0509150518454933,8.20952995722083,-2.01682795565735));
#3719=CARTESIAN_POINT('Ctrl Pts',(0.317346157923531,8.19398814269962,-1.99235909767874));
#3720=CARTESIAN_POINT('Ctrl Pts',(0.818350872074179,8.16476286770749,-1.84303438253474));
#3721=CARTESIAN_POINT('Ctrl Pts',(1.04882097278607,8.15225195365897,-1.72233608337629));
#3722=CARTESIAN_POINT('Ctrl Pts',(1.45145272527099,8.12422186462602,-1.39994376724921));
#3723=CARTESIAN_POINT('Ctrl Pts',(1.6197241441659,8.10927675151018,-1.20125879919931));
#3724=CARTESIAN_POINT('Ctrl Pts',(1.87504113665927,8.07876436630004,-0.744677545611848));
#3725=CARTESIAN_POINT('Ctrl Pts',(1.95716921969409,8.06349017467688,-0.48974363433592));
#3726=CARTESIAN_POINT('Ctrl Pts',(2.01584665253484,8.03573648438144,0.0257595247521755));
#3727=CARTESIAN_POINT('Ctrl Pts',(1.99635790625494,8.02320603143971,0.280844471619683));
#3728=CARTESIAN_POINT('Ctrl Pts',(1.8611518568783,7.99418245413774,0.777301056952316));
#3729=CARTESIAN_POINT('Ctrl Pts',(1.74398071264898,7.97884704441316,1.0132146515514));
#3730=CARTESIAN_POINT('Ctrl Pts',(1.4230787837332,7.94842748141968,1.43009302106559));
#3731=CARTESIAN_POINT('Ctrl Pts',(1.22120597579789,7.9337370171667,1.6058827908322));
#3732=CARTESIAN_POINT('Ctrl Pts',(0.770197508503904,7.90742818990788,1.86318425309167));
#3733=CARTESIAN_POINT('Ctrl Pts',(0.527356863978595,7.89326248564391,1.94589485813412));
#3734=CARTESIAN_POINT('Ctrl Pts',(0.184077252924329,7.87323784166574,1.99365311316229));
#3735=CARTESIAN_POINT('Ctrl Pts',(0.0919931555425928,7.86786626931849,2.));
#3736=CARTESIAN_POINT('Ctrl Pts',(7.41933818794109E-16,7.86250000191184,
2.));
#3737=CARTESIAN_POINT('Origin',(0.,70.,0.));
#3738=CARTESIAN_POINT('',(1.15522243134092E-14,7.07500000000001,2.));
#3739=CARTESIAN_POINT('',(2.77424798298637E-14,7.16250000191184,2.));
#3740=CARTESIAN_POINT('',(-2.44929359829471E-16,70.,2.));
#3741=CARTESIAN_POINT('Ctrl Pts',(2.77555756156289E-15,7.07500000000001,
2.));
#3742=CARTESIAN_POINT('Ctrl Pts',(0.18075001537359,7.0855437508968,2.));
#3743=CARTESIAN_POINT('Ctrl Pts',(0.361045488426424,7.09606098682489,1.97549558457209));
#3744=CARTESIAN_POINT('Ctrl Pts',(0.780464168592415,7.12052707650124,1.85884827886082));
#3745=CARTESIAN_POINT('Ctrl Pts',(1.00980068654218,7.13296927010253,1.74491581958734));
#3746=CARTESIAN_POINT('Ctrl Pts',(1.424797160282,7.16103928503801,1.42887195069992));
#3747=CARTESIAN_POINT('Ctrl Pts',(1.60308448387472,7.1765141876913,1.22548255482433));
#3748=CARTESIAN_POINT('Ctrl Pts',(1.86388487381245,7.20715280130596,0.769568467827498));
#3749=CARTESIAN_POINT('Ctrl Pts',(1.94739624750753,7.22202289434249,0.523432277310207));
#3750=CARTESIAN_POINT('Ctrl Pts',(2.01664966892294,7.2498957261951,0.0116767768689988));
#3751=CARTESIAN_POINT('Ctrl Pts',(2.00124002591604,7.2625490039063,-0.249121784725706));
#3752=CARTESIAN_POINT('Ctrl Pts',(1.87045356876465,7.29196387648333,-0.755875660500865));
#3753=CARTESIAN_POINT('Ctrl Pts',(1.7542241045094,7.30750009794585,-0.996307975805123));
#3754=CARTESIAN_POINT('Ctrl Pts',(1.44098348851282,7.33753973800396,-1.41008908265801));
#3755=CARTESIAN_POINT('Ctrl Pts',(1.24999174383528,7.35178900326569,-1.58188224921385));
#3756=CARTESIAN_POINT('Ctrl Pts',(0.804853188205148,7.37831632268762,-1.84998612746433));
#3757=CARTESIAN_POINT('Ctrl Pts',(0.552818933868428,7.3927522288577,-1.94028996818693));
#3758=CARTESIAN_POINT('Ctrl Pts',(0.0319492719416979,7.42313629247009,-2.01673692536205));
#3759=CARTESIAN_POINT('Ctrl Pts',(-0.2314801387626,7.43850300809451,-2.00366511395298));
#3760=CARTESIAN_POINT('Ctrl Pts',(-0.73082548624653,7.46763148669773,-1.87886356825441));
#3761=CARTESIAN_POINT('Ctrl Pts',(-0.962733721555366,7.48026571814896,-1.77125814433366));
#3762=CARTESIAN_POINT('Ctrl Pts',(-1.38366999666347,7.5078495257626,-1.4682680303301));
#3763=CARTESIAN_POINT('Ctrl Pts',(-1.56595192662907,7.52307867990314,-1.27204948049025));
#3764=CARTESIAN_POINT('Ctrl Pts',(-1.83971471151476,7.55360098365991,-0.825921573800778));
#3765=CARTESIAN_POINT('Ctrl Pts',(-1.93089668745128,7.56859866822386,-0.581688350316966));
#3766=CARTESIAN_POINT('Ctrl Pts',(-2.01512890183861,7.59674314815885,-0.073203622539262));
#3767=CARTESIAN_POINT('Ctrl Pts',(-2.0078505381786,7.60917390033838,0.186128641640483));
#3768=CARTESIAN_POINT('Ctrl Pts',(-1.89369140290797,7.63825805879553,0.695935864369098));
#3769=CARTESIAN_POINT('Ctrl Pts',(-1.78477579336675,7.65380071724004,0.940718254859585));
#3770=CARTESIAN_POINT('Ctrl Pts',(-1.48359922254668,7.68403526170145,1.36532264806138));
#3771=CARTESIAN_POINT('Ctrl Pts',(-1.29736617565955,7.6984627489118,1.54339112972496));
#3772=CARTESIAN_POINT('Ctrl Pts',(-0.859053556344717,7.7255025169672,1.82557981636653));
#3773=CARTESIAN_POINT('Ctrl Pts',(-0.608949336314592,7.73947795538168,1.92352746147435));
#3774=CARTESIAN_POINT('Ctrl Pts',(-0.232127609363206,7.76145922278717,1.9899015910211));
#3775=CARTESIAN_POINT('Ctrl Pts',(-0.116037570983665,7.76823114169263,2.));
#3776=CARTESIAN_POINT('Ctrl Pts',(-1.30451205393456E-14,7.77500000000001,
2.));
#3777=CARTESIAN_POINT('Ctrl Pts',(-8.81239525796218E-15,7.86250000191184,
2.));
#3778=CARTESIAN_POINT('Ctrl Pts',(-0.170927915536333,7.85252920683889,2.));
#3779=CARTESIAN_POINT('Ctrl Pts',(-0.341541867911621,7.84257672628365,1.97808665376321));
#3780=CARTESIAN_POINT('Ctrl Pts',(-0.758885913122223,7.81823165697969,1.86857667624832));
#3781=CARTESIAN_POINT('Ctrl Pts',(-0.994861517242304,7.80544273906337,1.75434374789522));
#3782=CARTESIAN_POINT('Ctrl Pts',(-1.40796857062281,7.77769218627607,1.44353273218894));
#3783=CARTESIAN_POINT('Ctrl Pts',(-1.58173289424033,7.76288250550425,1.25069995931156));
#3784=CARTESIAN_POINT('Ctrl Pts',(-1.85193784129827,7.73229012686178,0.801130810995777));
#3785=CARTESIAN_POINT('Ctrl Pts',(-1.94234540788994,7.71679662924098,0.54663592886225));
#3786=CARTESIAN_POINT('Ctrl Pts',(-2.01585596229509,7.68856662216761,0.0302680495322416));
#3787=CARTESIAN_POINT('Ctrl Pts',(-2.00339738064947,7.67619058053996,-0.225829963435849));
#3788=CARTESIAN_POINT('Ctrl Pts',(-1.88179826829948,7.64739455891102,-0.725638083383513));
#3789=CARTESIAN_POINT('Ctrl Pts',(-1.77152704155437,7.63213418936647,-0.964049936863562));
#3790=CARTESIAN_POINT('Ctrl Pts',(-1.46304234590713,7.60166108043189,-1.3891573340967));
#3791=CARTESIAN_POINT('Ctrl Pts',(-1.26624422002002,7.58675269938869,-1.57064529371589));
#3792=CARTESIAN_POINT('Ctrl Pts',(-0.823160978616651,7.56020718367607,-1.84029600133115));
#3793=CARTESIAN_POINT('Ctrl Pts',(-0.583407349987985,7.5465320973278,-1.92976747259992));
#3794=CARTESIAN_POINT('Ctrl Pts',(-0.0736314799885643,7.51679517157783,
-2.01591269398287));
#3795=CARTESIAN_POINT('Ctrl Pts',(0.192116356904062,7.50129321442576,-2.00808913417545));
#3796=CARTESIAN_POINT('Ctrl Pts',(0.703897777311664,7.47143929823532,-1.89026446179254));
#3797=CARTESIAN_POINT('Ctrl Pts',(0.945012887021492,7.45829339178382,-1.7819919174932));
#3798=CARTESIAN_POINT('Ctrl Pts',(1.36754933020624,7.43080230809323,-1.48176111862576));
#3799=CARTESIAN_POINT('Ctrl Pts',(1.54610675000263,7.41612637933859,-1.2943432444248));
#3800=CARTESIAN_POINT('Ctrl Pts',(1.82811837678127,7.3856478205279,-0.853843734184673));
#3801=CARTESIAN_POINT('Ctrl Pts',(1.92553893926196,7.37012516637964,-0.602820657550663));
#3802=CARTESIAN_POINT('Ctrl Pts',(2.01423887029515,7.34156875761561,-0.0887612910552623));
#3803=CARTESIAN_POINT('Ctrl Pts',(2.00914246080169,7.3292552201465,0.168482755517828));
#3804=CARTESIAN_POINT('Ctrl Pts',(1.90163687533782,7.30070050621638,0.671651123354299));
#3805=CARTESIAN_POINT('Ctrl Pts',(1.79854795643332,7.28552962113398,0.912438351228735));
#3806=CARTESIAN_POINT('Ctrl Pts',(1.5030122408241,7.25501617620551,1.34582029118175));
#3807=CARTESIAN_POINT('Ctrl Pts',(1.31156334985062,7.23997567820554,1.53301187052302));
#3808=CARTESIAN_POINT('Ctrl Pts',(0.876747931810209,7.21303104797744,1.81533642668372));
#3809=CARTESIAN_POINT('Ctrl Pts',(0.640051660201568,7.19983634875693,1.91168002068908));
#3810=CARTESIAN_POINT('Ctrl Pts',(0.262351243869515,7.17780382447089,1.98709445304633));
#3811=CARTESIAN_POINT('Ctrl Pts',(0.131176897671107,7.17015198760932,2.));
#3812=CARTESIAN_POINT('Ctrl Pts',(1.94635974004598E-14,7.16250000191184,
2.));
#3813=CARTESIAN_POINT('Origin',(0.,70.,0.));
#3814=CARTESIAN_POINT('',(-1.84411445862298E-14,6.37500000000001,2.));
#3815=CARTESIAN_POINT('',(-2.40529750310148E-14,6.46250000191183,2.));
#3816=CARTESIAN_POINT('',(-2.44929359829471E-16,70.,2.));
#3817=CARTESIAN_POINT('Ctrl Pts',(-1.17961196366423E-15,6.37500000000001,
2.));
#3818=CARTESIAN_POINT('Ctrl Pts',(0.218380548180877,6.38773886531056,2.));
#3819=CARTESIAN_POINT('Ctrl Pts',(0.435591688754577,6.40040951517736,1.96422966283633));
#3820=CARTESIAN_POINT('Ctrl Pts',(0.884929306534349,6.42662087621452,1.81168954605897));
#3821=CARTESIAN_POINT('Ctrl Pts',(1.10891682053198,6.438941027859,1.68393039943082));
#3822=CARTESIAN_POINT('Ctrl Pts',(1.50482320290809,6.46765999926712,1.34401885449842));
#3823=CARTESIAN_POINT('Ctrl Pts',(1.67015368308462,6.48319254064221,1.13200787079262));
#3824=CARTESIAN_POINT('Ctrl Pts',(1.90358767799519,6.51360412968123,0.664787709398107));
#3825=CARTESIAN_POINT('Ctrl Pts',(1.9730051297779,6.52820790949486,0.415786023931368));
#3826=CARTESIAN_POINT('Ctrl Pts',(2.01464938398039,6.55556436137238,-0.101687964028044));
#3827=CARTESIAN_POINT('Ctrl Pts',(1.98385038468369,6.56893096680269,-0.365411973405472));
#3828=CARTESIAN_POINT('Ctrl Pts',(1.82194588911147,6.59893251064738,-0.865812920669644));
#3829=CARTESIAN_POINT('Ctrl Pts',(1.69248158566176,6.61441563030838,-1.0975529549371));
#3830=CARTESIAN_POINT('Ctrl Pts',(1.35744755693107,6.64403843999516,-1.49050052758113));
#3831=CARTESIAN_POINT('Ctrl Pts',(1.15786121375317,6.65745809586443,-1.6503169834607));
#3832=CARTESIAN_POINT('Ctrl Pts',(0.699330416206954,6.68420572572129,-1.89241907057509));
#3833=CARTESIAN_POINT('Ctrl Pts',(0.442588821013814,6.69918231877421,-1.96834453019336));
#3834=CARTESIAN_POINT('Ctrl Pts',(-0.0802124617398179,6.72967906026817,
-2.0152105369091));
#3835=CARTESIAN_POINT('Ctrl Pts',(-0.341071598113087,6.74489584322328,-1.98776130908745));
#3836=CARTESIAN_POINT('Ctrl Pts',(-0.832646432250627,6.7735710418813,-1.83616520518011));
#3837=CARTESIAN_POINT('Ctrl Pts',(-1.05930402513081,6.78590309899885,-1.71542183448551));
#3838=CARTESIAN_POINT('Ctrl Pts',(-1.46493654415258,6.81429808767927,-1.38753887196545));
#3839=CARTESIAN_POINT('Ctrl Pts',(-1.6368748729707,6.8298078339344,-1.17979415780545));
#3840=CARTESIAN_POINT('Ctrl Pts',(-1.88421942023241,6.86034603599379,-0.718098969736138));
#3841=CARTESIAN_POINT('Ctrl Pts',(-1.96078093250865,6.87508991725929,-0.470448619999976));
#3842=CARTESIAN_POINT('Ctrl Pts',(-2.01644214931359,6.9027110607266,0.0441722054775648));
#3843=CARTESIAN_POINT('Ctrl Pts',(-1.99352526301469,6.91566651786864,0.306378436585966));
#3844=CARTESIAN_POINT('Ctrl Pts',(-1.84749330568526,6.94537423800143,0.810127196963264));
#3845=CARTESIAN_POINT('Ctrl Pts',(-1.72470323726598,6.96089109295482,1.04638838822703));
#3846=CARTESIAN_POINT('Ctrl Pts',(-1.40063186189325,6.99073713004903,1.45008400843909));
#3847=CARTESIAN_POINT('Ctrl Pts',(-1.2054102831749,7.00468440014814,1.61598195763032));
#3848=CARTESIAN_POINT('Ctrl Pts',(-0.753718017516963,7.03103311564486,1.87141600842067));
#3849=CARTESIAN_POINT('Ctrl Pts',(-0.4993269770152,7.04587259300746,1.95471461206462));
#3850=CARTESIAN_POINT('Ctrl Pts',(-0.157628533769269,7.06580500219681,1.99534645887765));
#3851=CARTESIAN_POINT('Ctrl Pts',(-0.0787711029033106,7.07040501899732,
2.));
#3852=CARTESIAN_POINT('Ctrl Pts',(7.06522986662669E-16,7.07500000000001,
2.));
#3853=CARTESIAN_POINT('Ctrl Pts',(7.28583859910259E-16,7.16250000191184,
2.));
#3854=CARTESIAN_POINT('Ctrl Pts',(-0.130085342337019,7.15491169027551,2.));
#3855=CARTESIAN_POINT('Ctrl Pts',(-0.260173193860504,7.14732323226997,1.98730835440023));
#3856=CARTESIAN_POINT('Ctrl Pts',(-0.647613436418503,7.12472255145409,1.91060868087785));
#3857=CARTESIAN_POINT('Ctrl Pts',(-0.894039501496567,7.11111652008545,1.80844586712125));
#3858=CARTESIAN_POINT('Ctrl Pts',(-1.32599961792236,7.08389237484571,1.51893983950038));
#3859=CARTESIAN_POINT('Ctrl Pts',(-1.50919536615133,7.06936117580825,1.33706481088031));
#3860=CARTESIAN_POINT('Ctrl Pts',(-1.80274755706425,7.03902033480642,0.905954354073171));
#3861=CARTESIAN_POINT('Ctrl Pts',(-1.90707273670512,7.02348138496407,0.658595088928268));
#3862=CARTESIAN_POINT('Ctrl Pts',(-2.01097324670968,6.99460692224855,0.147015945325011));
#3863=CARTESIAN_POINT('Ctrl Pts',(-2.01325706028901,6.98225626544635,-0.111453029951849));
#3864=CARTESIAN_POINT('Ctrl Pts',(-1.91969827815215,6.95394570843383,-0.617840534886077));
#3865=CARTESIAN_POINT('Ctrl Pts',(-1.82374050019459,6.93887488292517,-0.860764263014212));
#3866=CARTESIAN_POINT('Ctrl Pts',(-1.54119962505294,6.90834755189457,-1.30192365114519));
#3867=CARTESIAN_POINT('Ctrl Pts',(-1.35519670898698,6.89318956543488,-1.49458513392608));
#3868=CARTESIAN_POINT('Ctrl Pts',(-0.928663878567721,6.86585886200204,-1.78933391177686));
#3869=CARTESIAN_POINT('Ctrl Pts',(-0.694874058553572,6.85303432199413,-1.89243627183466));
#3870=CARTESIAN_POINT('Ctrl Pts',(-0.192898216433379,6.82375239787045,-2.00781138139783));
#3871=CARTESIAN_POINT('Ctrl Pts',(0.0712480461586881,6.80834386588591,-2.0157963318781));
#3872=CARTESIAN_POINT('Ctrl Pts',(0.592606320201799,6.77793129990006,-1.92873446867424));
#3873=CARTESIAN_POINT('Ctrl Pts',(0.844272547940869,6.76378702629052,-1.83257521656462));
#3874=CARTESIAN_POINT('Ctrl Pts',(1.28524275043711,6.73682548011264,-1.55346927790099));
#3875=CARTESIAN_POINT('Ctrl Pts',(1.47272450383278,6.72244283300577,-1.37700934113293));
#3876=CARTESIAN_POINT('Ctrl Pts',(1.77705222671155,6.69225595917844,-0.95516790025197));
#3877=CARTESIAN_POINT('Ctrl Pts',(1.88787211036145,6.67671349033682,-0.71148869609447));
#3878=CARTESIAN_POINT('Ctrl Pts',(2.0063256635788,6.64754281569382,-0.202448280385498));
#3879=CARTESIAN_POINT('Ctrl Pts',(2.01569937528843,6.63506547903315,0.0572550936125673));
#3880=CARTESIAN_POINT('Ctrl Pts',(1.93535184143689,6.6069908702112,0.566599553397501));
#3881=CARTESIAN_POINT('Ctrl Pts',(1.8461595770448,6.59202509099077,0.811349975365595));
#3882=CARTESIAN_POINT('Ctrl Pts',(1.57607152285567,6.5615082351801,1.25949164744684));
#3883=CARTESIAN_POINT('Ctrl Pts',(1.39535709278812,6.54625119348052,1.45716722427951));
#3884=CARTESIAN_POINT('Ctrl Pts',(0.976765707076176,6.51856319528433,1.76357359946584));
#3885=CARTESIAN_POINT('Ctrl Pts',(0.745627243960202,6.50599492447618,1.87305159405641));
#3886=CARTESIAN_POINT('Ctrl Pts',(0.336420990336705,6.48212455968148,1.97874051917636));
#3887=CARTESIAN_POINT('Ctrl Pts',(0.168358723701333,6.47232092746108,2.));
#3888=CARTESIAN_POINT('Ctrl Pts',(-1.93942084614207E-14,6.46250000191184,
2.));
#3889=CARTESIAN_POINT('Origin',(0.,70.,0.));
#3890=CARTESIAN_POINT('',(-4.66744018697397E-15,5.67500000000001,2.));
#3891=CARTESIAN_POINT('',(-1.75217411439621E-14,5.76250000191184,2.));
#3892=CARTESIAN_POINT('',(-2.44929359829471E-16,70.,2.));
#3893=CARTESIAN_POINT('Ctrl Pts',(-2.82412981889024E-14,5.67500000000001,
2.));
#3894=CARTESIAN_POINT('Ctrl Pts',(0.256622987290695,5.68996967425863,2.));
#3895=CARTESIAN_POINT('Ctrl Pts',(0.510903094812502,5.70480268053074,1.95060829662963));
#3896=CARTESIAN_POINT('Ctrl Pts',(0.98864487151693,5.73267095083849,1.75767422282175));
#3897=CARTESIAN_POINT('Ctrl Pts',(1.20729575864517,5.74527608905864,1.61532781592622));
#3898=CARTESIAN_POINT('Ctrl Pts',(1.58274048039481,5.77463261224839,1.25098247340035));
#3899=CARTESIAN_POINT('Ctrl Pts',(1.73418273505864,5.79017111479687,1.03083511832571));
#3900=CARTESIAN_POINT('Ctrl Pts',(1.93867276023932,5.82024768614334,0.5535357786726));
#3901=CARTESIAN_POINT('Ctrl Pts',(1.99335332242581,5.8345297636046,0.302393801107101));
#3902=CARTESIAN_POINT('Ctrl Pts',(2.00575387368111,5.86114343640657,-0.217260834076487));
#3903=CARTESIAN_POINT('Ctrl Pts',(1.95934408693273,5.87548241404785,-0.480948278564949));
#3904=CARTESIAN_POINT('Ctrl Pts',(1.76766966346345,5.90585080865594,-0.971423311783889));
#3905=CARTESIAN_POINT('Ctrl Pts',(1.62571995226474,5.92122936175023,-1.19388501131151));
#3906=CARTESIAN_POINT('Ctrl Pts',(1.26980990061511,5.950399530426,-1.56581983817613));
#3907=CARTESIAN_POINT('Ctrl Pts',(1.06147049699314,5.96308088767541,-1.71390324343442));
#3908=CARTESIAN_POINT('Ctrl Pts',(0.589774685924296,5.99059647665443,-1.929382466369));
#3909=CARTESIAN_POINT('Ctrl Pts',(0.329024203695872,6.00580692145109,-1.99049109052132));
#3910=CARTESIAN_POINT('Ctrl Pts',(-0.194257962683431,6.03633171448988,-2.00724376634386));
#3911=CARTESIAN_POINT('Ctrl Pts',(-0.451709422575361,6.05134971631691,-1.96538755078824));
#3912=CARTESIAN_POINT('Ctrl Pts',(-0.934962207318963,6.07953946209362,-1.78656451965216));
#3913=CARTESIAN_POINT('Ctrl Pts',(-1.15638485129736,6.09194407065691,-1.65189124887631));
#3914=CARTESIAN_POINT('Ctrl Pts',(-1.54263006545917,6.12097164144872,-1.30029314231204));
#3915=CARTESIAN_POINT('Ctrl Pts',(-1.70139491179651,6.13651387264503,-1.08429967942574));
#3916=CARTESIAN_POINT('Ctrl Pts',(-1.92109767821886,6.16677837403545,-0.612063369916115));
#3917=CARTESIAN_POINT('Ctrl Pts',(-1.98350264718633,6.18123453238429,-0.361935172777406));
#3918=CARTESIAN_POINT('Ctrl Pts',(-2.01132046858475,6.20832476822178,0.158251798944814));
#3919=CARTESIAN_POINT('Ctrl Pts',(-1.97259634046109,6.22219505710803,0.423526679365465));
#3920=CARTESIAN_POINT('Ctrl Pts',(-1.7948926351988,6.25247731484111,0.920362642571417));
#3921=CARTESIAN_POINT('Ctrl Pts',(-1.65895060736644,6.26791324593325,1.14742866950801));
#3922=CARTESIAN_POINT('Ctrl Pts',(-1.31315585809985,6.29730720024909,1.52963337576748));
#3923=CARTESIAN_POINT('Ctrl Pts',(-1.1091346462743,6.31030047896735,1.68342957030648));
#3924=CARTESIAN_POINT('Ctrl Pts',(-0.643837424469834,6.33744281690594,1.91201655428822));
#3925=CARTESIAN_POINT('Ctrl Pts',(-0.38494640051787,6.35254479330314,1.98043092804347));
#3926=CARTESIAN_POINT('Ctrl Pts',(-0.0801986050553553,6.37032174803845,
1.99879523621637));
#3927=CARTESIAN_POINT('Ctrl Pts',(-0.0400796075752101,6.37266202289145,
2.));
#3928=CARTESIAN_POINT('Ctrl Pts',(7.06522986662669E-16,6.37500000000001,
2.));
#3929=CARTESIAN_POINT('Ctrl Pts',(7.41933818794109E-16,6.46250000191184,
2.));
#3930=CARTESIAN_POINT('Ctrl Pts',(-0.0915607604235562,6.4571589575538,2.));
#3931=CARTESIAN_POINT('Ctrl Pts',(-0.183209202623249,6.45181279842548,1.9937126289666));
#3932=CARTESIAN_POINT('Ctrl Pts',(-0.536976989776565,6.43117634417487,1.94473142989058));
#3933=CARTESIAN_POINT('Ctrl Pts',(-0.789715492509543,6.41658655291459,1.856492941354));
#3934=CARTESIAN_POINT('Ctrl Pts',(-1.23682283738656,6.39019265575449,1.59216681994931));
#3935=CARTESIAN_POINT('Ctrl Pts',(-1.42908114885385,6.37599432609523,1.4221131695151));
#3936=CARTESIAN_POINT('Ctrl Pts',(-1.74555908957954,6.34601287342013,1.01135294443712));
#3937=CARTESIAN_POINT('Ctrl Pts',(-1.86376231924679,6.33048108973694,0.772148028373824));
#3938=CARTESIAN_POINT('Ctrl Pts',(-1.99910065587187,6.300977719091,0.266270373989555));
#3939=CARTESIAN_POINT('Ctrl Pts',(-2.01674596082411,6.28824391348039,0.00505734510263627));
#3940=CARTESIAN_POINT('Ctrl Pts',(-1.95156457334202,6.26044596836682,-0.5075667722337));
#3941=CARTESIAN_POINT('Ctrl Pts',(-1.8701369046458,6.24561266472461,-0.754177749248546));
#3942=CARTESIAN_POINT('Ctrl Pts',(-1.61336286469494,6.21500178306147,-1.21186750021966));
#3943=CARTESIAN_POINT('Ctrl Pts',(-1.43697083813152,6.19951511201499,-1.41658410011584));
#3944=CARTESIAN_POINT('Ctrl Pts',(-1.02477287316995,6.17134663556016,-1.73619272141809));
#3945=CARTESIAN_POINT('Ctrl Pts',(-0.796248904014463,6.15894785464601,-1.85216696661008));
#3946=CARTESIAN_POINT('Ctrl Pts',(-0.301840294904721,6.13010735244795,-1.99416116119649));
#3947=CARTESIAN_POINT('Ctrl Pts',(-0.0399698268648906,6.11483157514562,
-2.01647577831176));
#3948=CARTESIAN_POINT('Ctrl Pts',(0.482246501087751,6.08436895601506,-1.95900073504723));
#3949=CARTESIAN_POINT('Ctrl Pts',(0.737369936774645,6.06948675559999,-1.87791959018816));
#3950=CARTESIAN_POINT('Ctrl Pts',(1.19114008483323,6.04301683029658,-1.62650353527467));
#3951=CARTESIAN_POINT('Ctrl Pts',(1.38767659175461,6.02923991067642,-1.46245415041243));
#3952=CARTESIAN_POINT('Ctrl Pts',(1.71508941030679,5.99946084104511,-1.06201332529899));
#3953=CARTESIAN_POINT('Ctrl Pts',(1.83992077022183,5.98395276040648,-0.827104360618089));
#3954=CARTESIAN_POINT('Ctrl Pts',(1.99076641106456,5.95415471494468,-0.324346803895114));
#3955=CARTESIAN_POINT('Ctrl Pts',(2.01606600444625,5.94108482252657,-0.0616853330448833));
#3956=CARTESIAN_POINT('Ctrl Pts',(1.96466974215094,5.91354366508803,0.453814552315483));
#3957=CARTESIAN_POINT('Ctrl Pts',(1.89028497862779,5.89884136498054,0.701898555063765));
#3958=CARTESIAN_POINT('Ctrl Pts',(1.6471704709921,5.86833924208025,1.16532177551644));
#3959=CARTESIAN_POINT('Ctrl Pts',(1.47723680651845,5.85282115977933,1.3743888940881));
#3960=CARTESIAN_POINT('Ctrl Pts',(1.0745560612086,5.82432638399933,1.70595133625727));
#3961=CARTESIAN_POINT('Ctrl Pts',(0.848720261100305,5.81200868380936,1.82882984987381));
#3962=CARTESIAN_POINT('Ctrl Pts',(0.409621056617632,5.78639456354787,1.96840229651907));
#3963=CARTESIAN_POINT('Ctrl Pts',(0.205248527642598,5.77447283269099,2.));
#3964=CARTESIAN_POINT('Ctrl Pts',(2.28983498828939E-15,5.76250000191184,
2.));
#3965=CARTESIAN_POINT('Origin',(0.,70.,0.));
#3966=CARTESIAN_POINT('',(3.10331689486287E-14,4.97500000000001,2.));
#3967=CARTESIAN_POINT('',(-3.30631497031952E-16,5.06250000191184,2.));
#3968=CARTESIAN_POINT('',(-2.44929359829471E-16,70.,2.));
#3969=CARTESIAN_POINT('Ctrl Pts',(7.06522986662669E-16,4.97500000000001,
2.));
#3970=CARTESIAN_POINT('Ctrl Pts',(0.0362596285020658,4.97711514499596,2.));
#3971=CARTESIAN_POINT('Ctrl Pts',(0.0725542216904652,4.97923232959862,1.99901394277815));
#3972=CARTESIAN_POINT('Ctrl Pts',(0.364710195054145,4.99627476137817,1.98309063559847));
#3973=CARTESIAN_POINT('Ctrl Pts',(0.61556521188284,5.01090797069318,1.92009875767504));
#3974=CARTESIAN_POINT('Ctrl Pts',(1.08546753210051,5.03831893937254,1.7001948362507));
#3975=CARTESIAN_POINT('Ctrl Pts',(1.29899833487608,5.05159334250551,1.54322313517846));
#3976=CARTESIAN_POINT('Ctrl Pts',(1.65364486511862,5.08153556301639,1.15527615098086));
#3977=CARTESIAN_POINT('Ctrl Pts',(1.7910990033383,5.09702672449809,0.92798986320257));
#3978=CARTESIAN_POINT('Ctrl Pts',(1.96691498867721,5.12669588188906,0.442200263735244));
#3979=CARTESIAN_POINT('Ctrl Pts',(2.00705569561547,5.14021574498876,0.189604412736546));
#3980=CARTESIAN_POINT('Ctrl Pts',(1.99054196800901,5.16688173088232,-0.328711009630941));
#3981=CARTESIAN_POINT('Ctrl Pts',(1.92948015500898,5.18183108715165,-0.589377465160195));
#3982=CARTESIAN_POINT('Ctrl Pts',(1.71145619097226,5.21231906344031,-1.06700668742727));
#3983=CARTESIAN_POINT('Ctrl Pts',(1.55841129512922,5.22755387528183,-1.28021724022294));
#3984=CARTESIAN_POINT('Ctrl Pts',(1.18337201187085,5.25627821511708,-1.63228267774596));
#3985=CARTESIAN_POINT('Ctrl Pts',(0.96642767135054,5.26862505250456,-1.76938598269431));
#3986=CARTESIAN_POINT('Ctrl Pts',(0.480800266469448,5.29695331778929,-1.95964812161272));
#3987=CARTESIAN_POINT('Ctrl Pts',(0.215025294473574,5.31245685782238,-2.00627095256879));
#3988=CARTESIAN_POINT('Ctrl Pts',(-0.308876250480484,5.34301778127804,-1.99264086171038));
#3989=CARTESIAN_POINT('Ctrl Pts',(-0.562092181003058,5.35778871055852,-1.93651970495745));
#3990=CARTESIAN_POINT('Ctrl Pts',(-1.03650185539069,5.38546260823113,-1.73015564751182));
#3991=CARTESIAN_POINT('Ctrl Pts',(-1.25264836203467,5.39834736740584,-1.58071660922677));
#3992=CARTESIAN_POINT('Ctrl Pts',(-1.61804096069133,5.42799478922013,-1.20480937132668));
#3993=CARTESIAN_POINT('Ctrl Pts',(-1.76269945501799,5.44351674674541,-0.981072916918595));
#3994=CARTESIAN_POINT('Ctrl Pts',(-1.95324518871418,5.47340670783459,-0.499416761929923));
#3995=CARTESIAN_POINT('Ctrl Pts',(-2.000799555136,5.48747150510802,-0.247538258858837));
#3996=CARTESIAN_POINT('Ctrl Pts',(-1.9991444128466,5.51373996717858,0.271486840785107));
#3997=CARTESIAN_POINT('Ctrl Pts',(-1.94559635272304,5.52855066299585,0.53374659844057));
#3998=CARTESIAN_POINT('Ctrl Pts',(-1.74112500106917,5.55898103606433,1.01806017706896));
#3999=CARTESIAN_POINT('Ctrl Pts',(-1.59373661025392,5.5742955484624,1.23611417643179));
#4000=CARTESIAN_POINT('Ctrl Pts',(-1.22853150879851,5.60325276527767,1.59846715016656));
#4001=CARTESIAN_POINT('Ctrl Pts',(-1.01608589317159,5.61572832289833,1.74124724903627));
#4002=CARTESIAN_POINT('Ctrl Pts',(-0.53600079059646,5.64373328721522,1.94538128070972));
#4003=CARTESIAN_POINT('Ctrl Pts',(-0.270859636694515,5.65919985452616,1.99960110895732));
#4004=CARTESIAN_POINT('Ctrl Pts',(-0.00197433811420763,5.67488483027668,
1.99999926914862));
#4005=CARTESIAN_POINT('Ctrl Pts',(-0.000987151723183884,5.67494241614949,
2.));
#4006=CARTESIAN_POINT('Ctrl Pts',(7.0652298666267E-16,5.67500000000001,
2.));
#4007=CARTESIAN_POINT('Ctrl Pts',(7.41933818794109E-16,5.76250000191184,
2.));
#4008=CARTESIAN_POINT('Ctrl Pts',(-0.0535565212988742,5.75937587150274,
2.));
#4009=CARTESIAN_POINT('Ctrl Pts',(-0.107172686776816,5.75624826184986,1.99784881882323));
#4010=CARTESIAN_POINT('Ctrl Pts',(-0.424952970807837,5.73771107861472,1.97222923346625));
#4011=CARTESIAN_POINT('Ctrl Pts',(-0.682377513849286,5.7226946469373,1.89859966741249));
#4012=CARTESIAN_POINT('Ctrl Pts',(-1.14299744186195,5.69582515113657,1.66063450329597));
#4013=CARTESIAN_POINT('Ctrl Pts',(-1.34393980807102,5.68254748379355,1.50267567444916));
#4014=CARTESIAN_POINT('Ctrl Pts',(-1.68230444135283,5.65299448637494,1.11303295175884));
#4015=CARTESIAN_POINT('Ctrl Pts',(-1.81378229442771,5.63752446314882,0.882714683088012));
#4016=CARTESIAN_POINT('Ctrl Pts',(-1.98055406188004,5.6074351644053,0.383386760058109));
#4017=CARTESIAN_POINT('Ctrl Pts',(-2.01378555634754,5.59392326899395,0.119188618895204));
#4018=CARTESIAN_POINT('Ctrl Pts',(-1.97641370238146,5.56664853380106,-0.399134469638205));
#4019=CARTESIAN_POINT('Ctrl Pts',(-1.90916731049059,5.55208939285681,-0.648505996663667));
#4020=CARTESIAN_POINT('Ctrl Pts',(-1.67997638436286,5.52172093793137,-1.11732206094771));
#4021=CARTESIAN_POINT('Ctrl Pts',(-1.51667023686694,5.50618405975824,-1.33058764000911));
#4022=CARTESIAN_POINT('Ctrl Pts',(-1.12374216379702,5.47736857298723,-1.67412922133258));
#4023=CARTESIAN_POINT('Ctrl Pts',(-0.900553375234095,5.46503228213383,-1.80402555433781));
#4024=CARTESIAN_POINT('Ctrl Pts',(-0.414442565133177,5.43667581821127,-1.97364496289496));
#4025=CARTESIAN_POINT('Ctrl Pts',(-0.155750888780536,5.42158547042404,-2.01066050345587));
#4026=CARTESIAN_POINT('Ctrl Pts',(0.367563861501855,5.39105877665756,-1.98373238228265));
#4027=CARTESIAN_POINT('Ctrl Pts',(0.627056522500649,5.37592170476597,-1.91758693942038));
#4028=CARTESIAN_POINT('Ctrl Pts',(1.09435980158698,5.34866234681927,-1.69307362107187));
#4029=CARTESIAN_POINT('Ctrl Pts',(1.29972095426504,5.33577658468415,-1.54106552793296));
#4030=CARTESIAN_POINT('Ctrl Pts',(1.64869242831578,5.30645201211671,-1.16206830702074));
#4031=CARTESIAN_POINT('Ctrl Pts',(1.78653036949275,5.29103273007053,-0.936426451804174));
#4032=CARTESIAN_POINT('Ctrl Pts',(1.96893851738666,5.26066923556934,-0.440698528848537));
#4033=CARTESIAN_POINT('Ctrl Pts',(2.0100395236924,5.24663127996597,-0.174956107182668));
#4034=CARTESIAN_POINT('Ctrl Pts',(1.98631606581007,5.21962086016237,0.346014798692541));
#4035=CARTESIAN_POINT('Ctrl Pts',(1.92597945494549,5.20521014024438,0.596437715271993));
#4036=CARTESIAN_POINT('Ctrl Pts',(1.71034122468579,5.17499330673269,1.07007710653928));
#4037=CARTESIAN_POINT('Ctrl Pts',(1.55352787914582,5.15945059907308,1.28720670046375));
#4038=CARTESIAN_POINT('Ctrl Pts',(1.17015730592201,5.13033381134792,1.64223051902134));
#4039=CARTESIAN_POINT('Ctrl Pts',(0.949481719457653,5.11788643554687,1.77895158304812));
#4040=CARTESIAN_POINT('Ctrl Pts',(0.482289331210749,5.09063354623247,1.95605222622256));
#4041=CARTESIAN_POINT('Ctrl Pts',(0.242062470307809,5.0766203126798,2.));
#4042=CARTESIAN_POINT('Ctrl Pts',(1.8249290967276E-14,5.06250000191184,
2.));
#4043=CARTESIAN_POINT('Origin',(0.,70.,0.));
#4044=CARTESIAN_POINT('',(3.07729604272322E-14,4.27500000000001,2.));
#4045=CARTESIAN_POINT('',(-9.5940548587481E-15,4.36250000191184,2.));
#4046=CARTESIAN_POINT('',(-2.44929359829471E-16,70.,2.));
#4047=CARTESIAN_POINT('Ctrl Pts',(7.0652298666267E-16,4.27500000000001,
2.));
#4048=CARTESIAN_POINT('Ctrl Pts',(0.0660280436593563,4.27885163588014,2.));
#4049=CARTESIAN_POINT('Ctrl Pts',(0.132131846816979,4.28270769106434,1.99673030440369));
#4050=CARTESIAN_POINT('Ctrl Pts',(0.461823825134132,4.30193972313284,1.96391816789203));
#4051=CARTESIAN_POINT('Ctrl Pts',(0.717794879749972,4.31687136798543,1.88549083015052));
#4052=CARTESIAN_POINT('Ctrl Pts',(1.17402763380875,4.34348494530552,1.6388735121033));
#4053=CARTESIAN_POINT('Ctrl Pts',(1.37213504547016,4.35707126239266,1.47701394256362));
#4054=CARTESIAN_POINT('Ctrl Pts',(1.70349591608626,4.38676999221564,1.08044284214248));
#4055=CARTESIAN_POINT('Ctrl Pts',(1.8307315019229,4.40226600685819,0.847160802724497));
#4056=CARTESIAN_POINT('Ctrl Pts',(1.98729226136375,4.43216992419419,0.345607151660183));
#4057=CARTESIAN_POINT('Ctrl Pts',(2.01542930392403,4.44538731856774,0.0823992975103338));
#4058=CARTESIAN_POINT('Ctrl Pts',(1.96829235486285,4.47330001037226,-0.442914176380998));
#4059=CARTESIAN_POINT('Ctrl Pts',(1.8922780240453,4.48848985463503,-0.699708217371228));
#4060=CARTESIAN_POINT('Ctrl Pts',(1.64767567224347,4.51901639054792,-1.16275568291626));
#4061=CARTESIAN_POINT('Ctrl Pts',(1.48372605197918,4.53405583238078,-1.3658030669174));
#4062=CARTESIAN_POINT('Ctrl Pts',(1.08912209056416,4.56229404554539,-1.69695001975465));
#4063=CARTESIAN_POINT('Ctrl Pts',(0.862727582973985,4.57467422432653,-1.82250652223345));
#4064=CARTESIAN_POINT('Ctrl Pts',(0.366158831456928,4.60364073483169,-1.98405622766587));
#4065=CARTESIAN_POINT('Ctrl Pts',(0.0997367074387389,4.61918202539941,-2.01508899181099));
#4066=CARTESIAN_POINT('Ctrl Pts',(-0.419619216201984,4.64947778761179,-1.97211248715117));
#4067=CARTESIAN_POINT('Ctrl Pts',(-0.667959623064703,4.66396431134545,-1.9024140392818));
#4068=CARTESIAN_POINT('Ctrl Pts',(-1.13328695123016,4.69110840548844,-1.66908381206157));
#4069=CARTESIAN_POINT('Ctrl Pts',(-1.34418864430199,4.70486981007299,-1.50445653481907));
#4070=CARTESIAN_POINT('Ctrl Pts',(-1.68783946026691,4.73509648447215,-1.10453044531571));
#4071=CARTESIAN_POINT('Ctrl Pts',(-1.81798635539873,4.75054300699671,-0.873908940965106));
#4072=CARTESIAN_POINT('Ctrl Pts',(-1.97904354795584,4.77998358540772,-0.384123038876249));
#4073=CARTESIAN_POINT('Ctrl Pts',(-2.01172361530772,4.79305470316162,-0.130712590377672));
#4074=CARTESIAN_POINT('Ctrl Pts',(-1.98009257935505,4.82011772909884,0.38673420455541));
#4075=CARTESIAN_POINT('Ctrl Pts',(-1.91142647080755,4.83519536864651,0.64554966835597));
#4076=CARTESIAN_POINT('Ctrl Pts',(-1.67982007339063,4.86571576749315,1.11597886925722));
#4077=CARTESIAN_POINT('Ctrl Pts',(-1.52117051331359,4.88085741078071,1.32410930857298));
#4078=CARTESIAN_POINT('Ctrl Pts',(-1.13618802742279,4.90933838299361,1.66561660581584));
#4079=CARTESIAN_POINT('Ctrl Pts',(-0.914523747015572,4.9216527814241,1.79689914786514));
#4080=CARTESIAN_POINT('Ctrl Pts',(-0.457540602005686,4.94831013154968,1.96050414645654));
#4081=CARTESIAN_POINT('Ctrl Pts',(-0.2294704759585,4.96161422223576,2.));
#4082=CARTESIAN_POINT('Ctrl Pts',(-1.26981758441502E-14,4.97500000000001,
2.));
#4083=CARTESIAN_POINT('Ctrl Pts',(7.41933818794109E-16,5.06250000191184,
2.));
#4084=CARTESIAN_POINT('Ctrl Pts',(-0.0158442249904296,5.06157575545407,
2.));
#4085=CARTESIAN_POINT('Ctrl Pts',(-0.0316963144127123,5.06065105023777,
1.99981172099515));
#4086=CARTESIAN_POINT('Ctrl Pts',(-0.312652205616501,5.04426195658421,1.9931296883174));
#4087=CARTESIAN_POINT('Ctrl Pts',(-0.573905474679356,5.02902218255555,1.93416331683831));
#4088=CARTESIAN_POINT('Ctrl Pts',(-1.04744463333177,5.00139906496749,1.72252415915947));
#4089=CARTESIAN_POINT('Ctrl Pts',(-1.25705308625539,4.98879057716396,1.57609280123643));
#4090=CARTESIAN_POINT('Ctrl Pts',(-1.61586906011901,4.95968623431236,1.20713872273769));
#4091=CARTESIAN_POINT('Ctrl Pts',(-1.75952803750774,4.94432653048774,0.986036987279413));
#4092=CARTESIAN_POINT('Ctrl Pts',(-1.95522856438524,4.9139338069324,0.497404837687051));
#4093=CARTESIAN_POINT('Ctrl Pts',(-2.00384801559129,4.89944067328008,0.234142341287129));
#4094=CARTESIAN_POINT('Ctrl Pts',(-1.99567467843145,4.87242379832758,-0.295934209782576));
#4095=CARTESIAN_POINT('Ctrl Pts',(-1.93891490850734,4.8575523994666,-0.55754129455507));
#4096=CARTESIAN_POINT('Ctrl Pts',(-1.72863461118595,4.82709432180272,-1.0390494856024));
#4097=CARTESIAN_POINT('Ctrl Pts',(-1.57881402037006,4.81181238639888,-1.25505439639258));
#4098=CARTESIAN_POINT('Ctrl Pts',(-1.20940297661085,4.78295381636324,-1.61302636838513));
#4099=CARTESIAN_POINT('Ctrl Pts',(-0.995053317087455,4.77054477874194,-1.75338750766115));
#4100=CARTESIAN_POINT('Ctrl Pts',(-0.512595717979786,4.74240141879399,-1.95163357121211));
#4101=CARTESIAN_POINT('Ctrl Pts',(-0.247159709890235,4.72691765165544,-2.00262490886725));
#4102=CARTESIAN_POINT('Ctrl Pts',(0.277723269735549,4.69629947784393,-1.99727141138786));
#4103=CARTESIAN_POINT('Ctrl Pts',(0.532171369632447,4.68145667201661,-1.94500612820907));
#4104=CARTESIAN_POINT('Ctrl Pts',(1.00903693678815,4.65363951393253,-1.74615634794997));
#4105=CARTESIAN_POINT('Ctrl Pts',(1.22662568191518,4.64092713874215,-1.60081848208624));
#4106=CARTESIAN_POINT('Ctrl Pts',(1.59783861761927,4.61144636305487,-1.23157035516275));
#4107=CARTESIAN_POINT('Ctrl Pts',(1.74642054344869,4.59591333276462,-1.00987991108583));
#4108=CARTESIAN_POINT('Ctrl Pts',(1.94499629944206,4.56591677140326,-0.53074975348895));
#4109=CARTESIAN_POINT('Ctrl Pts',(1.99668628473844,4.55170530119424,-0.279278826673935));
#4110=CARTESIAN_POINT('Ctrl Pts',(2.00313609598665,4.52527705508717,0.240140973207252));
#4111=CARTESIAN_POINT('Ctrl Pts',(1.95373188159054,4.51072735281215,0.50324810074014));
#4112=CARTESIAN_POINT('Ctrl Pts',(1.756603634623,4.48032647258704,0.991217415942218));
#4113=CARTESIAN_POINT('Ctrl Pts',(1.61233983702273,4.46497371538134,1.21183245089532));
#4114=CARTESIAN_POINT('Ctrl Pts',(1.25249235733571,4.43589290269783,1.5797252126963));
#4115=CARTESIAN_POINT('Ctrl Pts',(1.04243026343621,4.42330843394563,1.72556888955745));
#4116=CARTESIAN_POINT('Ctrl Pts',(0.568236339304095,4.39564712170459,1.9358368161416));
#4117=CARTESIAN_POINT('Ctrl Pts',(0.306808131447931,4.38039714291298,1.99403813371026));
#4118=CARTESIAN_POINT('Ctrl Pts',(0.0277872371021949,4.36412092407614,1.99985528997697));
#4119=CARTESIAN_POINT('Ctrl Pts',(0.0138905427157841,4.36331028357026,2.));
#4120=CARTESIAN_POINT('Ctrl Pts',(7.41933818794109E-16,4.36250000191184,
2.));
#4121=CARTESIAN_POINT('Origin',(0.,70.,0.));
#4122=CARTESIAN_POINT('',(2.19171970823706E-14,3.57500000000001,2.));
#4123=CARTESIAN_POINT('',(-1.89095199247436E-14,3.66250000191184,2.));
#4124=CARTESIAN_POINT('',(-2.44929359829471E-16,70.,2.));
#4125=CARTESIAN_POINT('Ctrl Pts',(-4.64905891561784E-15,3.57500000000001,
2.));
#4126=CARTESIAN_POINT('Ctrl Pts',(0.10288782586422,3.58100178984209,2.));
#4127=CARTESIAN_POINT('Ctrl Pts',(0.205854153830501,3.58700815897345,1.99206073891009));
#4128=CARTESIAN_POINT('Ctrl Pts',(0.57260818517212,3.60840214413505,1.93490351158503));
#4129=CARTESIAN_POINT('Ctrl Pts',(0.826191600282839,3.62276308212701,1.84093919135471));
#4130=CARTESIAN_POINT('Ctrl Pts',(1.27039250159657,3.64962865702265,1.56559823623058));
#4131=CARTESIAN_POINT('Ctrl Pts',(1.4593745191971,3.66395565023105,1.3911061388883));
#4132=CARTESIAN_POINT('Ctrl Pts',(1.76750162445167,3.69408203946287,0.972655556930503));
#4133=CARTESIAN_POINT('Ctrl Pts',(1.88062319441531,3.70962289434875,0.730337180024206));
#4134=CARTESIAN_POINT('Ctrl Pts',(2.00429943040821,3.73889776006813,0.222249633187286));
#4135=CARTESIAN_POINT('Ctrl Pts',(2.01622565796333,3.75144201407525,-0.0379123639191237));
#4136=CARTESIAN_POINT('Ctrl Pts',(1.94058731459248,3.77943137644466,-0.548288233958856));
#4137=CARTESIAN_POINT('Ctrl Pts',(1.85380691481358,3.79435735942738,-0.793643385403029));
#4138=CARTESIAN_POINT('Ctrl Pts',(1.58818698640604,3.82486498480195,-1.24418201585821));
#4139=CARTESIAN_POINT('Ctrl Pts',(1.40938613254919,3.84015444861909,-1.44360418791558));
#4140=CARTESIAN_POINT('Ctrl Pts',(0.993648361474997,3.86796776492616,-1.75413875354027));
#4141=CARTESIAN_POINT('Ctrl Pts',(0.763432480597549,3.88046643863182,-1.86588484710983));
#4142=CARTESIAN_POINT('Ctrl Pts',(0.266522971048555,3.90945282668884,-1.99924678864832));
#4143=CARTESIAN_POINT('Ctrl Pts',(0.00382923850926156,3.92477662775364,
-2.01692743821058));
#4144=CARTESIAN_POINT('Ctrl Pts',(-0.517842312609391,3.95520746823556,-1.94991132167082));
#4145=CARTESIAN_POINT('Ctrl Pts',(-0.771408032450691,3.96999176339004,-1.86416776779294));
#4146=CARTESIAN_POINT('Ctrl Pts',(-1.22084519606734,3.9962227458683,-1.60441164222163));
#4147=CARTESIAN_POINT('Ctrl Pts',(-1.41460864884182,4.01035849540025,-1.43646575078409));
#4148=CARTESIAN_POINT('Ctrl Pts',(-1.73494915944347,4.04026710313756,-1.02937753727333));
#4149=CARTESIAN_POINT('Ctrl Pts',(-1.85551383526763,4.05579201768493,-0.791671976409806));
#4150=CARTESIAN_POINT('Ctrl Pts',(-1.99633687991085,4.08540082780284,-0.286873759418399));
#4151=CARTESIAN_POINT('Ctrl Pts',(-2.01668239103348,4.09824266680982,-0.0251545927172321));
#4152=CARTESIAN_POINT('Ctrl Pts',(-1.95639182414602,4.12595008392364,0.488501251547938));
#4153=CARTESIAN_POINT('Ctrl Pts',(-1.87746515861466,4.1407380396657,0.735658527789376));
#4154=CARTESIAN_POINT('Ctrl Pts',(-1.62553284661629,4.17131294748868,1.19543155433835));
#4155=CARTESIAN_POINT('Ctrl Pts',(-1.45142503291765,4.18681224680635,1.40171692008769));
#4156=CARTESIAN_POINT('Ctrl Pts',(-1.04259593990855,4.21509773737192,1.72558683920426));
#4157=CARTESIAN_POINT('Ctrl Pts',(-0.815036462771399,4.22745620633834,1.84401178999322));
#4158=CARTESIAN_POINT('Ctrl Pts',(-0.385591264380167,4.2525071762445,1.9720265737401));
#4159=CARTESIAN_POINT('Ctrl Pts',(-0.193119675665181,4.26373468558621,2.));
#4160=CARTESIAN_POINT('Ctrl Pts',(4.78783679369599E-15,4.27500000000001,
2.));
#4161=CARTESIAN_POINT('Ctrl Pts',(-9.71445146547012E-16,4.36250000191184,
2.00000000000001));
#4162=CARTESIAN_POINT('Ctrl Pts',(-0.243975293587871,4.34826810978588,2.00000000000001));
#4163=CARTESIAN_POINT('Ctrl Pts',(-0.486052805080953,4.33414692161546,1.95535511648689));
#4164=CARTESIAN_POINT('Ctrl Pts',(-0.954650468971208,4.30681205788853,1.77620586455412));
#4165=CARTESIAN_POINT('Ctrl Pts',(-1.17505972947074,4.29434742704428,1.63875101545638));
#4166=CARTESIAN_POINT('Ctrl Pts',(-1.55739883696697,4.26519892138022,1.28250382752127));
#4167=CARTESIAN_POINT('Ctrl Pts',(-1.71351233898587,4.24965630570933,1.06497199965594));
#4168=CARTESIAN_POINT('Ctrl Pts',(-1.92769479020271,4.21945699872622,0.590839049257593));
#4169=CARTESIAN_POINT('Ctrl Pts',(-1.98729139697089,4.20506274456764,0.340314828621115));
#4170=CARTESIAN_POINT('Ctrl Pts',(-2.00954797662932,4.17808103015945,-0.180934760325271));
#4171=CARTESIAN_POINT('Ctrl Pts',(-1.9675919825813,4.16398096231088,-0.446845468523272));
#4172=CARTESIAN_POINT('Ctrl Pts',(-1.7834956004059,4.13358858419427,-0.942170436269723));
#4173=CARTESIAN_POINT('Ctrl Pts',(-1.6449810345462,4.11817556531004,-1.16729766358963));
#4174=CARTESIAN_POINT('Ctrl Pts',(-1.29487251259413,4.08887602700756,-1.54514285966028));
#4175=CARTESIAN_POINT('Ctrl Pts',(-1.08902820576111,4.07602664724791,-1.69650964028479));
#4176=CARTESIAN_POINT('Ctrl Pts',(-0.621006080495942,4.04872535660744,-1.91955540343306));
#4177=CARTESIAN_POINT('Ctrl Pts',(-0.361301926763335,4.03357594763971,-1.98488304645561));
#4178=CARTESIAN_POINT('Ctrl Pts',(0.162021093548409,4.00304877145485,-2.01015480855732));
#4179=CARTESIAN_POINT('Ctrl Pts',(0.420517058828189,3.98796984014687,-1.97234939629171));
#4180=CARTESIAN_POINT('Ctrl Pts',(0.906166143150877,3.95964031022804,-1.80123236434251));
#4181=CARTESIAN_POINT('Ctrl Pts',(1.12906709225369,3.94729600477414,-1.67056385612915));
#4182=CARTESIAN_POINT('Ctrl Pts',(1.52091712445733,3.91844586292025,-1.32571387488676));
#4183=CARTESIAN_POINT('Ctrl Pts',(1.68349038929167,3.90290771385181,-1.1120000086205));
#4184=CARTESIAN_POINT('Ctrl Pts',(1.91114725778974,3.87255536647302,-0.64261710248446));
#4185=CARTESIAN_POINT('Ctrl Pts',(1.97760963120897,3.85801258071494,-0.393116670908036));
#4186=CARTESIAN_POINT('Ctrl Pts',(2.01343691144459,3.83076750771852,0.125511018469023));
#4187=CARTESIAN_POINT('Ctrl Pts',(1.97932244832764,3.81720080245072,0.389881750771629));
#4188=CARTESIAN_POINT('Ctrl Pts',(1.81078776901429,3.78707999692248,0.88881552875744));
#4189=CARTESIAN_POINT('Ctrl Pts',(1.67858452272334,3.77161503396507,1.11861482411685));
#4190=CARTESIAN_POINT('Ctrl Pts',(1.33901702364243,3.74208747590405,1.50705950322995));
#4191=CARTESIAN_POINT('Ctrl Pts',(1.13758132292479,3.72885891241579,1.66434621300729));
#4192=CARTESIAN_POINT('Ctrl Pts',(0.676205697517938,3.70194533426706,1.90080719990041));
#4193=CARTESIAN_POINT('Ctrl Pts',(0.418538303422225,3.68691473627814,1.97360121051258));
#4194=CARTESIAN_POINT('Ctrl Pts',(0.10284044210722,3.66849902770143,1.99801918799822));
#4195=CARTESIAN_POINT('Ctrl Pts',(0.051391973731045,3.66549786704615,2.));
#4196=CARTESIAN_POINT('Ctrl Pts',(7.41933818794109E-16,3.66250000191184,
2.));
#4197=CARTESIAN_POINT('Origin',(0.,70.,0.));
#4198=CARTESIAN_POINT('',(1.66219536719514E-14,2.87500000000001,2.));
#4199=CARTESIAN_POINT('',(2.61585959811339E-14,2.96250000191184,2.));
#4200=CARTESIAN_POINT('',(-2.44929359829471E-16,70.,2.));
#4201=CARTESIAN_POINT('Ctrl Pts',(-2.67147415300428E-15,2.87500000000001,
2.));
#4202=CARTESIAN_POINT('Ctrl Pts',(0.142854417545159,2.88333317435681,2.));
#4203=CARTESIAN_POINT('Ctrl Pts',(0.285642418419913,2.89166247440784,1.98469424875995));
#4204=CARTESIAN_POINT('Ctrl Pts',(0.682597198502697,2.91481816991267,1.89818103146292));
#4205=CARTESIAN_POINT('Ctrl Pts',(0.925716172957715,2.92812717302022,1.79221826774021));
#4206=CARTESIAN_POINT('Ctrl Pts',(1.35184472923469,2.9555174173453,1.49605747809885));
#4207=CARTESIAN_POINT('Ctrl Pts',(1.53218851063789,2.97013947289794,1.31073737308708));
#4208=CARTESIAN_POINT('Ctrl Pts',(1.81863070732071,3.00056835732941,0.873779151272685));
#4209=CARTESIAN_POINT('Ctrl Pts',(1.91869602817475,3.01609874159016,0.6241300100535));
#4210=CARTESIAN_POINT('Ctrl Pts',(2.01318760980476,3.04477733779127,0.110995770600117));
#4211=CARTESIAN_POINT('Ctrl Pts',(2.01090097070637,3.05709343668879,-0.14670730974588));
#4212=CARTESIAN_POINT('Ctrl Pts',(1.90872769732121,3.08555539239449,-0.651118152739248));
#4213=CARTESIAN_POINT('Ctrl Pts',(1.80836309406561,3.10068935707265,-0.892747430518395));
#4214=CARTESIAN_POINT('Ctrl Pts',(1.51777575078367,3.13121115556886,-1.32915167232376));
#4215=CARTESIAN_POINT('Ctrl Pts',(1.32839168621177,3.14629813498382,-1.51845547314241));
#4216=CARTESIAN_POINT('Ctrl Pts',(0.896730869869025,3.17339142956617,-1.80554413046886));
#4217=CARTESIAN_POINT('Ctrl Pts',(0.661159371273239,3.18643237000908,-1.90447594325186));
#4218=CARTESIAN_POINT('Ctrl Pts',(0.156768122434926,3.21585519285798,-2.0110156257623));
#4219=CARTESIAN_POINT('Ctrl Pts',(-0.107961243487111,3.23129773920343,-2.01422501025046));
#4220=CARTESIAN_POINT('Ctrl Pts',(-0.626497303349286,3.26154567602872,-1.91776934607945));
#4221=CARTESIAN_POINT('Ctrl Pts',(-0.874929158688982,3.27534818132766,-1.81790614058459));
#4222=CARTESIAN_POINT('Ctrl Pts',(-1.31037026177602,3.30247174333069,-1.53240089327968));
#4223=CARTESIAN_POINT('Ctrl Pts',(-1.49523945497418,3.31694671969792,-1.35260494880721));
#4224=CARTESIAN_POINT('Ctrl Pts',(-1.79298548980222,3.34723065175449,-0.925042313880283));
#4225=CARTESIAN_POINT('Ctrl Pts',(-1.89983272617656,3.36277236045616,-0.679084547617561));
#4226=CARTESIAN_POINT('Ctrl Pts',(-2.00935353942889,3.39176223073334,-0.168465810346163));
#4227=CARTESIAN_POINT('Ctrl Pts',(-2.01437192448993,3.40415129531614,0.0904719705272669));
#4228=CARTESIAN_POINT('Ctrl Pts',(-1.92593105442421,3.43237101196896,0.598016130591884));
#4229=CARTESIAN_POINT('Ctrl Pts',(-1.83259363071763,3.44740231043446,0.841670288414954));
#4230=CARTESIAN_POINT('Ctrl Pts',(-1.55486165485373,3.47792829465682,1.2855794359492));
#4231=CARTESIAN_POINT('Ctrl Pts',(-1.37089308146782,3.49312607037783,1.48020307013478));
#4232=CARTESIAN_POINT('Ctrl Pts',(-0.947425565242967,3.5205961769955,1.77948107537659));
#4233=CARTESIAN_POINT('Ctrl Pts',(-0.714674206606716,3.53331067128129,1.88505586375424));
#4234=CARTESIAN_POINT('Ctrl Pts',(-0.314624656407887,3.55664689504289,1.98141733522263));
#4235=CARTESIAN_POINT('Ctrl Pts',(-0.15740419443768,3.56581808865781,2.));
#4236=CARTESIAN_POINT('Ctrl Pts',(1.38777878078145E-15,3.57500000000001,
2.));
#4237=CARTESIAN_POINT('Ctrl Pts',(1.62717062046625E-14,3.66250000191184,
2.));
#4238=CARTESIAN_POINT('Ctrl Pts',(-0.207355900358025,3.65040424105762,2.));
#4239=CARTESIAN_POINT('Ctrl Pts',(-0.413792093728005,3.63836212977771,1.96775009577714));
#4240=CARTESIAN_POINT('Ctrl Pts',(-0.854549734069061,3.61265126742448,1.82612830148329));
#4241=CARTESIAN_POINT('Ctrl Pts',(-1.08008775545534,3.60033644823094,1.70247079478363));
#4242=CARTESIAN_POINT('Ctrl Pts',(-1.4816897339598,3.57180552160872,1.36956992521774));
#4243=CARTESIAN_POINT('Ctrl Pts',(-1.65089053657749,3.55628470367144,1.1600255371002));
#4244=CARTESIAN_POINT('Ctrl Pts',(-1.89246080795477,3.52579628244731,0.695981974276634));
#4245=CARTESIAN_POINT('Ctrl Pts',(-1.9660518643494,3.51110938596556,0.44774463721724));
#4246=CARTESIAN_POINT('Ctrl Pts',(-2.0158918157091,3.48359753615755,-0.0680736440507168));
#4247=CARTESIAN_POINT('Ctrl Pts',(-1.98971941010455,3.47048355845382,-0.330902723038247));
#4248=CARTESIAN_POINT('Ctrl Pts',(-1.83711373268955,3.44065274920631,-0.833292676932479));
#4249=CARTESIAN_POINT('Ctrl Pts',(-1.71153971309772,3.42514819400045,-1.06770308137849));
#4250=CARTESIAN_POINT('Ctrl Pts',(-1.38290885522477,3.39539377052543,-1.46695280379187));
#4251=CARTESIAN_POINT('Ctrl Pts',(-1.18588972314158,3.38167690242843,-1.63032726093278));
#4252=CARTESIAN_POINT('Ctrl Pts',(-0.731360668453417,3.35516270757162,-1.88026878965662));
#4253=CARTESIAN_POINT('Ctrl Pts',(-0.475973639380006,3.34026513087567,-1.96053509495005));
#4254=CARTESIAN_POINT('Ctrl Pts',(0.0463498516951409,3.30979626056296,-2.01632879391251));
#4255=CARTESIAN_POINT('Ctrl Pts',(0.30806663221086,3.29452944836621,-1.99319836390888));
#4256=CARTESIAN_POINT('Ctrl Pts',(0.802029459668345,3.26571495009785,-1.84968137667425));
#4257=CARTESIAN_POINT('Ctrl Pts',(1.03025639010877,3.25332989512491,-1.7329555238452));
#4258=CARTESIAN_POINT('Ctrl Pts',(1.44142228330395,3.22512539488095,-1.41203794953861));
#4259=CARTESIAN_POINT('Ctrl Pts',(1.61711480830446,3.20963467736261,-1.20683739285706));
#4260=CARTESIAN_POINT('Ctrl Pts',(1.87240490201655,3.17903451791594,-0.74850312996786));
#4261=CARTESIAN_POINT('Ctrl Pts',(1.95306549537904,3.16421498493323,-0.501721870167323));
#4262=CARTESIAN_POINT('Ctrl Pts',(2.01674725741211,3.13644472993755,0.0112199341423071));
#4263=CARTESIAN_POINT('Ctrl Pts',(1.9982757761014,3.12367911104514,0.272587206719206));
#4264=CARTESIAN_POINT('Ctrl Pts',(1.86125774248558,3.09414330988512,0.7781370452862));
#4265=CARTESIAN_POINT('Ctrl Pts',(1.74232935182834,3.07861345336577,1.0168851415062));
#4266=CARTESIAN_POINT('Ctrl Pts',(1.42466403861883,3.04865399292359,1.42652450344923));
#4267=CARTESIAN_POINT('Ctrl Pts',(1.23194233115013,3.0344746889772,1.59593400063326));
#4268=CARTESIAN_POINT('Ctrl Pts',(0.784116556100397,3.00813043731828,1.85886261012239));
#4269=CARTESIAN_POINT('Ctrl Pts',(0.531122256623746,2.99348213354822,1.94633773788873));
#4270=CARTESIAN_POINT('Ctrl Pts',(0.179209454759298,2.9729538867728,1.99398432590961));
#4271=CARTESIAN_POINT('Ctrl Pts',(0.0895606200734576,2.96772437141612,2.));
#4272=CARTESIAN_POINT('Ctrl Pts',(7.41933818794109E-16,2.96250000191184,
2.));
#4273=CARTESIAN_POINT('Origin',(0.,70.,0.));
#4274=CARTESIAN_POINT('',(2.71387147450608E-14,2.17500000000001,2.));
#4275=CARTESIAN_POINT('',(2.37375725299738E-14,2.26250000191184,2.));
#4276=CARTESIAN_POINT('',(-2.44929359829471E-16,70.,2.));
#4277=CARTESIAN_POINT('Ctrl Pts',(1.35655375821386E-14,2.17500000000001,
2.));
#4278=CARTESIAN_POINT('Ctrl Pts',(0.182979636269589,2.18567381211573,2.));
#4279=CARTESIAN_POINT('Ctrl Pts',(0.365491336649497,2.19632032797123,1.97488723208934));
#4280=CARTESIAN_POINT('Ctrl Pts',(0.791337489295804,2.22116135354227,1.85491186723268));
#4281=CARTESIAN_POINT('Ctrl Pts',(1.02430206525457,2.23378427945719,1.73715519322295));
#4282=CARTESIAN_POINT('Ctrl Pts',(1.43173051123552,2.26168749328194,1.42004372716924));
#4283=CARTESIAN_POINT('Ctrl Pts',(1.60253840374314,2.27657231975359,1.22401655890837));
#4284=CARTESIAN_POINT('Ctrl Pts',(1.86551616881027,2.3072216491371,0.769147462816087));
#4285=CARTESIAN_POINT('Ctrl Pts',(1.95165471009802,2.32269142931126,0.512657341461188));
#4286=CARTESIAN_POINT('Ctrl Pts',(2.01602776099352,2.35072106227596,-0.00501969927426783));
#4287=CARTESIAN_POINT('Ctrl Pts',(1.99914036922866,2.36318353242911,-0.26046995469053));
#4288=CARTESIAN_POINT('Ctrl Pts',(1.86898493410317,2.3921232774136,-0.758183063998182));
#4289=CARTESIAN_POINT('Ctrl Pts',(1.7543702215466,2.40743215030844,-0.995047322113318));
#4290=CARTESIAN_POINT('Ctrl Pts',(1.43812396380874,2.43786779255932,-1.4149319313869));
#4291=CARTESIAN_POINT('Ctrl Pts',(1.23815836053804,2.45268945480269,-1.59287456003142));
#4292=CARTESIAN_POINT('Ctrl Pts',(0.790103953079335,2.47898836731802,-1.85477368624924));
#4293=CARTESIAN_POINT('Ctrl Pts',(0.548432060457288,2.49300812980667,-1.94004603316793));
#4294=CARTESIAN_POINT('Ctrl Pts',(0.0363177609825734,2.5228814639427,-2.01699349355232));
#4295=CARTESIAN_POINT('Ctrl Pts',(-0.229740885380059,2.53840155164718,-2.00419789204612));
#4296=CARTESIAN_POINT('Ctrl Pts',(-0.738375400475203,2.56807189836107,-1.87687947883354));
#4297=CARTESIAN_POINT('Ctrl Pts',(-0.976262444410051,2.58098300576251,-1.76487034365478));
#4298=CARTESIAN_POINT('Ctrl Pts',(-1.39291398846778,2.60863690599144,-1.45801896507246));
#4299=CARTESIAN_POINT('Ctrl Pts',(-1.56849735241706,2.62339761807215,-1.26720574431744));
#4300=CARTESIAN_POINT('Ctrl Pts',(-1.84316960403584,2.65395003042836,-0.821006922788507));
#4301=CARTESIAN_POINT('Ctrl Pts',(-1.9362248745901,2.66945599004052,-0.56779400979672));
#4302=CARTESIAN_POINT('Ctrl Pts',(-2.0154427085729,2.69780963370476,-0.0522738600723176));
#4303=CARTESIAN_POINT('Ctrl Pts',(-2.00574981824586,2.71015036433805,0.204244764812837));
#4304=CARTESIAN_POINT('Ctrl Pts',(-1.88946498189406,2.73885605799548,0.705333053313018));
#4305=CARTESIAN_POINT('Ctrl Pts',(-1.7818984055525,2.75408407701296,0.944666063070827));
#4306=CARTESIAN_POINT('Ctrl Pts',(-1.47827330814531,2.78457551452497,1.37294196239716));
#4307=CARTESIAN_POINT('Ctrl Pts',(-1.28347335848784,2.79953528661918,1.55660084858788));
#4308=CARTESIAN_POINT('Ctrl Pts',(-0.843495908200234,2.82623234117405,1.83104437667243));
#4309=CARTESIAN_POINT('Ctrl Pts',(-0.604909818686825,2.83971359390995,1.9231130425793));
#4310=CARTESIAN_POINT('Ctrl Pts',(-0.237846563856373,2.86112561710839,1.98939716012295));
#4311=CARTESIAN_POINT('Ctrl Pts',(-0.118900276756154,2.86806415052256,2.));
#4312=CARTESIAN_POINT('Ctrl Pts',(-1.56472057533108E-14,2.87500000000001,
2.));
#4313=CARTESIAN_POINT('Ctrl Pts',(-1.870031907103E-14,2.96250000191184,
2.));
#4314=CARTESIAN_POINT('Ctrl Pts',(-0.170295006100021,2.95256612655601,2.));
#4315=CARTESIAN_POINT('Ctrl Pts',(-0.340271071332373,2.94265085608412,1.97824864775472));
#4316=CARTESIAN_POINT('Ctrl Pts',(-0.751083640266264,2.91868678956298,1.87087579921638));
#4317=CARTESIAN_POINT('Ctrl Pts',(-0.98193900049545,2.90614098403221,1.76070459522563));
#4318=CARTESIAN_POINT('Ctrl Pts',(-1.39965977067423,2.87841458049973,1.45303534142691));
#4319=CARTESIAN_POINT('Ctrl Pts',(-1.5797910577715,2.86314747147452,1.25482380547795));
#4320=CARTESIAN_POINT('Ctrl Pts',(-1.84851543059949,2.83263313129627,0.8059446082032));
#4321=CARTESIAN_POINT('Ctrl Pts',(-1.93697072901004,2.81767938203182,0.561006830098362));
#4322=CARTESIAN_POINT('Ctrl Pts',(-2.01587940205785,2.78963075638733,0.0513459771668947));
#4323=CARTESIAN_POINT('Ctrl Pts',(-2.00572725273602,2.77713418851999,-0.208496521839839));
#4324=CARTESIAN_POINT('Ctrl Pts',(-1.88567989006105,2.74793159773073,-0.717248527079829));
#4325=CARTESIAN_POINT('Ctrl Pts',(-1.77415593218552,2.7323894605413,-0.96051466878277));
#4326=CARTESIAN_POINT('Ctrl Pts',(-1.46866489711293,2.70222075332442,-1.3813248654293));
#4327=CARTESIAN_POINT('Ctrl Pts',(-1.28072316225833,2.6878549600921,-1.5571856115837));
#4328=CARTESIAN_POINT('Ctrl Pts',(-0.83876688931226,2.6609226030884,-1.83514444640525));
#4329=CARTESIAN_POINT('Ctrl Pts',(-0.586517626705013,2.6467135301363,-1.93063622781826));
#4330=CARTESIAN_POINT('Ctrl Pts',(-0.0646611294151879,2.61627190112773,
-2.01600742742588));
#4331=CARTESIAN_POINT('Ctrl Pts',(0.199371655450169,2.60086998867725,-2.00716806135491));
#4332=CARTESIAN_POINT('Ctrl Pts',(0.700909854133423,2.57161359375406,-1.89021092239354));
#4333=CARTESIAN_POINT('Ctrl Pts',(0.934382523524579,2.55882394907885,-1.78635678502449));
#4334=CARTESIAN_POINT('Ctrl Pts',(1.35998525898409,2.53145074879445,-1.49022979710036));
#4335=CARTESIAN_POINT('Ctrl Pts',(1.54537189209187,2.51628048076993,-1.29696939125311));
#4336=CARTESIAN_POINT('Ctrl Pts',(1.82645344292305,2.48575319485243,-0.854968354846357));
#4337=CARTESIAN_POINT('Ctrl Pts',(1.9216149980674,2.47069422434185,-0.611819595365497));
#4338=CARTESIAN_POINT('Ctrl Pts',(2.01361840955679,2.4424111985188,-0.105079072986001));
#4339=CARTESIAN_POINT('Ctrl Pts',(2.01050509035082,2.43005029389354,0.153531091476245));
#4340=CARTESIAN_POINT('Ctrl Pts',(1.90489887199435,2.40114067312447,0.664821392875117));
#4341=CARTESIAN_POINT('Ctrl Pts',(1.79980646867443,2.3856006996941,0.911757963010447));
#4342=CARTESIAN_POINT('Ctrl Pts',(1.50497723934194,2.35527678943077,1.34179597963616));
#4343=CARTESIAN_POINT('Ctrl Pts',(1.32127121823364,2.34076249986297,1.52304168137978));
#4344=CARTESIAN_POINT('Ctrl Pts',(0.888254477253353,2.31356877136604,1.81133557117034));
#4345=CARTESIAN_POINT('Ctrl Pts',(0.641222071284661,2.29990462273678,1.91280290869273));
#4346=CARTESIAN_POINT('Ctrl Pts',(0.2555299886456,2.27740591791616,1.98775831208609));
#4347=CARTESIAN_POINT('Ctrl Pts',(0.127758721976142,2.26995259402711,2.));
#4348=CARTESIAN_POINT('Ctrl Pts',(1.68615121864946E-14,2.26250000191184,
2.));
#4349=CARTESIAN_POINT('Origin',(0.,70.,0.));
#4350=CARTESIAN_POINT('',(-3.85812841423205E-14,1.475,2.));
#4351=CARTESIAN_POINT('',(3.55434499861684E-14,1.56250000191184,2.));
#4352=CARTESIAN_POINT('',(-2.44929359829471E-16,70.,2.));
#4353=CARTESIAN_POINT('Ctrl Pts',(-1.4210854715202E-13,1.475,2.));
#4354=CARTESIAN_POINT('Ctrl Pts',(0.223954565798372,1.48806401633825,2.00000000000002));
#4355=CARTESIAN_POINT('Ctrl Pts',(0.446651237620323,1.50105465552787,1.9623799948505));
#4356=CARTESIAN_POINT('Ctrl Pts',(0.900089169467497,1.52750520155229,1.80421749486211));
#4357=CARTESIAN_POINT('Ctrl Pts',(1.12307065137741,1.53982838655968,1.67453697057544));
#4358=CARTESIAN_POINT('Ctrl Pts',(1.51076243853498,1.56824166311884,1.33593391556795));
#4359=CARTESIAN_POINT('Ctrl Pts',(1.67091754054934,1.58335571929184,1.12921878454133));
#4360=CARTESIAN_POINT('Ctrl Pts',(1.90620009350724,1.61388037620501,0.660827725173358));
#4361=CARTESIAN_POINT('Ctrl Pts',(1.9769374846594,1.62899082464268,0.402558669348879));
#4362=CARTESIAN_POINT('Ctrl Pts',(2.01270379504195,1.65616111587045,-0.114623925871697));
#4363=CARTESIAN_POINT('Ctrl Pts',(1.98205222019211,1.66912791403358,-0.368272346770132));
#4364=CARTESIAN_POINT('Ctrl Pts',(1.82499297610609,1.69850535884176,-0.859116744253398));
#4365=CARTESIAN_POINT('Ctrl Pts',(1.6968392350588,1.71393742373891,-1.09060280984857));
#4366=CARTESIAN_POINT('Ctrl Pts',(1.35620729238248,1.74423917115757,-1.49375790704674));
#4367=CARTESIAN_POINT('Ctrl Pts',(1.14602139104281,1.75814875218919,-1.66047779684889));
#4368=CARTESIAN_POINT('Ctrl Pts',(0.68194353692421,1.78521996034611,-1.89742151731383));
#4369=CARTESIAN_POINT('Ctrl Pts',(0.434308572257149,1.79966533328502,-1.96890560133894));
#4370=CARTESIAN_POINT('Ctrl Pts',(-0.0843191117818514,1.82991861485396,
-2.01576595793462));
#4371=CARTESIAN_POINT('Ctrl Pts',(-0.350761000175043,1.84546105834356,-1.98680844766632));
#4372=CARTESIAN_POINT('Ctrl Pts',(-0.84874346307474,1.87451003534605,-1.82911354044634));
#4373=CARTESIAN_POINT('Ctrl Pts',(-1.07641941754803,1.88692413493962,-1.70509214089635));
#4374=CARTESIAN_POINT('Ctrl Pts',(-1.4735737909184,1.91509679720116,-1.37671524045494));
#4375=CARTESIAN_POINT('Ctrl Pts',(-1.6389065717559,1.930107164216,-1.17504195672059));
#4376=CARTESIAN_POINT('Ctrl Pts',(-1.88692619873131,1.9606311148776,-0.714018630620639));
#4377=CARTESIAN_POINT('Ctrl Pts',(-1.96488487202629,1.97584868051013,-0.457798413426827));
#4378=CARTESIAN_POINT('Ctrl Pts',(-2.01513953465624,2.0033900823559,0.0583654128161219));
#4379=CARTESIAN_POINT('Ctrl Pts',(-1.99156021339034,2.01605324342356,0.3128990953386));
#4380=CARTESIAN_POINT('Ctrl Pts',(-1.84837802151728,2.04520766626291,0.807340722581691));
#4381=CARTESIAN_POINT('Ctrl Pts',(-1.72718253099971,2.06058178955858,1.04169718973461));
#4382=CARTESIAN_POINT('Ctrl Pts',(-1.39912001823063,2.09095620884004,1.45354778048657));
#4383=CARTESIAN_POINT('Ctrl Pts',(-1.19431701439985,2.10533150749335,1.62599281106236));
#4384=CARTESIAN_POINT('Ctrl Pts',(-0.738641153368917,2.13191259938682,1.87597514462229));
#4385=CARTESIAN_POINT('Ctrl Pts',(-0.494017521167705,2.14618231126523,1.95468012692659));
#4386=CARTESIAN_POINT('Ctrl Pts',(-0.16104599383136,2.16560565035985,1.99514263757503));
#4387=CARTESIAN_POINT('Ctrl Pts',(-0.0804777381855486,2.17030546527252,
2.));
#4388=CARTESIAN_POINT('Ctrl Pts',(7.06522986662669E-16,2.17500000000001,
2.));
#4389=CARTESIAN_POINT('Ctrl Pts',(8.91647866652079E-15,2.26250000191184,
2.));
#4390=CARTESIAN_POINT('Ctrl Pts',(-0.133416331800623,2.2547173825568,2.));
#4391=CARTESIAN_POINT('Ctrl Pts',(-0.266818983260238,2.24693556122166,1.98665001605873));
#4392=CARTESIAN_POINT('Ctrl Pts',(-0.646448707316979,2.22479049398501,1.90952359766146));
#4393=CARTESIAN_POINT('Ctrl Pts',(-0.882803305241684,2.2116438631352,1.8123973313908));
#4394=CARTESIAN_POINT('Ctrl Pts',(-1.31666706932481,2.18465417488529,1.52863142004111));
#4395=CARTESIAN_POINT('Ctrl Pts',(-1.50749435171128,2.16959942830896,1.34079890614957));
#4396=CARTESIAN_POINT('Ctrl Pts',(-1.80153755051224,2.13908306064985,0.90649740615324));
#4397=CARTESIAN_POINT('Ctrl Pts',(-1.90380360717819,2.1239231559428,0.665452453606646));
#4398=CARTESIAN_POINT('Ctrl Pts',(-2.00969796320355,2.09539638641008,0.161906997632573));
#4399=CARTESIAN_POINT('Ctrl Pts',(-2.01394684785679,2.08308360048019,-0.0954742925500754));
#4400=CARTESIAN_POINT('Ctrl Pts',(-1.92349946949502,2.05449019122032,-0.609257189730553));
#4401=CARTESIAN_POINT('Ctrl Pts',(-1.82527917470336,2.0389650075537,-0.859868612177484));
#4402=CARTESIAN_POINT('Ctrl Pts',(-1.54192651951901,2.00850107238417,-1.29930440628386));
#4403=CARTESIAN_POINT('Ctrl Pts',(-1.36282768343608,1.9938412321369,-1.48609122379259));
#4404=CARTESIAN_POINT('Ctrl Pts',(-0.939207245649434,1.96638046159267,-1.78509613340325));
#4405=CARTESIAN_POINT('Ctrl Pts',(-0.697490100720316,1.95318692445385,-1.89267404339112));
#4406=CARTESIAN_POINT('Ctrl Pts',(-0.185133210869436,1.92329943921255,-2.00873304752374));
#4407=CARTESIAN_POINT('Ctrl Pts',(0.0805470681854508,1.90780142293435,-2.0156364878012));
#4408=CARTESIAN_POINT('Ctrl Pts',(0.589884203102323,1.8780900900642,-1.92779010209547));
#4409=CARTESIAN_POINT('Ctrl Pts',(0.829285228352145,1.864474850519,-1.837537672256));
#4410=CARTESIAN_POINT('Ctrl Pts',(1.27143703921337,1.83788368417352,-1.56644555478925));
#4411=CARTESIAN_POINT('Ctrl Pts',(1.4676374048311,1.82295966690869,-1.38430296119986));
#4412=CARTESIAN_POINT('Ctrl Pts',(1.77466543106788,1.79248065499219,-0.958237706752163));
#4413=CARTESIAN_POINT('Ctrl Pts',(1.8841247533492,1.77722982458753,-0.719545926011083));
#4414=CARTESIAN_POINT('Ctrl Pts',(2.00412757277745,1.74846085058755,-0.219351590116043));
#4415=CARTESIAN_POINT('Ctrl Pts',(2.01575665841001,1.7360969016035,0.0368712940846499));
#4416=CARTESIAN_POINT('Ctrl Pts',(1.94053433806999,1.70782968876513,0.552987368037824));
#4417=CARTESIAN_POINT('Ctrl Pts',(1.84933110419448,1.69233226331264,0.807100622354414));
#4418=CARTESIAN_POINT('Ctrl Pts',(1.57778244929932,1.66175151715696,1.25566371706682));
#4419=CARTESIAN_POINT('Ctrl Pts',(1.40347029545737,1.64695635989922,1.4478927089961));
#4420=CARTESIAN_POINT('Ctrl Pts',(0.989299965515635,1.61923469029751,1.75751810289436));
#4421=CARTESIAN_POINT('Ctrl Pts',(0.752753555657878,1.60641062599187,1.87108596660523));
#4422=CARTESIAN_POINT('Ctrl Pts',(0.337028356974093,1.58215998940198,1.97866476993144));
#4423=CARTESIAN_POINT('Ctrl Pts',(0.168658385814324,1.57233840775101,2.));
#4424=CARTESIAN_POINT('Ctrl Pts',(4.85722573273506E-16,1.56250000191184,
2.));
#4425=CARTESIAN_POINT('Origin',(0.,70.,0.));
#4426=CARTESIAN_POINT('',(-7.54708115709547E-15,0.775000000000007,2.));
#4427=CARTESIAN_POINT('',(2.64014572677706E-14,0.862500001911841,2.));
#4428=CARTESIAN_POINT('',(-2.44929359829471E-16,70.,2.));
#4429=CARTESIAN_POINT('Ctrl Pts',(-1.38777878078145E-15,0.775000000000008,
2.));
#4430=CARTESIAN_POINT('Ctrl Pts',(0.263641812514793,0.790379105730038,2.));
#4431=CARTESIAN_POINT('Ctrl Pts',(0.524773806618217,0.805611805386091,1.94786890290239));
#4432=CARTESIAN_POINT('Ctrl Pts',(1.00270510760052,0.833491131276723,1.7490090237614));
#4433=CARTESIAN_POINT('Ctrl Pts',(1.2163618842073,0.845922301161266,1.60777046374085));
#4434=CARTESIAN_POINT('Ctrl Pts',(1.58424989383885,0.874816756963846,1.2482088136233));
#4435=CARTESIAN_POINT('Ctrl Pts',(1.73319192739454,0.890110749075232,1.0314580066477));
#4436=CARTESIAN_POINT('Ctrl Pts',(1.94137076405355,0.920559320787235,0.548924705768364));
#4437=CARTESIAN_POINT('Ctrl Pts',(1.9969671379211,0.935408976994167,0.287076326897205));
#4438=CARTESIAN_POINT('Ctrl Pts',(2.00266664909294,0.961786339306387,-0.231769421015456));
#4439=CARTESIAN_POINT('Ctrl Pts',(1.95713900686814,0.975692568602954,-0.483835156331504));
#4440=CARTESIAN_POINT('Ctrl Pts',(1.77062477881778,1.00552284657222,-0.966637482806648));
#4441=CARTESIAN_POINT('Ctrl Pts',(1.62792865993129,1.02103774381255,-1.19136715780624));
#4442=CARTESIAN_POINT('Ctrl Pts',(1.26545504715454,1.05076689279692,-1.57057745140074));
#4443=CARTESIAN_POINT('Ctrl Pts',(1.05002459454285,1.06374856531836,-1.7220676167783));
#4444=CARTESIAN_POINT('Ctrl Pts',(0.576842766048914,1.09135083864717,-1.93215175399565));
#4445=CARTESIAN_POINT('Ctrl Pts',(0.324257631581426,1.10608497149111,-1.99017081615757));
#4446=CARTESIAN_POINT('Ctrl Pts',(-0.199111495671019,1.1366148372475,-2.00788391891833));
#4447=CARTESIAN_POINT('Ctrl Pts',(-0.465028558889729,1.15212666593526,-1.96342070884061));
#4448=CARTESIAN_POINT('Ctrl Pts',(-0.952205920019837,1.18054534533451,-1.77711387884304));
#4449=CARTESIAN_POINT('Ctrl Pts',(-1.17044128448817,1.19287314868519,-1.641615758944));
#4450=CARTESIAN_POINT('Ctrl Pts',(-1.54823753074778,1.22153080742898,-1.29246199804695));
#4451=CARTESIAN_POINT('Ctrl Pts',(-1.7028485139701,1.2367410570788,-1.0806418315239));
#4452=CARTESIAN_POINT('Ctrl Pts',(-1.92465185066364,1.26724065016377,-0.604964678147023));
#4453=CARTESIAN_POINT('Ctrl Pts',(-1.98782202608,1.2822267987879,-0.344787186479645));
#4454=CARTESIAN_POINT('Ctrl Pts',(-2.0085179530319,1.30900338630977,0.173302986422976));
#4455=CARTESIAN_POINT('Ctrl Pts',(-1.97044884668927,1.32238847684033,0.4261155410126));
#4456=CARTESIAN_POINT('Ctrl Pts',(-1.79873862119006,1.35199476629224,0.913031139575736));
#4457=CARTESIAN_POINT('Ctrl Pts',(-1.66330887508614,1.36747489263217,1.14126777153031));
#4458=CARTESIAN_POINT('Ctrl Pts',(-1.3116979731138,1.39749737524703,1.5325561541498));
#4459=CARTESIAN_POINT('Ctrl Pts',(-1.09889701745739,1.41089767398167,1.69164661172676));
#4460=CARTESIAN_POINT('Ctrl Pts',(-0.630261499474268,1.43823474586402,1.91529946453159));
#4461=CARTESIAN_POINT('Ctrl Pts',(-0.380091506104799,1.45282799547724,1.98017506043044));
#4462=CARTESIAN_POINT('Ctrl Pts',(-0.0830206559478754,1.47015712840306,
1.99870903416013));
#4463=CARTESIAN_POINT('Ctrl Pts',(-0.0414887428399634,1.47257982333434,
2.));
#4464=CARTESIAN_POINT('Ctrl Pts',(-1.50526581573235E-13,1.475,2.));
#4465=CARTESIAN_POINT('Ctrl Pts',(7.41933818794109E-16,1.56250000191184,
2.));
#4466=CARTESIAN_POINT('Ctrl Pts',(-0.0941640936003199,1.55700709645182,
2.));
#4467=CARTESIAN_POINT('Ctrl Pts',(-0.188418089770249,1.55150894667523,1.99335001499073));
#4468=CARTESIAN_POINT('Ctrl Pts',(-0.533623864488207,1.53137194315001,1.94417515988776));
#4469=CARTESIAN_POINT('Ctrl Pts',(-0.776121134681528,1.5172262690554,1.86071371261903));
#4470=CARTESIAN_POINT('Ctrl Pts',(-1.22623678899418,1.49096952255383,1.60204214273226));
#4471=CARTESIAN_POINT('Ctrl Pts',(-1.42755153341047,1.47621646136407,1.42562718359061));
#4472=CARTESIAN_POINT('Ctrl Pts',(-1.74709544586349,1.44578927622245,1.00781388350229));
#4473=CARTESIAN_POINT('Ctrl Pts',(-1.8635057748182,1.43046160716481,0.771614257467079));
#4474=CARTESIAN_POINT('Ctrl Pts',(-1.99720748551615,1.40146292080669,0.274781854700861));
#4475=CARTESIAN_POINT('Ctrl Pts',(-2.01592235701723,1.38895402525217,0.019589420613992));
#4476=CARTESIAN_POINT('Ctrl Pts',(-1.95564851891177,1.36116039250832,-0.495782708893493));
#4477=CARTESIAN_POINT('Ctrl Pts',(-1.87273279584763,1.34587593916101,-0.750465005444869));
#4478=CARTESIAN_POINT('Ctrl Pts',(-1.61604197277987,1.31536666819081,-1.20619143161691));
#4479=CARTESIAN_POINT('Ctrl Pts',(-1.44721963392012,1.3004343306366,-1.40430543534141));
#4480=CARTESIAN_POINT('Ctrl Pts',(-1.04355166329762,1.27243148996314,-1.72556011301291));
#4481=CARTESIAN_POINT('Ctrl Pts',(-0.81254646348664,1.25989854561521,-1.84562551552966));
#4482=CARTESIAN_POINT('Ctrl Pts',(-0.310972319885067,1.23064005390512,-1.99335257263115));
#4483=CARTESIAN_POINT('Ctrl Pts',(-0.0445515678019491,1.21509884336694,
-2.01696751857633));
#4484=CARTESIAN_POINT('Ctrl Pts',(0.472067650418802,1.18496272230406,-1.96013306796473));
#4485=CARTESIAN_POINT('Ctrl Pts',(0.717825270595456,1.17062686112709,-1.88407560427836));
#4486=CARTESIAN_POINT('Ctrl Pts',(1.17863878906077,1.14374607254995,-1.6377962436916));
#4487=CARTESIAN_POINT('Ctrl Pts',(1.38695540224028,1.12942016937891,-1.4656059683808));
#4488=CARTESIAN_POINT('Ctrl Pts',(1.71966797178848,1.09892764261738,-1.05410216737661));
#4489=CARTESIAN_POINT('Ctrl Pts',(1.84262257064793,1.08353778589356,-0.82044988079058));
#4490=CARTESIAN_POINT('Ctrl Pts',(1.98930206580404,1.05432659707209,-0.326903747509112));
#4491=CARTESIAN_POINT('Ctrl Pts',(2.01466873925147,1.04159555592171,-0.0726019437903748));
#4492=CARTESIAN_POINT('Ctrl Pts',(1.96808522885465,1.01414748587772,0.443833932638237));
#4493=CARTESIAN_POINT('Ctrl Pts',(1.89195071824916,0.998955904156174,0.70059298260607));
#4494=CARTESIAN_POINT('Ctrl Pts',(1.64713688415654,0.968429476623535,1.16351620342109));
#4495=CARTESIAN_POINT('Ctrl Pts',(1.48310153656839,0.953391807058156,1.36647901093069));
#4496=CARTESIAN_POINT('Ctrl Pts',(1.08833999596802,0.925157628666796,1.69745511758567));
#4497=CARTESIAN_POINT('Ctrl Pts',(0.861866671489158,0.912775557748692,1.8229169881279));
#4498=CARTESIAN_POINT('Ctrl Pts',(0.417954610804559,0.886880687542087,1.96709817284442));
#4499=CARTESIAN_POINT('Ctrl Pts',(0.209440523454726,0.87471736578003,2.));
#4500=CARTESIAN_POINT('Ctrl Pts',(8.67361737988404E-16,0.862500001911838,
2.));
#4501=CARTESIAN_POINT('Origin',(0.,0.45,0.));
#4502=CARTESIAN_POINT('',(-2.44929359829471E-16,0.440000000000001,-2.));
#4503=CARTESIAN_POINT('',(1.90060369884293E-8,0.404509613602118,-1.96450961360212));
#4504=CARTESIAN_POINT('',(-2.46154006628618E-16,0.45,-2.01));
#4505=CARTESIAN_POINT('',(1.07566249295046,0.444996920070102,-1.69202921096245));
#4506=CARTESIAN_POINT('Origin',(0.,0.440000000000001,0.));
#4507=CARTESIAN_POINT('',(1.22721437665197,0.445850114232433,-1.58662519203873));
#4508=CARTESIAN_POINT('Ctrl Pts',(1.07566249295046,0.444996920070102,-1.69202921096245));
#4509=CARTESIAN_POINT('Ctrl Pts',(1.09611643683742,0.443060583023077,-1.67673166768133));
#4510=CARTESIAN_POINT('Ctrl Pts',(1.1167162602212,0.441907359466892,-1.66168928306883));
#4511=CARTESIAN_POINT('Ctrl Pts',(1.13725615399585,0.44160691752963,-1.64714258414414));
#4512=CARTESIAN_POINT('Ctrl Pts',(1.15842534493283,0.441297270712311,-1.63215020636371));
#4513=CARTESIAN_POINT('Ctrl Pts',(1.17953119574262,0.441893460704303,-1.61768416278773));
#4514=CARTESIAN_POINT('Ctrl Pts',(1.20038775671367,0.443471757258991,-1.60404747924317));
#4515=CARTESIAN_POINT('Ctrl Pts',(1.20941519791304,0.44415489861496,-1.59814505079277));
#4516=CARTESIAN_POINT('Ctrl Pts',(1.21839639510557,0.445022033500666,-1.59239850981534));
#4517=CARTESIAN_POINT('Ctrl Pts',(1.22731813304862,0.446079346610564,-1.58683475673666));
#4518=CARTESIAN_POINT('',(1.31150072492913E-11,0.264072050762771,1.82407205076277));
#4519=CARTESIAN_POINT('Ctrl Pts',(1.22456646636222,0.44,-1.5812770059231));
#4520=CARTESIAN_POINT('Ctrl Pts',(1.34092436486328,0.434825310204451,-1.48462261860236));
#4521=CARTESIAN_POINT('Ctrl Pts',(1.44576508331674,0.429407853078801,-1.37490110720192));
#4522=CARTESIAN_POINT('Ctrl Pts',(1.62424340516482,0.418528363271193,-1.13898239124983));
#4523=CARTESIAN_POINT('Ctrl Pts',(1.69851441965134,0.413111710208662,-1.01444043254867));
#4524=CARTESIAN_POINT('Ctrl Pts',(1.85949786400429,0.398560929406842,-0.661377198370944));
#4525=CARTESIAN_POINT('Ctrl Pts',(1.91858368406403,0.389540675297832,-0.423038305434833));
#4526=CARTESIAN_POINT('Ctrl Pts',(1.94755017248106,0.372319500206739,0.073807683981543));
#4527=CARTESIAN_POINT('Ctrl Pts',(1.91303291352136,0.363978840607724,0.326681990469294));
#4528=CARTESIAN_POINT('Ctrl Pts',(1.74862425848826,0.345324659582443,0.794041188679305));
#4529=CARTESIAN_POINT('Ctrl Pts',(1.62615811693947,0.335882829432591,1.00394140613174));
#4530=CARTESIAN_POINT('Ctrl Pts',(1.27814151888825,0.315411208564217,1.40228678216834));
#4531=CARTESIAN_POINT('Ctrl Pts',(1.06504837422352,0.306309114754379,1.54645068384557));
#4532=CARTESIAN_POINT('Ctrl Pts',(0.738669273324379,0.293563865877837,1.70724532485268));
#4533=CARTESIAN_POINT('Ctrl Pts',(0.589469481980592,0.287689020611286,1.75814842742425));
#4534=CARTESIAN_POINT('Ctrl Pts',(0.292319615601393,0.275866774827419,1.81832292184012));
#4535=CARTESIAN_POINT('Ctrl Pts',(0.146071997417127,0.269995076562265,1.82999507656121));
#4536=CARTESIAN_POINT('Ctrl Pts',(1.31614857901141E-11,0.264072050762774,
1.82407205076277));
#4537=CARTESIAN_POINT('',(-0.414966524668622,0.0611138874999821,-1.56710338511853));
#4538=CARTESIAN_POINT('Ctrl Pts',(1.31119073931707E-11,0.264072050762771,
1.82407205076277));
#4539=CARTESIAN_POINT('Ctrl Pts',(-0.182500618677702,0.256671892675391,
1.8166718926767));
#4540=CARTESIAN_POINT('Ctrl Pts',(-0.362846391412083,0.249266998949665,
1.7818819341821));
#4541=CARTESIAN_POINT('Ctrl Pts',(-0.695425892968101,0.235448646498967,
1.66401272030053));
#4542=CARTESIAN_POINT('Ctrl Pts',(-0.874684974565809,0.228481241516197,
1.57533708528328));
#4543=CARTESIAN_POINT('Ctrl Pts',(-1.22898394413066,0.211375383019265,1.29647398987752));
#4544=CARTESIAN_POINT('Ctrl Pts',(-1.38061231788004,0.201854495765184,1.11869581647509));
#4545=CARTESIAN_POINT('Ctrl Pts',(-1.60022755658981,0.182831136549121,0.724548107605763));
#4546=CARTESIAN_POINT('Ctrl Pts',(-1.67005790774639,0.173520054063588,0.514053964643143));
#4547=CARTESIAN_POINT('Ctrl Pts',(-1.71881409521262,0.158649088175912,0.147705584520746));
#4548=CARTESIAN_POINT('Ctrl Pts',(-1.73283633029671,0.150263481745077,-0.0918032208300236));
#4549=CARTESIAN_POINT('Ctrl Pts',(-1.60131282490526,0.129348630402047,-0.577463975714151));
#4550=CARTESIAN_POINT('Ctrl Pts',(-1.50916906144907,0.120153028228782,-0.767510573105503));
#4551=CARTESIAN_POINT('Ctrl Pts',(-1.26910066605646,0.102383574220385,-1.09098903228809));
#4552=CARTESIAN_POINT('Ctrl Pts',(-1.12774845722577,0.093949227674449,-1.22519616910076));
#4553=CARTESIAN_POINT('Ctrl Pts',(-0.822715308031425,0.0789309073211611,
-1.42794886846669));
#4554=CARTESIAN_POINT('Ctrl Pts',(-0.638864841828697,0.0712113726913205,
-1.51826095786994));
#4555=CARTESIAN_POINT('Ctrl Pts',(-0.41496652466861,0.0611138875000055,
-1.56710338511849));
#4556=CARTESIAN_POINT('',(-1.9852919333802E-16,0.061113887500004,-1.6211138875));
#4557=CARTESIAN_POINT('Origin',(-1.15733580648385E-15,0.0611138875000017,
-3.60822483003176E-15));
#4558=CARTESIAN_POINT('',(-1.91044900666986E-16,-2.08166817117217E-16,-1.55999999999999));
#4559=CARTESIAN_POINT('',(-2.46154006628618E-16,0.45,-2.01));
#4560=CARTESIAN_POINT('Origin',(0.,0.,0.));
#4561=CARTESIAN_POINT('',(1.55927926836488,0.0611138874999996,-0.443461835441161));
#4562=CARTESIAN_POINT('Origin',(-1.15733580648385E-15,0.0611138875000017,
-3.60822483003176E-15));
#4563=CARTESIAN_POINT('Ctrl Pts',(1.55927926836487,0.0611138874999902,-0.443461835441164));
#4564=CARTESIAN_POINT('Ctrl Pts',(1.54461788344873,0.0822167370265837,-0.572156824316265));
#4565=CARTESIAN_POINT('Ctrl Pts',(1.51500223189783,0.103443446107898,-0.698682493147245));
#4566=CARTESIAN_POINT('Ctrl Pts',(1.4255755483403,0.146036084380937,-0.946435303136844));
#4567=CARTESIAN_POINT('Ctrl Pts',(1.36511359324264,0.167235369334923,-1.06646836094372));
#4568=CARTESIAN_POINT('Ctrl Pts',(1.18480286160083,0.216895387258446,-1.33771622745885));
#4569=CARTESIAN_POINT('Ctrl Pts',(1.03366605550938,0.247409205792169,-1.5081345966626));
#4570=CARTESIAN_POINT('Ctrl Pts',(0.585735228688806,0.319098797267994,-1.8037064814823));
#4571=CARTESIAN_POINT('Ctrl Pts',(0.344445827034462,0.355553556198311,-1.90155408525721));
#4572=CARTESIAN_POINT('Ctrl Pts',(0.0608150575562096,0.395936422252363,
-1.95522821977963));
#4573=CARTESIAN_POINT('Ctrl Pts',(0.030455422336093,0.400230280246623,-1.96023027994078));
#4574=CARTESIAN_POINT('Ctrl Pts',(1.97280240755613E-8,0.404509616171237,
-1.96450961617124));
#4575=CARTESIAN_POINT('Origin',(0.,9.65431457505077,0.));
#4576=CARTESIAN_POINT('',(-2.59276989545945E-16,9.93715728752539,-2.11715728752538));
#4577=CARTESIAN_POINT('Origin',(0.,9.93715728752539,0.));
#4578=CARTESIAN_POINT('Origin',(-2.93915231795365E-16,9.65431457505077,
-2.4));
#4579=CARTESIAN_POINT('Origin',(0.,11.9,0.));
#4580=CARTESIAN_POINT('',(-4.82336772927411E-16,12.,-3.9385786437627));
#4581=CARTESIAN_POINT('Origin',(0.,12.,0.));
#4582=CARTESIAN_POINT('',(-4.90996333489766E-16,11.8292893218814,-4.00928932188135));
#4583=CARTESIAN_POINT('Origin',(-4.82336772927411E-16,11.9,-3.9385786437627));
#4584=CARTESIAN_POINT('Origin',(0.,11.8292893218814,0.));
#4585=CARTESIAN_POINT('Origin',(0.,9.82000000000001,0.));
#4586=CARTESIAN_POINT('',(-2.44929359829471E-16,9.82000000000001,-2.));
#4587=CARTESIAN_POINT('Origin',(0.,0.45,0.));
#4588=CARTESIAN_POINT('',(-0.257142857142752,0.440000000000001,-1.983400501921));
#4589=CARTESIAN_POINT('Ctrl Pts',(1.97280240755613E-8,0.404509616171237,
-1.96450961617124));
#4590=CARTESIAN_POINT('Ctrl Pts',(-0.0851508098666215,0.416474291496151,
-1.97647429235125));
#4591=CARTESIAN_POINT('Ctrl Pts',(-0.171050352799175,0.428324849718101,
-1.98278931537122));
#4592=CARTESIAN_POINT('Ctrl Pts',(-0.257142860795768,0.440000000495393,
-1.98340050194693));
#4593=CARTESIAN_POINT('Origin',(0.,0.440000000000001,0.));
#4594=CARTESIAN_POINT('Origin',(0.,70.,0.));
#4595=CARTESIAN_POINT('',(3.88911999139645E-5,0.512497733258513,-1.99999999962187));
#4596=CARTESIAN_POINT('Ctrl Pts',(7.41933818794109E-16,0.862500001911838,
2.));
#4597=CARTESIAN_POINT('Ctrl Pts',(-0.0552703432441355,0.85927589855593,
2.));
#4598=CARTESIAN_POINT('Ctrl Pts',(-0.110605204112353,0.856048031671933,
1.99770894428596));
#4599=CARTESIAN_POINT('Ctrl Pts',(-0.420525197530566,0.837969365389204,
1.97191801653875));
#4600=CARTESIAN_POINT('Ctrl Pts',(-0.668822497164996,0.823485356243864,
1.90210933332907));
#4601=CARTESIAN_POINT('Ctrl Pts',(-1.13407308457661,0.796345738644854,1.66855652158443));
#4602=CARTESIAN_POINT('Ctrl Pts',(-1.34493079919103,0.782575416162501,1.50380074095044));
#4603=CARTESIAN_POINT('Ctrl Pts',(-1.68839639792481,0.75234409837338,1.10367580094517));
#4604=CARTESIAN_POINT('Ctrl Pts',(-1.81842083590996,0.736898436276265,0.873000627974349));
#4605=CARTESIAN_POINT('Ctrl Pts',(-1.97923207905364,0.707461727060999,0.38314931713809));
#4606=CARTESIAN_POINT('Ctrl Pts',(-2.01178745902749,0.694397241615903,0.129724445636981));
#4607=CARTESIAN_POINT('Ctrl Pts',(-1.97990252339381,0.667327612876277,-0.38770646183827));
#4608=CARTESIAN_POINT('Ctrl Pts',(-1.91110912213568,0.652247930485477,-0.646488870964808));
#4609=CARTESIAN_POINT('Ctrl Pts',(-1.67927651187011,0.62172721310498,-1.11679377315213));
#4610=CARTESIAN_POINT('Ctrl Pts',(-1.52053416600623,0.606587237749995,-1.32483762606637));
#4611=CARTESIAN_POINT('Ctrl Pts',(-1.14842110785954,0.579074246128193,-1.65461404442982));
#4612=CARTESIAN_POINT('Ctrl Pts',(-0.943653674653732,0.567546466266641,
-1.77936282934091));
#4613=CARTESIAN_POINT('Ctrl Pts',(-0.491508565968716,0.541171334926682,
-1.95432023904762));
#4614=CARTESIAN_POINT('Ctrl Pts',(-0.246785668814814,0.526895832592705,
-2.00000479927351));
#4615=CARTESIAN_POINT('Ctrl Pts',(3.88911998226715E-5,0.512497733258518,
-1.99999999962187));
#4616=CARTESIAN_POINT('Ctrl Pts',(3.88911998825542E-5,0.512497733258514,
-1.99999999962187));
#4617=CARTESIAN_POINT('Ctrl Pts',(0.172907047386434,0.502413757480966,-1.99999663809686));
#4618=CARTESIAN_POINT('Ctrl Pts',(0.345047132249512,0.492372252530618,-1.97758246327963));
#4619=CARTESIAN_POINT('Ctrl Pts',(0.710657412499713,0.471044986182691,-1.88072556043873));
#4620=CARTESIAN_POINT('Ctrl Pts',(0.899787219881527,0.460416896217352,-1.79791535289817));
#4621=CARTESIAN_POINT('Ctrl Pts',(1.07297685035835,0.449803484035599,-1.68781535678376));
#4622=CARTESIAN_POINT('Ctrl Pts',(-0.257142857142745,0.440000000000001,
-1.983400501921));
#4623=CARTESIAN_POINT('Ctrl Pts',(-0.481635713382096,0.453095416613961,
-1.95429557106834));
#4624=CARTESIAN_POINT('Ctrl Pts',(-0.699591640436684,0.465809512358811,
-1.88728564808705));
#4625=CARTESIAN_POINT('Ctrl Pts',(-1.1001273672762,0.489174096424447,-1.68497256298937));
#4626=CARTESIAN_POINT('Ctrl Pts',(-1.28046697101911,0.500590709856682,-1.55237102657148));
#4627=CARTESIAN_POINT('Ctrl Pts',(-1.61723343414184,0.527945616611,-1.20531651088329));
#4628=CARTESIAN_POINT('Ctrl Pts',(-1.76065753494044,0.543307978847312,-0.984026546458247));
#4629=CARTESIAN_POINT('Ctrl Pts',(-1.95580405938054,0.573697470973118,-0.495138509125262));
#4630=CARTESIAN_POINT('Ctrl Pts',(-2.00411916259232,0.588168923320128,-0.231816382286525));
#4631=CARTESIAN_POINT('Ctrl Pts',(-1.99550412590271,0.614665037838943,0.287696770244476));
#4632=CARTESIAN_POINT('Ctrl Pts',(-1.94272556814002,0.62890241602013,0.539052054300045));
#4633=CARTESIAN_POINT('Ctrl Pts',(-1.7419954325077,0.658928568404834,1.01752413058528));
#4634=CARTESIAN_POINT('Ctrl Pts',(-1.59237071225919,0.674463850180423,1.23865708487486));
#4635=CARTESIAN_POINT('Ctrl Pts',(-1.21961396478033,0.703899598653046,1.60612258395746));
#4636=CARTESIAN_POINT('Ctrl Pts',(-1.00163913819066,0.716571050272238,1.75037007568662));
#4637=CARTESIAN_POINT('Ctrl Pts',(-0.52412048953386,0.744426304777219,1.94720477377504));
#4638=CARTESIAN_POINT('Ctrl Pts',(-0.269351609796664,0.75928782276189,1.99843116295333));
#4639=CARTESIAN_POINT('Ctrl Pts',(-0.0079409294476568,0.774536779115582,
1.99998817825517));
#4640=CARTESIAN_POINT('Ctrl Pts',(-0.00397018014396892,0.774768406158276,
2.));
#4641=CARTESIAN_POINT('Ctrl Pts',(7.0652298666267E-16,0.775000000000008,
2.));
#4642=CARTESIAN_POINT('Ctrl Pts',(-1.6211138875,71.7812500009559,0.));
#4643=CARTESIAN_POINT('Ctrl Pts',(-1.6211138875,71.7229166676226,-0.935950539335166));
#4644=CARTESIAN_POINT('Ctrl Pts',(-0.81055694375,71.6645833342892,-1.40392580900275));
#4645=CARTESIAN_POINT('Ctrl Pts',(-1.14620883215705E-16,71.6062500009559,
-1.87190107867033));
#4646=CARTESIAN_POINT('Ctrl Pts',(0.81055694375,71.5479166676226,-1.40392580900275));
#4647=CARTESIAN_POINT('Ctrl Pts',(1.6211138875,71.4895833342893,-0.935950539335166));
#4648=CARTESIAN_POINT('Ctrl Pts',(1.6211138875,71.4312500009559,-1.9852919333802E-16));
#4649=CARTESIAN_POINT('Ctrl Pts',(1.6211138875,71.3729166676226,0.935950539335165));
#4650=CARTESIAN_POINT('Ctrl Pts',(0.810556943750001,71.3145833342893,1.40392580900275));
#4651=CARTESIAN_POINT('Ctrl Pts',(3.43862649647115E-16,71.2562500009559,
1.87190107867033));
#4652=CARTESIAN_POINT('Ctrl Pts',(-0.810556943749999,71.1979166676226,1.40392580900275));
#4653=CARTESIAN_POINT('Ctrl Pts',(-1.6211138875,71.1395833342893,0.935950539335167));
#4654=CARTESIAN_POINT('Ctrl Pts',(-1.6211138875,71.0812500009559,0.));
#4655=CARTESIAN_POINT('Ctrl Pts',(-1.6211138875,71.0229166676226,-0.935950539335166));
#4656=CARTESIAN_POINT('Ctrl Pts',(-0.81055694375,70.9645833342893,-1.40392580900275));
#4657=CARTESIAN_POINT('Ctrl Pts',(-1.14620883215705E-16,70.9062500009559,
-1.87190107867033));
#4658=CARTESIAN_POINT('Ctrl Pts',(0.81055694375,70.8479166676226,-1.40392580900275));
#4659=CARTESIAN_POINT('Ctrl Pts',(1.6211138875,70.7895833342893,-0.935950539335166));
#4660=CARTESIAN_POINT('Ctrl Pts',(1.6211138875,70.7312500009559,-1.9852919333802E-16));
#4661=CARTESIAN_POINT('Ctrl Pts',(1.6211138875,70.6729166676226,0.935950539335165));
#4662=CARTESIAN_POINT('Ctrl Pts',(0.810556943750001,70.6145833342893,1.40392580900275));
#4663=CARTESIAN_POINT('Ctrl Pts',(3.43862649647115E-16,70.5562500009559,
1.87190107867033));
#4664=CARTESIAN_POINT('Ctrl Pts',(-0.810556943749999,70.4979166676226,1.40392580900275));
#4665=CARTESIAN_POINT('Ctrl Pts',(-1.6211138875,70.4395833342893,0.935950539335167));
#4666=CARTESIAN_POINT('Ctrl Pts',(-1.6211138875,70.3812500009559,0.));
#4667=CARTESIAN_POINT('Ctrl Pts',(-1.6211138875,70.3229166676226,-0.935950539335166));
#4668=CARTESIAN_POINT('Ctrl Pts',(-0.81055694375,70.2645833342893,-1.40392580900275));
#4669=CARTESIAN_POINT('Ctrl Pts',(-1.14620883215705E-16,70.2062500009559,
-1.87190107867033));
#4670=CARTESIAN_POINT('Ctrl Pts',(0.81055694375,70.1479166676226,-1.40392580900275));
#4671=CARTESIAN_POINT('Ctrl Pts',(1.6211138875,70.0895833342893,-0.935950539335166));
#4672=CARTESIAN_POINT('Ctrl Pts',(1.6211138875,70.0312500009559,-1.9852919333802E-16));
#4673=CARTESIAN_POINT('Ctrl Pts',(1.6211138875,69.9729166676226,0.935950539335165));
#4674=CARTESIAN_POINT('Ctrl Pts',(0.810556943750001,69.9145833342892,1.40392580900275));
#4675=CARTESIAN_POINT('Ctrl Pts',(3.43862649647115E-16,69.8562500009559,
1.87190107867033));
#4676=CARTESIAN_POINT('Ctrl Pts',(-0.810556943749999,69.7979166676226,1.40392580900275));
#4677=CARTESIAN_POINT('Ctrl Pts',(-1.6211138875,69.7395833342893,0.935950539335167));
#4678=CARTESIAN_POINT('Ctrl Pts',(-1.6211138875,69.6812500009559,0.));
#4679=CARTESIAN_POINT('Ctrl Pts',(-1.6211138875,69.6229166676226,-0.935950539335166));
#4680=CARTESIAN_POINT('Ctrl Pts',(-0.81055694375,69.5645833342893,-1.40392580900275));
#4681=CARTESIAN_POINT('Ctrl Pts',(-1.14620883215705E-16,69.5062500009559,
-1.87190107867033));
#4682=CARTESIAN_POINT('Ctrl Pts',(0.81055694375,69.4479166676226,-1.40392580900275));
#4683=CARTESIAN_POINT('Ctrl Pts',(1.6211138875,69.3895833342893,-0.935950539335166));
#4684=CARTESIAN_POINT('Ctrl Pts',(1.6211138875,69.3312500009559,-1.9852919333802E-16));
#4685=CARTESIAN_POINT('Ctrl Pts',(1.6211138875,69.2729166676226,0.935950539335165));
#4686=CARTESIAN_POINT('Ctrl Pts',(0.810556943750001,69.2145833342893,1.40392580900275));
#4687=CARTESIAN_POINT('Ctrl Pts',(3.43862649647115E-16,69.1562500009559,
1.87190107867033));
#4688=CARTESIAN_POINT('Ctrl Pts',(-0.810556943749999,69.0979166676226,1.40392580900275));
#4689=CARTESIAN_POINT('Ctrl Pts',(-1.6211138875,69.0395833342892,0.935950539335167));
#4690=CARTESIAN_POINT('Ctrl Pts',(-1.6211138875,68.9812500009559,0.));
#4691=CARTESIAN_POINT('Ctrl Pts',(-1.6211138875,68.9229166676226,-0.935950539335166));
#4692=CARTESIAN_POINT('Ctrl Pts',(-0.81055694375,68.8645833342893,-1.40392580900275));
#4693=CARTESIAN_POINT('Ctrl Pts',(-1.14620883215705E-16,68.8062500009559,
-1.87190107867033));
#4694=CARTESIAN_POINT('Ctrl Pts',(0.81055694375,68.7479166676226,-1.40392580900275));
#4695=CARTESIAN_POINT('Ctrl Pts',(1.6211138875,68.6895833342893,-0.935950539335166));
#4696=CARTESIAN_POINT('Ctrl Pts',(1.6211138875,68.6312500009559,-1.9852919333802E-16));
#4697=CARTESIAN_POINT('Ctrl Pts',(1.6211138875,68.5729166676226,0.935950539335165));
#4698=CARTESIAN_POINT('Ctrl Pts',(0.810556943750001,68.5145833342893,1.40392580900275));
#4699=CARTESIAN_POINT('Ctrl Pts',(3.43862649647115E-16,68.4562500009559,
1.87190107867033));
#4700=CARTESIAN_POINT('Ctrl Pts',(-0.810556943749999,68.3979166676226,1.40392580900275));
#4701=CARTESIAN_POINT('Ctrl Pts',(-1.6211138875,68.3395833342893,0.935950539335167));
#4702=CARTESIAN_POINT('Ctrl Pts',(-1.6211138875,68.2812500009559,0.));
#4703=CARTESIAN_POINT('Ctrl Pts',(-1.6211138875,68.2229166676226,-0.935950539335166));
#4704=CARTESIAN_POINT('Ctrl Pts',(-0.81055694375,68.1645833342892,-1.40392580900275));
#4705=CARTESIAN_POINT('Ctrl Pts',(-1.14620883215705E-16,68.1062500009559,
-1.87190107867033));
#4706=CARTESIAN_POINT('Ctrl Pts',(0.81055694375,68.0479166676226,-1.40392580900275));
#4707=CARTESIAN_POINT('Ctrl Pts',(1.6211138875,67.9895833342893,-0.935950539335166));
#4708=CARTESIAN_POINT('Ctrl Pts',(1.6211138875,67.9312500009559,-1.9852919333802E-16));
#4709=CARTESIAN_POINT('Ctrl Pts',(1.6211138875,67.8729166676226,0.935950539335165));
#4710=CARTESIAN_POINT('Ctrl Pts',(0.810556943750001,67.8145833342893,1.40392580900275));
#4711=CARTESIAN_POINT('Ctrl Pts',(3.43862649647115E-16,67.7562500009559,
1.87190107867033));
#4712=CARTESIAN_POINT('Ctrl Pts',(-0.810556943749999,67.6979166676226,1.40392580900275));
#4713=CARTESIAN_POINT('Ctrl Pts',(-1.6211138875,67.6395833342893,0.935950539335167));
#4714=CARTESIAN_POINT('Ctrl Pts',(-1.6211138875,67.5812500009559,0.));
#4715=CARTESIAN_POINT('Ctrl Pts',(-1.6211138875,67.5229166676226,-0.935950539335166));
#4716=CARTESIAN_POINT('Ctrl Pts',(-0.81055694375,67.4645833342893,-1.40392580900275));
#4717=CARTESIAN_POINT('Ctrl Pts',(-1.14620883215705E-16,67.4062500009559,
-1.87190107867033));
#4718=CARTESIAN_POINT('Ctrl Pts',(0.81055694375,67.3479166676226,-1.40392580900275));
#4719=CARTESIAN_POINT('Ctrl Pts',(1.6211138875,67.2895833342892,-0.935950539335166));
#4720=CARTESIAN_POINT('Ctrl Pts',(1.6211138875,67.2312500009559,-1.9852919333802E-16));
#4721=CARTESIAN_POINT('Ctrl Pts',(1.6211138875,67.1729166676226,0.935950539335165));
#4722=CARTESIAN_POINT('Ctrl Pts',(0.810556943750001,67.1145833342893,1.40392580900275));
#4723=CARTESIAN_POINT('Ctrl Pts',(3.43862649647115E-16,67.0562500009559,
1.87190107867033));
#4724=CARTESIAN_POINT('Ctrl Pts',(-0.810556943749999,66.9979166676226,1.40392580900275));
#4725=CARTESIAN_POINT('Ctrl Pts',(-1.6211138875,66.9395833342893,0.935950539335167));
#4726=CARTESIAN_POINT('Ctrl Pts',(-1.6211138875,66.8812500009559,0.));
#4727=CARTESIAN_POINT('Ctrl Pts',(-1.6211138875,66.8229166676226,-0.935950539335166));
#4728=CARTESIAN_POINT('Ctrl Pts',(-0.81055694375,66.7645833342893,-1.40392580900275));
#4729=CARTESIAN_POINT('Ctrl Pts',(-1.14620883215705E-16,66.7062500009559,
-1.87190107867033));
#4730=CARTESIAN_POINT('Ctrl Pts',(0.81055694375,66.6479166676226,-1.40392580900275));
#4731=CARTESIAN_POINT('Ctrl Pts',(1.6211138875,66.5895833342893,-0.935950539335166));
#4732=CARTESIAN_POINT('Ctrl Pts',(1.6211138875,66.5312500009559,-1.9852919333802E-16));
#4733=CARTESIAN_POINT('Ctrl Pts',(1.6211138875,66.4729166676226,0.935950539335165));
#4734=CARTESIAN_POINT('Ctrl Pts',(0.810556943750001,66.4145833342893,1.40392580900275));
#4735=CARTESIAN_POINT('Ctrl Pts',(3.43862649647115E-16,66.3562500009559,
1.87190107867033));
#4736=CARTESIAN_POINT('Ctrl Pts',(-0.810556943749999,66.2979166676226,1.40392580900275));
#4737=CARTESIAN_POINT('Ctrl Pts',(-1.6211138875,66.2395833342893,0.935950539335167));
#4738=CARTESIAN_POINT('Ctrl Pts',(-1.6211138875,66.1812500009559,0.));
#4739=CARTESIAN_POINT('Ctrl Pts',(-1.6211138875,66.1229166676226,-0.935950539335166));
#4740=CARTESIAN_POINT('Ctrl Pts',(-0.81055694375,66.0645833342893,-1.40392580900275));
#4741=CARTESIAN_POINT('Ctrl Pts',(-1.14620883215705E-16,66.0062500009559,
-1.87190107867033));
#4742=CARTESIAN_POINT('Ctrl Pts',(0.81055694375,65.9479166676226,-1.40392580900275));
#4743=CARTESIAN_POINT('Ctrl Pts',(1.6211138875,65.8895833342893,-0.935950539335166));
#4744=CARTESIAN_POINT('Ctrl Pts',(1.6211138875,65.8312500009559,-1.9852919333802E-16));
#4745=CARTESIAN_POINT('Ctrl Pts',(1.6211138875,65.7729166676226,0.935950539335165));
#4746=CARTESIAN_POINT('Ctrl Pts',(0.810556943750001,65.7145833342893,1.40392580900275));
#4747=CARTESIAN_POINT('Ctrl Pts',(3.43862649647115E-16,65.6562500009559,
1.87190107867033));
#4748=CARTESIAN_POINT('Ctrl Pts',(-0.810556943749999,65.5979166676226,1.40392580900275));
#4749=CARTESIAN_POINT('Ctrl Pts',(-1.6211138875,65.5395833342892,0.935950539335167));
#4750=CARTESIAN_POINT('Ctrl Pts',(-1.6211138875,65.4812500009559,0.));
#4751=CARTESIAN_POINT('Ctrl Pts',(-1.6211138875,65.4229166676226,-0.935950539335166));
#4752=CARTESIAN_POINT('Ctrl Pts',(-0.81055694375,65.3645833342893,-1.40392580900275));
#4753=CARTESIAN_POINT('Ctrl Pts',(-1.14620883215705E-16,65.3062500009559,
-1.87190107867033));
#4754=CARTESIAN_POINT('Ctrl Pts',(0.81055694375,65.2479166676226,-1.40392580900275));
#4755=CARTESIAN_POINT('Ctrl Pts',(1.6211138875,65.1895833342893,-0.935950539335166));
#4756=CARTESIAN_POINT('Ctrl Pts',(1.6211138875,65.1312500009559,-1.9852919333802E-16));
#4757=CARTESIAN_POINT('Ctrl Pts',(1.6211138875,65.0729166676226,0.935950539335165));
#4758=CARTESIAN_POINT('Ctrl Pts',(0.810556943750001,65.0145833342893,1.40392580900275));
#4759=CARTESIAN_POINT('Ctrl Pts',(3.43862649647115E-16,64.9562500009559,
1.87190107867033));
#4760=CARTESIAN_POINT('Ctrl Pts',(-0.810556943749999,64.8979166676226,1.40392580900275));
#4761=CARTESIAN_POINT('Ctrl Pts',(-1.6211138875,64.8395833342893,0.935950539335167));
#4762=CARTESIAN_POINT('Ctrl Pts',(-1.6211138875,64.7812500009559,0.));
#4763=CARTESIAN_POINT('Ctrl Pts',(-1.6211138875,64.7229166676226,-0.935950539335166));
#4764=CARTESIAN_POINT('Ctrl Pts',(-0.81055694375,64.6645833342893,-1.40392580900275));
#4765=CARTESIAN_POINT('Ctrl Pts',(-1.14620883215705E-16,64.6062500009559,
-1.87190107867033));
#4766=CARTESIAN_POINT('Ctrl Pts',(0.81055694375,64.5479166676226,-1.40392580900275));
#4767=CARTESIAN_POINT('Ctrl Pts',(1.6211138875,64.4895833342893,-0.935950539335166));
#4768=CARTESIAN_POINT('Ctrl Pts',(1.6211138875,64.4312500009559,-1.9852919333802E-16));
#4769=CARTESIAN_POINT('Ctrl Pts',(1.6211138875,64.3729166676226,0.935950539335165));
#4770=CARTESIAN_POINT('Ctrl Pts',(0.810556943750001,64.3145833342893,1.40392580900275));
#4771=CARTESIAN_POINT('Ctrl Pts',(3.43862649647115E-16,64.2562500009559,
1.87190107867033));
#4772=CARTESIAN_POINT('Ctrl Pts',(-0.810556943749999,64.1979166676226,1.40392580900275));
#4773=CARTESIAN_POINT('Ctrl Pts',(-1.6211138875,64.1395833342893,0.935950539335167));
#4774=CARTESIAN_POINT('Ctrl Pts',(-1.6211138875,64.0812500009559,0.));
#4775=CARTESIAN_POINT('Ctrl Pts',(-1.6211138875,64.0229166676226,-0.935950539335166));
#4776=CARTESIAN_POINT('Ctrl Pts',(-0.81055694375,63.9645833342893,-1.40392580900275));
#4777=CARTESIAN_POINT('Ctrl Pts',(-1.14620883215705E-16,63.9062500009559,
-1.87190107867033));
#4778=CARTESIAN_POINT('Ctrl Pts',(0.81055694375,63.8479166676226,-1.40392580900275));
#4779=CARTESIAN_POINT('Ctrl Pts',(1.6211138875,63.7895833342893,-0.935950539335166));
#4780=CARTESIAN_POINT('Ctrl Pts',(1.6211138875,63.7312500009559,-1.9852919333802E-16));
#4781=CARTESIAN_POINT('Ctrl Pts',(1.6211138875,63.6729166676226,0.935950539335165));
#4782=CARTESIAN_POINT('Ctrl Pts',(0.810556943750001,63.6145833342893,1.40392580900275));
#4783=CARTESIAN_POINT('Ctrl Pts',(3.43862649647115E-16,63.5562500009559,
1.87190107867033));
#4784=CARTESIAN_POINT('Ctrl Pts',(-0.810556943749999,63.4979166676226,1.40392580900275));
#4785=CARTESIAN_POINT('Ctrl Pts',(-1.6211138875,63.4395833342893,0.935950539335167));
#4786=CARTESIAN_POINT('Ctrl Pts',(-1.6211138875,63.3812500009559,0.));
#4787=CARTESIAN_POINT('Ctrl Pts',(-1.6211138875,63.3229166676226,-0.935950539335166));
#4788=CARTESIAN_POINT('Ctrl Pts',(-0.81055694375,63.2645833342892,-1.40392580900275));
#4789=CARTESIAN_POINT('Ctrl Pts',(-1.14620883215705E-16,63.2062500009559,
-1.87190107867033));
#4790=CARTESIAN_POINT('Ctrl Pts',(0.81055694375,63.1479166676226,-1.40392580900275));
#4791=CARTESIAN_POINT('Ctrl Pts',(1.6211138875,63.0895833342893,-0.935950539335166));
#4792=CARTESIAN_POINT('Ctrl Pts',(1.6211138875,63.0312500009559,-1.9852919333802E-16));
#4793=CARTESIAN_POINT('Ctrl Pts',(1.6211138875,62.9729166676226,0.935950539335165));
#4794=CARTESIAN_POINT('Ctrl Pts',(0.810556943750001,62.9145833342893,1.40392580900275));
#4795=CARTESIAN_POINT('Ctrl Pts',(3.43862649647115E-16,62.8562500009559,
1.87190107867033));
#4796=CARTESIAN_POINT('Ctrl Pts',(-0.810556943749999,62.7979166676226,1.40392580900275));
#4797=CARTESIAN_POINT('Ctrl Pts',(-1.6211138875,62.7395833342893,0.935950539335167));
#4798=CARTESIAN_POINT('Ctrl Pts',(-1.6211138875,62.6812500009559,0.));
#4799=CARTESIAN_POINT('Ctrl Pts',(-1.6211138875,62.6229166676226,-0.935950539335166));
#4800=CARTESIAN_POINT('Ctrl Pts',(-0.81055694375,62.5645833342893,-1.40392580900275));
#4801=CARTESIAN_POINT('Ctrl Pts',(-1.14620883215705E-16,62.5062500009559,
-1.87190107867033));
#4802=CARTESIAN_POINT('Ctrl Pts',(0.81055694375,62.4479166676226,-1.40392580900275));
#4803=CARTESIAN_POINT('Ctrl Pts',(1.6211138875,62.3895833342893,-0.935950539335166));
#4804=CARTESIAN_POINT('Ctrl Pts',(1.6211138875,62.3312500009559,-1.9852919333802E-16));
#4805=CARTESIAN_POINT('Ctrl Pts',(1.6211138875,62.2729166676226,0.935950539335165));
#4806=CARTESIAN_POINT('Ctrl Pts',(0.810556943750001,62.2145833342893,1.40392580900275));
#4807=CARTESIAN_POINT('Ctrl Pts',(3.43862649647115E-16,62.1562500009559,
1.87190107867033));
#4808=CARTESIAN_POINT('Ctrl Pts',(-0.810556943749999,62.0979166676226,1.40392580900275));
#4809=CARTESIAN_POINT('Ctrl Pts',(-1.6211138875,62.0395833342893,0.935950539335167));
#4810=CARTESIAN_POINT('Ctrl Pts',(-1.6211138875,61.9812500009559,0.));
#4811=CARTESIAN_POINT('Ctrl Pts',(-1.6211138875,61.9229166676226,-0.935950539335166));
#4812=CARTESIAN_POINT('Ctrl Pts',(-0.81055694375,61.8645833342893,-1.40392580900275));
#4813=CARTESIAN_POINT('Ctrl Pts',(-1.14620883215705E-16,61.8062500009559,
-1.87190107867033));
#4814=CARTESIAN_POINT('Ctrl Pts',(0.81055694375,61.7479166676226,-1.40392580900275));
#4815=CARTESIAN_POINT('Ctrl Pts',(1.6211138875,61.6895833342893,-0.935950539335166));
#4816=CARTESIAN_POINT('Ctrl Pts',(1.6211138875,61.6312500009559,-1.9852919333802E-16));
#4817=CARTESIAN_POINT('Ctrl Pts',(1.6211138875,61.5729166676226,0.935950539335165));
#4818=CARTESIAN_POINT('Ctrl Pts',(0.810556943750001,61.5145833342893,1.40392580900275));
#4819=CARTESIAN_POINT('Ctrl Pts',(3.43862649647115E-16,61.4562500009559,
1.87190107867033));
#4820=CARTESIAN_POINT('Ctrl Pts',(-0.810556943749999,61.3979166676226,1.40392580900275));
#4821=CARTESIAN_POINT('Ctrl Pts',(-1.6211138875,61.3395833342893,0.935950539335167));
#4822=CARTESIAN_POINT('Ctrl Pts',(-1.6211138875,61.2812500009559,0.));
#4823=CARTESIAN_POINT('Ctrl Pts',(-1.6211138875,61.2229166676226,-0.935950539335166));
#4824=CARTESIAN_POINT('Ctrl Pts',(-0.81055694375,61.1645833342893,-1.40392580900275));
#4825=CARTESIAN_POINT('Ctrl Pts',(-1.14620883215705E-16,61.1062500009559,
-1.87190107867033));
#4826=CARTESIAN_POINT('Ctrl Pts',(0.81055694375,61.0479166676226,-1.40392580900275));
#4827=CARTESIAN_POINT('Ctrl Pts',(1.6211138875,60.9895833342893,-0.935950539335166));
#4828=CARTESIAN_POINT('Ctrl Pts',(1.6211138875,60.9312500009559,-1.9852919333802E-16));
#4829=CARTESIAN_POINT('Ctrl Pts',(1.6211138875,60.8729166676226,0.935950539335165));
#4830=CARTESIAN_POINT('Ctrl Pts',(0.810556943750001,60.8145833342893,1.40392580900275));
#4831=CARTESIAN_POINT('Ctrl Pts',(3.43862649647115E-16,60.7562500009559,
1.87190107867033));
#4832=CARTESIAN_POINT('Ctrl Pts',(-0.810556943749999,60.6979166676226,1.40392580900275));
#4833=CARTESIAN_POINT('Ctrl Pts',(-1.6211138875,60.6395833342892,0.935950539335167));
#4834=CARTESIAN_POINT('Ctrl Pts',(-1.6211138875,60.5812500009559,0.));
#4835=CARTESIAN_POINT('Ctrl Pts',(-1.6211138875,60.5229166676226,-0.935950539335166));
#4836=CARTESIAN_POINT('Ctrl Pts',(-0.81055694375,60.4645833342893,-1.40392580900275));
#4837=CARTESIAN_POINT('Ctrl Pts',(-1.14620883215705E-16,60.4062500009559,
-1.87190107867033));
#4838=CARTESIAN_POINT('Ctrl Pts',(0.81055694375,60.3479166676226,-1.40392580900275));
#4839=CARTESIAN_POINT('Ctrl Pts',(1.6211138875,60.2895833342893,-0.935950539335166));
#4840=CARTESIAN_POINT('Ctrl Pts',(1.6211138875,60.2312500009559,-1.9852919333802E-16));
#4841=CARTESIAN_POINT('Ctrl Pts',(1.6211138875,60.1729166676226,0.935950539335165));
#4842=CARTESIAN_POINT('Ctrl Pts',(0.810556943750001,60.1145833342893,1.40392580900275));
#4843=CARTESIAN_POINT('Ctrl Pts',(3.43862649647115E-16,60.0562500009559,
1.87190107867033));
#4844=CARTESIAN_POINT('Ctrl Pts',(-0.810556943749999,59.9979166676226,1.40392580900275));
#4845=CARTESIAN_POINT('Ctrl Pts',(-1.6211138875,59.9395833342893,0.935950539335167));
#4846=CARTESIAN_POINT('Ctrl Pts',(-1.6211138875,59.8812500009559,0.));
#4847=CARTESIAN_POINT('Ctrl Pts',(-1.6211138875,59.8229166676226,-0.935950539335166));
#4848=CARTESIAN_POINT('Ctrl Pts',(-0.81055694375,59.7645833342893,-1.40392580900275));
#4849=CARTESIAN_POINT('Ctrl Pts',(-1.14620883215705E-16,59.7062500009559,
-1.87190107867033));
#4850=CARTESIAN_POINT('Ctrl Pts',(0.81055694375,59.6479166676226,-1.40392580900275));
#4851=CARTESIAN_POINT('Ctrl Pts',(1.6211138875,59.5895833342893,-0.935950539335166));
#4852=CARTESIAN_POINT('Ctrl Pts',(1.6211138875,59.5312500009559,-1.9852919333802E-16));
#4853=CARTESIAN_POINT('Ctrl Pts',(1.6211138875,59.4729166676226,0.935950539335165));
#4854=CARTESIAN_POINT('Ctrl Pts',(0.810556943750001,59.4145833342893,1.40392580900275));
#4855=CARTESIAN_POINT('Ctrl Pts',(3.43862649647115E-16,59.3562500009559,
1.87190107867033));
#4856=CARTESIAN_POINT('Ctrl Pts',(-0.810556943749999,59.2979166676226,1.40392580900275));
#4857=CARTESIAN_POINT('Ctrl Pts',(-1.6211138875,59.2395833342893,0.935950539335167));
#4858=CARTESIAN_POINT('Ctrl Pts',(-1.6211138875,59.1812500009559,0.));
#4859=CARTESIAN_POINT('Ctrl Pts',(-1.6211138875,59.1229166676226,-0.935950539335166));
#4860=CARTESIAN_POINT('Ctrl Pts',(-0.81055694375,59.0645833342893,-1.40392580900275));
#4861=CARTESIAN_POINT('Ctrl Pts',(-1.14620883215705E-16,59.0062500009559,
-1.87190107867033));
#4862=CARTESIAN_POINT('Ctrl Pts',(0.81055694375,58.9479166676226,-1.40392580900275));
#4863=CARTESIAN_POINT('Ctrl Pts',(1.6211138875,58.8895833342893,-0.935950539335166));
#4864=CARTESIAN_POINT('Ctrl Pts',(1.6211138875,58.8312500009559,-1.9852919333802E-16));
#4865=CARTESIAN_POINT('Ctrl Pts',(1.6211138875,58.7729166676226,0.935950539335165));
#4866=CARTESIAN_POINT('Ctrl Pts',(0.810556943750001,58.7145833342893,1.40392580900275));
#4867=CARTESIAN_POINT('Ctrl Pts',(3.43862649647115E-16,58.6562500009559,
1.87190107867033));
#4868=CARTESIAN_POINT('Ctrl Pts',(-0.810556943749999,58.5979166676226,1.40392580900275));
#4869=CARTESIAN_POINT('Ctrl Pts',(-1.6211138875,58.5395833342892,0.935950539335167));
#4870=CARTESIAN_POINT('Ctrl Pts',(-1.6211138875,58.4812500009559,0.));
#4871=CARTESIAN_POINT('Ctrl Pts',(-1.6211138875,58.4229166676226,-0.935950539335166));
#4872=CARTESIAN_POINT('Ctrl Pts',(-0.81055694375,58.3645833342893,-1.40392580900275));
#4873=CARTESIAN_POINT('Ctrl Pts',(-1.14620883215705E-16,58.3062500009559,
-1.87190107867033));
#4874=CARTESIAN_POINT('Ctrl Pts',(0.81055694375,58.2479166676226,-1.40392580900275));
#4875=CARTESIAN_POINT('Ctrl Pts',(1.6211138875,58.1895833342893,-0.935950539335166));
#4876=CARTESIAN_POINT('Ctrl Pts',(1.6211138875,58.1312500009559,-1.9852919333802E-16));
#4877=CARTESIAN_POINT('Ctrl Pts',(1.6211138875,58.0729166676226,0.935950539335165));
#4878=CARTESIAN_POINT('Ctrl Pts',(0.810556943750001,58.0145833342893,1.40392580900275));
#4879=CARTESIAN_POINT('Ctrl Pts',(3.43862649647115E-16,57.9562500009559,
1.87190107867033));
#4880=CARTESIAN_POINT('Ctrl Pts',(-0.810556943749999,57.8979166676226,1.40392580900275));
#4881=CARTESIAN_POINT('Ctrl Pts',(-1.6211138875,57.8395833342893,0.935950539335167));
#4882=CARTESIAN_POINT('Ctrl Pts',(-1.6211138875,57.7812500009559,0.));
#4883=CARTESIAN_POINT('Ctrl Pts',(-1.6211138875,57.7229166676226,-0.935950539335166));
#4884=CARTESIAN_POINT('Ctrl Pts',(-0.81055694375,57.6645833342893,-1.40392580900275));
#4885=CARTESIAN_POINT('Ctrl Pts',(-1.14620883215705E-16,57.6062500009559,
-1.87190107867033));
#4886=CARTESIAN_POINT('Ctrl Pts',(0.81055694375,57.5479166676226,-1.40392580900275));
#4887=CARTESIAN_POINT('Ctrl Pts',(1.6211138875,57.4895833342893,-0.935950539335166));
#4888=CARTESIAN_POINT('Ctrl Pts',(1.6211138875,57.4312500009559,-1.9852919333802E-16));
#4889=CARTESIAN_POINT('Ctrl Pts',(1.6211138875,57.3729166676226,0.935950539335165));
#4890=CARTESIAN_POINT('Ctrl Pts',(0.810556943750001,57.3145833342893,1.40392580900275));
#4891=CARTESIAN_POINT('Ctrl Pts',(3.43862649647115E-16,57.2562500009559,
1.87190107867033));
#4892=CARTESIAN_POINT('Ctrl Pts',(-0.810556943749999,57.1979166676226,1.40392580900275));
#4893=CARTESIAN_POINT('Ctrl Pts',(-1.6211138875,57.1395833342893,0.935950539335167));
#4894=CARTESIAN_POINT('Ctrl Pts',(-1.6211138875,57.0812500009559,0.));
#4895=CARTESIAN_POINT('Ctrl Pts',(-1.6211138875,57.0229166676226,-0.935950539335166));
#4896=CARTESIAN_POINT('Ctrl Pts',(-0.81055694375,56.9645833342893,-1.40392580900275));
#4897=CARTESIAN_POINT('Ctrl Pts',(-1.14620883215705E-16,56.9062500009559,
-1.87190107867033));
#4898=CARTESIAN_POINT('Ctrl Pts',(0.81055694375,56.8479166676226,-1.40392580900275));
#4899=CARTESIAN_POINT('Ctrl Pts',(1.6211138875,56.7895833342892,-0.935950539335166));
#4900=CARTESIAN_POINT('Ctrl Pts',(1.6211138875,56.7312500009559,-1.9852919333802E-16));
#4901=CARTESIAN_POINT('Ctrl Pts',(1.6211138875,56.6729166676226,0.935950539335165));
#4902=CARTESIAN_POINT('Ctrl Pts',(0.810556943750001,56.6145833342893,1.40392580900275));
#4903=CARTESIAN_POINT('Ctrl Pts',(3.43862649647115E-16,56.5562500009559,
1.87190107867033));
#4904=CARTESIAN_POINT('Ctrl Pts',(-0.810556943749999,56.4979166676226,1.40392580900275));
#4905=CARTESIAN_POINT('Ctrl Pts',(-1.6211138875,56.4395833342893,0.935950539335167));
#4906=CARTESIAN_POINT('Ctrl Pts',(-1.6211138875,56.3812500009559,0.));
#4907=CARTESIAN_POINT('Ctrl Pts',(-1.6211138875,56.3229166676226,-0.935950539335166));
#4908=CARTESIAN_POINT('Ctrl Pts',(-0.81055694375,56.2645833342893,-1.40392580900275));
#4909=CARTESIAN_POINT('Ctrl Pts',(-1.14620883215705E-16,56.2062500009559,
-1.87190107867033));
#4910=CARTESIAN_POINT('Ctrl Pts',(0.81055694375,56.1479166676226,-1.40392580900275));
#4911=CARTESIAN_POINT('Ctrl Pts',(1.6211138875,56.0895833342893,-0.935950539335166));
#4912=CARTESIAN_POINT('Ctrl Pts',(1.6211138875,56.0312500009559,-1.9852919333802E-16));
#4913=CARTESIAN_POINT('Ctrl Pts',(1.6211138875,55.9729166676226,0.935950539335165));
#4914=CARTESIAN_POINT('Ctrl Pts',(0.810556943750001,55.9145833342893,1.40392580900275));
#4915=CARTESIAN_POINT('Ctrl Pts',(3.43862649647115E-16,55.8562500009559,
1.87190107867033));
#4916=CARTESIAN_POINT('Ctrl Pts',(-0.810556943749999,55.7979166676226,1.40392580900275));
#4917=CARTESIAN_POINT('Ctrl Pts',(-1.6211138875,55.7395833342893,0.935950539335167));
#4918=CARTESIAN_POINT('Ctrl Pts',(-1.6211138875,55.6812500009559,0.));
#4919=CARTESIAN_POINT('Ctrl Pts',(-1.6211138875,55.6229166676226,-0.935950539335166));
#4920=CARTESIAN_POINT('Ctrl Pts',(-0.81055694375,55.5645833342893,-1.40392580900275));
#4921=CARTESIAN_POINT('Ctrl Pts',(-1.14620883215705E-16,55.5062500009559,
-1.87190107867033));
#4922=CARTESIAN_POINT('Ctrl Pts',(0.81055694375,55.4479166676226,-1.40392580900275));
#4923=CARTESIAN_POINT('Ctrl Pts',(1.6211138875,55.3895833342893,-0.935950539335166));
#4924=CARTESIAN_POINT('Ctrl Pts',(1.6211138875,55.3312500009559,-1.9852919333802E-16));
#4925=CARTESIAN_POINT('Ctrl Pts',(1.6211138875,55.2729166676226,0.935950539335165));
#4926=CARTESIAN_POINT('Ctrl Pts',(0.810556943750001,55.2145833342893,1.40392580900275));
#4927=CARTESIAN_POINT('Ctrl Pts',(3.43862649647115E-16,55.1562500009559,
1.87190107867033));
#4928=CARTESIAN_POINT('Ctrl Pts',(-0.810556943749999,55.0979166676226,1.40392580900275));
#4929=CARTESIAN_POINT('Ctrl Pts',(-1.6211138875,55.0395833342893,0.935950539335167));
#4930=CARTESIAN_POINT('Ctrl Pts',(-1.6211138875,54.9812500009559,0.));
#4931=CARTESIAN_POINT('Ctrl Pts',(-1.6211138875,54.9229166676226,-0.935950539335166));
#4932=CARTESIAN_POINT('Ctrl Pts',(-0.81055694375,54.8645833342893,-1.40392580900275));
#4933=CARTESIAN_POINT('Ctrl Pts',(-1.14620883215705E-16,54.8062500009559,
-1.87190107867033));
#4934=CARTESIAN_POINT('Ctrl Pts',(0.81055694375,54.7479166676226,-1.40392580900275));
#4935=CARTESIAN_POINT('Ctrl Pts',(1.6211138875,54.6895833342893,-0.935950539335166));
#4936=CARTESIAN_POINT('Ctrl Pts',(1.6211138875,54.6312500009559,-1.9852919333802E-16));
#4937=CARTESIAN_POINT('Ctrl Pts',(1.6211138875,54.5729166676226,0.935950539335165));
#4938=CARTESIAN_POINT('Ctrl Pts',(0.810556943750001,54.5145833342893,1.40392580900275));
#4939=CARTESIAN_POINT('Ctrl Pts',(3.43862649647115E-16,54.4562500009559,
1.87190107867033));
#4940=CARTESIAN_POINT('Ctrl Pts',(-0.810556943749999,54.3979166676226,1.40392580900275));
#4941=CARTESIAN_POINT('Ctrl Pts',(-1.6211138875,54.3395833342893,0.935950539335167));
#4942=CARTESIAN_POINT('Ctrl Pts',(-1.6211138875,54.2812500009559,0.));
#4943=CARTESIAN_POINT('Ctrl Pts',(-1.6211138875,54.2229166676226,-0.935950539335166));
#4944=CARTESIAN_POINT('Ctrl Pts',(-0.81055694375,54.1645833342893,-1.40392580900275));
#4945=CARTESIAN_POINT('Ctrl Pts',(-1.14620883215705E-16,54.1062500009559,
-1.87190107867033));
#4946=CARTESIAN_POINT('Ctrl Pts',(0.81055694375,54.0479166676226,-1.40392580900275));
#4947=CARTESIAN_POINT('Ctrl Pts',(1.6211138875,53.9895833342893,-0.935950539335166));
#4948=CARTESIAN_POINT('Ctrl Pts',(1.6211138875,53.9312500009559,-1.9852919333802E-16));
#4949=CARTESIAN_POINT('Ctrl Pts',(1.6211138875,53.8729166676226,0.935950539335165));
#4950=CARTESIAN_POINT('Ctrl Pts',(0.810556943750001,53.8145833342893,1.40392580900275));
#4951=CARTESIAN_POINT('Ctrl Pts',(3.43862649647115E-16,53.7562500009559,
1.87190107867033));
#4952=CARTESIAN_POINT('Ctrl Pts',(-0.810556943749999,53.6979166676226,1.40392580900275));
#4953=CARTESIAN_POINT('Ctrl Pts',(-1.6211138875,53.6395833342893,0.935950539335167));
#4954=CARTESIAN_POINT('Ctrl Pts',(-1.6211138875,53.5812500009559,0.));
#4955=CARTESIAN_POINT('Ctrl Pts',(-1.6211138875,53.5229166676226,-0.935950539335166));
#4956=CARTESIAN_POINT('Ctrl Pts',(-0.81055694375,53.4645833342893,-1.40392580900275));
#4957=CARTESIAN_POINT('Ctrl Pts',(-1.14620883215705E-16,53.4062500009559,
-1.87190107867033));
#4958=CARTESIAN_POINT('Ctrl Pts',(0.81055694375,53.3479166676226,-1.40392580900275));
#4959=CARTESIAN_POINT('Ctrl Pts',(1.6211138875,53.2895833342893,-0.935950539335166));
#4960=CARTESIAN_POINT('Ctrl Pts',(1.6211138875,53.2312500009559,-1.9852919333802E-16));
#4961=CARTESIAN_POINT('Ctrl Pts',(1.6211138875,53.1729166676226,0.935950539335165));
#4962=CARTESIAN_POINT('Ctrl Pts',(0.810556943750001,53.1145833342893,1.40392580900275));
#4963=CARTESIAN_POINT('Ctrl Pts',(3.43862649647115E-16,53.0562500009559,
1.87190107867033));
#4964=CARTESIAN_POINT('Ctrl Pts',(-0.810556943749999,52.9979166676226,1.40392580900275));
#4965=CARTESIAN_POINT('Ctrl Pts',(-1.6211138875,52.9395833342893,0.935950539335167));
#4966=CARTESIAN_POINT('Ctrl Pts',(-1.6211138875,52.8812500009559,0.));
#4967=CARTESIAN_POINT('Ctrl Pts',(-1.6211138875,52.8229166676226,-0.935950539335166));
#4968=CARTESIAN_POINT('Ctrl Pts',(-0.81055694375,52.7645833342893,-1.40392580900275));
#4969=CARTESIAN_POINT('Ctrl Pts',(-1.14620883215705E-16,52.7062500009559,
-1.87190107867033));
#4970=CARTESIAN_POINT('Ctrl Pts',(0.81055694375,52.6479166676226,-1.40392580900275));
#4971=CARTESIAN_POINT('Ctrl Pts',(1.6211138875,52.5895833342892,-0.935950539335166));
#4972=CARTESIAN_POINT('Ctrl Pts',(1.6211138875,52.5312500009559,-1.9852919333802E-16));
#4973=CARTESIAN_POINT('Ctrl Pts',(1.6211138875,52.4729166676226,0.935950539335165));
#4974=CARTESIAN_POINT('Ctrl Pts',(0.810556943750001,52.4145833342892,1.40392580900275));
#4975=CARTESIAN_POINT('Ctrl Pts',(3.43862649647115E-16,52.3562500009559,
1.87190107867033));
#4976=CARTESIAN_POINT('Ctrl Pts',(-0.810556943749999,52.2979166676226,1.40392580900275));
#4977=CARTESIAN_POINT('Ctrl Pts',(-1.6211138875,52.2395833342893,0.935950539335167));
#4978=CARTESIAN_POINT('Ctrl Pts',(-1.6211138875,52.1812500009559,0.));
#4979=CARTESIAN_POINT('Ctrl Pts',(-1.6211138875,52.1229166676226,-0.935950539335166));
#4980=CARTESIAN_POINT('Ctrl Pts',(-0.81055694375,52.0645833342893,-1.40392580900275));
#4981=CARTESIAN_POINT('Ctrl Pts',(-1.14620883215705E-16,52.0062500009559,
-1.87190107867033));
#4982=CARTESIAN_POINT('Ctrl Pts',(0.81055694375,51.9479166676226,-1.40392580900275));
#4983=CARTESIAN_POINT('Ctrl Pts',(1.6211138875,51.8895833342892,-0.935950539335166));
#4984=CARTESIAN_POINT('Ctrl Pts',(1.6211138875,51.8312500009559,-1.9852919333802E-16));
#4985=CARTESIAN_POINT('Ctrl Pts',(1.6211138875,51.7729166676226,0.935950539335165));
#4986=CARTESIAN_POINT('Ctrl Pts',(0.810556943750001,51.7145833342893,1.40392580900275));
#4987=CARTESIAN_POINT('Ctrl Pts',(3.43862649647115E-16,51.6562500009559,
1.87190107867033));
#4988=CARTESIAN_POINT('Ctrl Pts',(-0.810556943749999,51.5979166676226,1.40392580900275));
#4989=CARTESIAN_POINT('Ctrl Pts',(-1.6211138875,51.5395833342893,0.935950539335167));
#4990=CARTESIAN_POINT('Ctrl Pts',(-1.6211138875,51.4812500009559,0.));
#4991=CARTESIAN_POINT('Ctrl Pts',(-1.6211138875,51.4229166676226,-0.935950539335166));
#4992=CARTESIAN_POINT('Ctrl Pts',(-0.81055694375,51.3645833342893,-1.40392580900275));
#4993=CARTESIAN_POINT('Ctrl Pts',(-1.14620883215705E-16,51.3062500009559,
-1.87190107867033));
#4994=CARTESIAN_POINT('Ctrl Pts',(0.81055694375,51.2479166676226,-1.40392580900275));
#4995=CARTESIAN_POINT('Ctrl Pts',(1.6211138875,51.1895833342892,-0.935950539335166));
#4996=CARTESIAN_POINT('Ctrl Pts',(1.6211138875,51.1312500009559,-1.9852919333802E-16));
#4997=CARTESIAN_POINT('Ctrl Pts',(1.6211138875,51.0729166676226,0.935950539335165));
#4998=CARTESIAN_POINT('Ctrl Pts',(0.810556943750001,51.0145833342893,1.40392580900275));
#4999=CARTESIAN_POINT('Ctrl Pts',(3.43862649647115E-16,50.9562500009559,
1.87190107867033));
#5000=CARTESIAN_POINT('Ctrl Pts',(-0.810556943749999,50.8979166676226,1.40392580900275));
#5001=CARTESIAN_POINT('Ctrl Pts',(-1.6211138875,50.8395833342893,0.935950539335167));
#5002=CARTESIAN_POINT('Ctrl Pts',(-1.6211138875,50.7812500009559,0.));
#5003=CARTESIAN_POINT('Ctrl Pts',(-1.6211138875,50.7229166676226,-0.935950539335166));
#5004=CARTESIAN_POINT('Ctrl Pts',(-0.81055694375,50.6645833342893,-1.40392580900275));
#5005=CARTESIAN_POINT('Ctrl Pts',(-1.14620883215705E-16,50.6062500009559,
-1.87190107867033));
#5006=CARTESIAN_POINT('Ctrl Pts',(0.81055694375,50.5479166676226,-1.40392580900275));
#5007=CARTESIAN_POINT('Ctrl Pts',(1.6211138875,50.4895833342893,-0.935950539335166));
#5008=CARTESIAN_POINT('Ctrl Pts',(1.6211138875,50.4312500009559,-1.9852919333802E-16));
#5009=CARTESIAN_POINT('Ctrl Pts',(1.6211138875,50.3729166676226,0.935950539335165));
#5010=CARTESIAN_POINT('Ctrl Pts',(0.810556943750001,50.3145833342893,1.40392580900275));
#5011=CARTESIAN_POINT('Ctrl Pts',(3.43862649647115E-16,50.2562500009559,
1.87190107867033));
#5012=CARTESIAN_POINT('Ctrl Pts',(-0.810556943749999,50.1979166676226,1.40392580900275));
#5013=CARTESIAN_POINT('Ctrl Pts',(-1.6211138875,50.1395833342892,0.935950539335167));
#5014=CARTESIAN_POINT('Ctrl Pts',(-1.6211138875,50.0812500009559,0.));
#5015=CARTESIAN_POINT('Ctrl Pts',(-1.6211138875,50.0229166676226,-0.935950539335166));
#5016=CARTESIAN_POINT('Ctrl Pts',(-0.81055694375,49.9645833342893,-1.40392580900275));
#5017=CARTESIAN_POINT('Ctrl Pts',(-1.14620883215705E-16,49.9062500009559,
-1.87190107867033));
#5018=CARTESIAN_POINT('Ctrl Pts',(0.81055694375,49.8479166676226,-1.40392580900275));
#5019=CARTESIAN_POINT('Ctrl Pts',(1.6211138875,49.7895833342893,-0.935950539335166));
#5020=CARTESIAN_POINT('Ctrl Pts',(1.6211138875,49.7312500009559,-1.9852919333802E-16));
#5021=CARTESIAN_POINT('Ctrl Pts',(1.6211138875,49.6729166676226,0.935950539335165));
#5022=CARTESIAN_POINT('Ctrl Pts',(0.810556943750001,49.6145833342893,1.40392580900275));
#5023=CARTESIAN_POINT('Ctrl Pts',(3.43862649647115E-16,49.5562500009559,
1.87190107867033));
#5024=CARTESIAN_POINT('Ctrl Pts',(-0.810556943749999,49.4979166676226,1.40392580900275));
#5025=CARTESIAN_POINT('Ctrl Pts',(-1.6211138875,49.4395833342893,0.935950539335167));
#5026=CARTESIAN_POINT('Ctrl Pts',(-1.6211138875,49.3812500009559,0.));
#5027=CARTESIAN_POINT('Ctrl Pts',(-1.6211138875,49.3229166676226,-0.935950539335166));
#5028=CARTESIAN_POINT('Ctrl Pts',(-0.81055694375,49.2645833342893,-1.40392580900275));
#5029=CARTESIAN_POINT('Ctrl Pts',(-1.14620883215705E-16,49.2062500009559,
-1.87190107867033));
#5030=CARTESIAN_POINT('Ctrl Pts',(0.81055694375,49.1479166676226,-1.40392580900275));
#5031=CARTESIAN_POINT('Ctrl Pts',(1.6211138875,49.0895833342893,-0.935950539335166));
#5032=CARTESIAN_POINT('Ctrl Pts',(1.6211138875,49.0312500009559,-1.9852919333802E-16));
#5033=CARTESIAN_POINT('Ctrl Pts',(1.6211138875,48.9729166676226,0.935950539335165));
#5034=CARTESIAN_POINT('Ctrl Pts',(0.810556943750001,48.9145833342893,1.40392580900275));
#5035=CARTESIAN_POINT('Ctrl Pts',(3.43862649647115E-16,48.8562500009559,
1.87190107867033));
#5036=CARTESIAN_POINT('Ctrl Pts',(-0.810556943749999,48.7979166676226,1.40392580900275));
#5037=CARTESIAN_POINT('Ctrl Pts',(-1.6211138875,48.7395833342893,0.935950539335167));
#5038=CARTESIAN_POINT('Ctrl Pts',(-1.6211138875,48.6812500009559,0.));
#5039=CARTESIAN_POINT('Ctrl Pts',(-1.6211138875,48.6229166676226,-0.935950539335166));
#5040=CARTESIAN_POINT('Ctrl Pts',(-0.81055694375,48.5645833342893,-1.40392580900275));
#5041=CARTESIAN_POINT('Ctrl Pts',(-1.14620883215705E-16,48.5062500009559,
-1.87190107867033));
#5042=CARTESIAN_POINT('Ctrl Pts',(0.81055694375,48.4479166676226,-1.40392580900275));
#5043=CARTESIAN_POINT('Ctrl Pts',(1.6211138875,48.3895833342893,-0.935950539335166));
#5044=CARTESIAN_POINT('Ctrl Pts',(1.6211138875,48.3312500009559,-1.9852919333802E-16));
#5045=CARTESIAN_POINT('Ctrl Pts',(1.6211138875,48.2729166676226,0.935950539335165));
#5046=CARTESIAN_POINT('Ctrl Pts',(0.810556943750001,48.2145833342893,1.40392580900275));
#5047=CARTESIAN_POINT('Ctrl Pts',(3.43862649647115E-16,48.1562500009559,
1.87190107867033));
#5048=CARTESIAN_POINT('Ctrl Pts',(-0.810556943749999,48.0979166676226,1.40392580900275));
#5049=CARTESIAN_POINT('Ctrl Pts',(-1.6211138875,48.0395833342893,0.935950539335167));
#5050=CARTESIAN_POINT('Ctrl Pts',(-1.6211138875,47.9812500009559,0.));
#5051=CARTESIAN_POINT('Ctrl Pts',(-1.6211138875,47.9229166676226,-0.935950539335166));
#5052=CARTESIAN_POINT('Ctrl Pts',(-0.81055694375,47.8645833342893,-1.40392580900275));
#5053=CARTESIAN_POINT('Ctrl Pts',(-1.14620883215705E-16,47.8062500009559,
-1.87190107867033));
#5054=CARTESIAN_POINT('Ctrl Pts',(0.81055694375,47.7479166676226,-1.40392580900275));
#5055=CARTESIAN_POINT('Ctrl Pts',(1.6211138875,47.6895833342893,-0.935950539335166));
#5056=CARTESIAN_POINT('Ctrl Pts',(1.6211138875,47.6312500009559,-1.9852919333802E-16));
#5057=CARTESIAN_POINT('Ctrl Pts',(1.6211138875,47.5729166676226,0.935950539335165));
#5058=CARTESIAN_POINT('Ctrl Pts',(0.810556943750001,47.5145833342893,1.40392580900275));
#5059=CARTESIAN_POINT('Ctrl Pts',(3.43862649647115E-16,47.4562500009559,
1.87190107867033));
#5060=CARTESIAN_POINT('Ctrl Pts',(-0.810556943749999,47.3979166676226,1.40392580900275));
#5061=CARTESIAN_POINT('Ctrl Pts',(-1.6211138875,47.3395833342893,0.935950539335167));
#5062=CARTESIAN_POINT('Ctrl Pts',(-1.6211138875,47.2812500009559,0.));
#5063=CARTESIAN_POINT('Ctrl Pts',(-1.6211138875,47.2229166676226,-0.935950539335166));
#5064=CARTESIAN_POINT('Ctrl Pts',(-0.81055694375,47.1645833342893,-1.40392580900275));
#5065=CARTESIAN_POINT('Ctrl Pts',(-1.14620883215705E-16,47.1062500009559,
-1.87190107867033));
#5066=CARTESIAN_POINT('Ctrl Pts',(0.81055694375,47.0479166676226,-1.40392580900275));
#5067=CARTESIAN_POINT('Ctrl Pts',(1.6211138875,46.9895833342893,-0.935950539335166));
#5068=CARTESIAN_POINT('Ctrl Pts',(1.6211138875,46.9312500009559,-1.9852919333802E-16));
#5069=CARTESIAN_POINT('Ctrl Pts',(1.6211138875,46.8729166676226,0.935950539335165));
#5070=CARTESIAN_POINT('Ctrl Pts',(0.810556943750001,46.8145833342893,1.40392580900275));
#5071=CARTESIAN_POINT('Ctrl Pts',(3.43862649647115E-16,46.7562500009559,
1.87190107867033));
#5072=CARTESIAN_POINT('Ctrl Pts',(-0.810556943749999,46.6979166676226,1.40392580900275));
#5073=CARTESIAN_POINT('Ctrl Pts',(-1.6211138875,46.6395833342893,0.935950539335167));
#5074=CARTESIAN_POINT('Ctrl Pts',(-1.6211138875,46.5812500009559,0.));
#5075=CARTESIAN_POINT('Ctrl Pts',(-1.6211138875,46.5229166676226,-0.935950539335166));
#5076=CARTESIAN_POINT('Ctrl Pts',(-0.81055694375,46.4645833342893,-1.40392580900275));
#5077=CARTESIAN_POINT('Ctrl Pts',(-1.14620883215705E-16,46.4062500009559,
-1.87190107867033));
#5078=CARTESIAN_POINT('Ctrl Pts',(0.81055694375,46.3479166676226,-1.40392580900275));
#5079=CARTESIAN_POINT('Ctrl Pts',(1.6211138875,46.2895833342893,-0.935950539335166));
#5080=CARTESIAN_POINT('Ctrl Pts',(1.6211138875,46.2312500009559,-1.9852919333802E-16));
#5081=CARTESIAN_POINT('Ctrl Pts',(1.6211138875,46.1729166676226,0.935950539335165));
#5082=CARTESIAN_POINT('Ctrl Pts',(0.810556943750001,46.1145833342893,1.40392580900275));
#5083=CARTESIAN_POINT('Ctrl Pts',(3.43862649647115E-16,46.0562500009559,
1.87190107867033));
#5084=CARTESIAN_POINT('Ctrl Pts',(-0.810556943749999,45.9979166676226,1.40392580900275));
#5085=CARTESIAN_POINT('Ctrl Pts',(-1.6211138875,45.9395833342893,0.935950539335167));
#5086=CARTESIAN_POINT('Ctrl Pts',(-1.6211138875,45.8812500009559,0.));
#5087=CARTESIAN_POINT('Ctrl Pts',(-1.6211138875,45.8229166676226,-0.935950539335166));
#5088=CARTESIAN_POINT('Ctrl Pts',(-0.81055694375,45.7645833342893,-1.40392580900275));
#5089=CARTESIAN_POINT('Ctrl Pts',(-1.14620883215705E-16,45.7062500009559,
-1.87190107867033));
#5090=CARTESIAN_POINT('Ctrl Pts',(0.81055694375,45.6479166676226,-1.40392580900275));
#5091=CARTESIAN_POINT('Ctrl Pts',(1.6211138875,45.5895833342893,-0.935950539335166));
#5092=CARTESIAN_POINT('Ctrl Pts',(1.6211138875,45.5312500009559,-1.9852919333802E-16));
#5093=CARTESIAN_POINT('Ctrl Pts',(1.6211138875,45.4729166676226,0.935950539335165));
#5094=CARTESIAN_POINT('Ctrl Pts',(0.810556943750001,45.4145833342893,1.40392580900275));
#5095=CARTESIAN_POINT('Ctrl Pts',(3.43862649647115E-16,45.3562500009559,
1.87190107867033));
#5096=CARTESIAN_POINT('Ctrl Pts',(-0.810556943749999,45.2979166676226,1.40392580900275));
#5097=CARTESIAN_POINT('Ctrl Pts',(-1.6211138875,45.2395833342893,0.935950539335167));
#5098=CARTESIAN_POINT('Ctrl Pts',(-1.6211138875,45.1812500009559,0.));
#5099=CARTESIAN_POINT('Ctrl Pts',(-1.6211138875,45.1229166676226,-0.935950539335166));
#5100=CARTESIAN_POINT('Ctrl Pts',(-0.81055694375,45.0645833342893,-1.40392580900275));
#5101=CARTESIAN_POINT('Ctrl Pts',(-1.14620883215705E-16,45.0062500009559,
-1.87190107867033));
#5102=CARTESIAN_POINT('Ctrl Pts',(0.81055694375,44.9479166676226,-1.40392580900275));
#5103=CARTESIAN_POINT('Ctrl Pts',(1.6211138875,44.8895833342893,-0.935950539335166));
#5104=CARTESIAN_POINT('Ctrl Pts',(1.6211138875,44.8312500009559,-1.9852919333802E-16));
#5105=CARTESIAN_POINT('Ctrl Pts',(1.6211138875,44.7729166676226,0.935950539335165));
#5106=CARTESIAN_POINT('Ctrl Pts',(0.810556943750001,44.7145833342893,1.40392580900275));
#5107=CARTESIAN_POINT('Ctrl Pts',(3.43862649647115E-16,44.6562500009559,
1.87190107867033));
#5108=CARTESIAN_POINT('Ctrl Pts',(-0.810556943749999,44.5979166676226,1.40392580900275));
#5109=CARTESIAN_POINT('Ctrl Pts',(-1.6211138875,44.5395833342893,0.935950539335167));
#5110=CARTESIAN_POINT('Ctrl Pts',(-1.6211138875,44.4812500009559,0.));
#5111=CARTESIAN_POINT('Ctrl Pts',(-1.6211138875,44.4229166676226,-0.935950539335166));
#5112=CARTESIAN_POINT('Ctrl Pts',(-0.81055694375,44.3645833342893,-1.40392580900275));
#5113=CARTESIAN_POINT('Ctrl Pts',(-1.14620883215705E-16,44.3062500009559,
-1.87190107867033));
#5114=CARTESIAN_POINT('Ctrl Pts',(0.81055694375,44.2479166676226,-1.40392580900275));
#5115=CARTESIAN_POINT('Ctrl Pts',(1.6211138875,44.1895833342893,-0.935950539335166));
#5116=CARTESIAN_POINT('Ctrl Pts',(1.6211138875,44.1312500009559,-1.9852919333802E-16));
#5117=CARTESIAN_POINT('Ctrl Pts',(1.6211138875,44.0729166676226,0.935950539335165));
#5118=CARTESIAN_POINT('Ctrl Pts',(0.810556943750001,44.0145833342893,1.40392580900275));
#5119=CARTESIAN_POINT('Ctrl Pts',(3.43862649647115E-16,43.9562500009559,
1.87190107867033));
#5120=CARTESIAN_POINT('Ctrl Pts',(-0.810556943749999,43.8979166676226,1.40392580900275));
#5121=CARTESIAN_POINT('Ctrl Pts',(-1.6211138875,43.8395833342893,0.935950539335167));
#5122=CARTESIAN_POINT('Ctrl Pts',(-1.6211138875,43.7812500009559,0.));
#5123=CARTESIAN_POINT('Ctrl Pts',(-1.6211138875,43.7229166676226,-0.935950539335166));
#5124=CARTESIAN_POINT('Ctrl Pts',(-0.81055694375,43.6645833342893,-1.40392580900275));
#5125=CARTESIAN_POINT('Ctrl Pts',(-1.14620883215705E-16,43.6062500009559,
-1.87190107867033));
#5126=CARTESIAN_POINT('Ctrl Pts',(0.81055694375,43.5479166676226,-1.40392580900275));
#5127=CARTESIAN_POINT('Ctrl Pts',(1.6211138875,43.4895833342893,-0.935950539335166));
#5128=CARTESIAN_POINT('Ctrl Pts',(1.6211138875,43.4312500009559,-1.9852919333802E-16));
#5129=CARTESIAN_POINT('Ctrl Pts',(1.6211138875,43.3729166676226,0.935950539335165));
#5130=CARTESIAN_POINT('Ctrl Pts',(0.810556943750001,43.3145833342893,1.40392580900275));
#5131=CARTESIAN_POINT('Ctrl Pts',(3.43862649647115E-16,43.2562500009559,
1.87190107867033));
#5132=CARTESIAN_POINT('Ctrl Pts',(-0.810556943749999,43.1979166676226,1.40392580900275));
#5133=CARTESIAN_POINT('Ctrl Pts',(-1.6211138875,43.1395833342893,0.935950539335167));
#5134=CARTESIAN_POINT('Ctrl Pts',(-1.6211138875,43.0812500009559,0.));
#5135=CARTESIAN_POINT('Ctrl Pts',(-1.6211138875,43.0229166676226,-0.935950539335166));
#5136=CARTESIAN_POINT('Ctrl Pts',(-0.81055694375,42.9645833342893,-1.40392580900275));
#5137=CARTESIAN_POINT('Ctrl Pts',(-1.14620883215705E-16,42.9062500009559,
-1.87190107867033));
#5138=CARTESIAN_POINT('Ctrl Pts',(0.81055694375,42.8479166676226,-1.40392580900275));
#5139=CARTESIAN_POINT('Ctrl Pts',(1.6211138875,42.7895833342893,-0.935950539335166));
#5140=CARTESIAN_POINT('Ctrl Pts',(1.6211138875,42.7312500009559,-1.9852919333802E-16));
#5141=CARTESIAN_POINT('Ctrl Pts',(1.6211138875,42.6729166676226,0.935950539335165));
#5142=CARTESIAN_POINT('Ctrl Pts',(0.810556943750001,42.6145833342893,1.40392580900275));
#5143=CARTESIAN_POINT('Ctrl Pts',(3.43862649647115E-16,42.5562500009559,
1.87190107867033));
#5144=CARTESIAN_POINT('Ctrl Pts',(-0.810556943749999,42.4979166676226,1.40392580900275));
#5145=CARTESIAN_POINT('Ctrl Pts',(-1.6211138875,42.4395833342892,0.935950539335167));
#5146=CARTESIAN_POINT('Ctrl Pts',(-1.6211138875,42.3812500009559,0.));
#5147=CARTESIAN_POINT('Ctrl Pts',(-1.6211138875,42.3229166676226,-0.935950539335166));
#5148=CARTESIAN_POINT('Ctrl Pts',(-0.81055694375,42.2645833342893,-1.40392580900275));
#5149=CARTESIAN_POINT('Ctrl Pts',(-1.14620883215705E-16,42.2062500009559,
-1.87190107867033));
#5150=CARTESIAN_POINT('Ctrl Pts',(0.81055694375,42.1479166676226,-1.40392580900275));
#5151=CARTESIAN_POINT('Ctrl Pts',(1.6211138875,42.0895833342893,-0.935950539335166));
#5152=CARTESIAN_POINT('Ctrl Pts',(1.6211138875,42.0312500009559,-1.9852919333802E-16));
#5153=CARTESIAN_POINT('Ctrl Pts',(1.6211138875,41.9729166676226,0.935950539335165));
#5154=CARTESIAN_POINT('Ctrl Pts',(0.810556943750001,41.9145833342893,1.40392580900275));
#5155=CARTESIAN_POINT('Ctrl Pts',(3.43862649647115E-16,41.8562500009559,
1.87190107867033));
#5156=CARTESIAN_POINT('Ctrl Pts',(-0.810556943749999,41.7979166676226,1.40392580900275));
#5157=CARTESIAN_POINT('Ctrl Pts',(-1.6211138875,41.7395833342893,0.935950539335167));
#5158=CARTESIAN_POINT('Ctrl Pts',(-1.6211138875,41.6812500009559,0.));
#5159=CARTESIAN_POINT('Ctrl Pts',(-1.6211138875,41.6229166676226,-0.935950539335166));
#5160=CARTESIAN_POINT('Ctrl Pts',(-0.81055694375,41.5645833342893,-1.40392580900275));
#5161=CARTESIAN_POINT('Ctrl Pts',(-1.14620883215705E-16,41.5062500009559,
-1.87190107867033));
#5162=CARTESIAN_POINT('Ctrl Pts',(0.81055694375,41.4479166676226,-1.40392580900275));
#5163=CARTESIAN_POINT('Ctrl Pts',(1.6211138875,41.3895833342893,-0.935950539335166));
#5164=CARTESIAN_POINT('Ctrl Pts',(1.6211138875,41.3312500009559,-1.9852919333802E-16));
#5165=CARTESIAN_POINT('Ctrl Pts',(1.6211138875,41.2729166676226,0.935950539335165));
#5166=CARTESIAN_POINT('Ctrl Pts',(0.810556943750001,41.2145833342893,1.40392580900275));
#5167=CARTESIAN_POINT('Ctrl Pts',(3.43862649647115E-16,41.1562500009559,
1.87190107867033));
#5168=CARTESIAN_POINT('Ctrl Pts',(-0.810556943749999,41.0979166676226,1.40392580900275));
#5169=CARTESIAN_POINT('Ctrl Pts',(-1.6211138875,41.0395833342892,0.935950539335167));
#5170=CARTESIAN_POINT('Ctrl Pts',(-1.6211138875,40.9812500009559,0.));
#5171=CARTESIAN_POINT('Ctrl Pts',(-1.6211138875,40.9229166676226,-0.935950539335166));
#5172=CARTESIAN_POINT('Ctrl Pts',(-0.81055694375,40.8645833342893,-1.40392580900275));
#5173=CARTESIAN_POINT('Ctrl Pts',(-1.14620883215705E-16,40.8062500009559,
-1.87190107867033));
#5174=CARTESIAN_POINT('Ctrl Pts',(0.81055694375,40.7479166676226,-1.40392580900275));
#5175=CARTESIAN_POINT('Ctrl Pts',(1.6211138875,40.6895833342893,-0.935950539335166));
#5176=CARTESIAN_POINT('Ctrl Pts',(1.6211138875,40.6312500009559,-1.9852919333802E-16));
#5177=CARTESIAN_POINT('Ctrl Pts',(1.6211138875,40.5729166676226,0.935950539335165));
#5178=CARTESIAN_POINT('Ctrl Pts',(0.810556943750001,40.5145833342893,1.40392580900275));
#5179=CARTESIAN_POINT('Ctrl Pts',(3.43862649647115E-16,40.4562500009559,
1.87190107867033));
#5180=CARTESIAN_POINT('Ctrl Pts',(-0.810556943749999,40.3979166676226,1.40392580900275));
#5181=CARTESIAN_POINT('Ctrl Pts',(-1.6211138875,40.3395833342893,0.935950539335167));
#5182=CARTESIAN_POINT('Ctrl Pts',(-1.6211138875,40.2812500009559,0.));
#5183=CARTESIAN_POINT('Ctrl Pts',(-1.6211138875,40.2229166676226,-0.935950539335166));
#5184=CARTESIAN_POINT('Ctrl Pts',(-0.81055694375,40.1645833342893,-1.40392580900275));
#5185=CARTESIAN_POINT('Ctrl Pts',(-1.14620883215705E-16,40.1062500009559,
-1.87190107867033));
#5186=CARTESIAN_POINT('Ctrl Pts',(0.81055694375,40.0479166676226,-1.40392580900275));
#5187=CARTESIAN_POINT('Ctrl Pts',(1.6211138875,39.9895833342893,-0.935950539335166));
#5188=CARTESIAN_POINT('Ctrl Pts',(1.6211138875,39.9312500009559,-1.9852919333802E-16));
#5189=CARTESIAN_POINT('Ctrl Pts',(1.6211138875,39.8729166676226,0.935950539335165));
#5190=CARTESIAN_POINT('Ctrl Pts',(0.810556943750001,39.8145833342893,1.40392580900275));
#5191=CARTESIAN_POINT('Ctrl Pts',(3.43862649647115E-16,39.7562500009559,
1.87190107867033));
#5192=CARTESIAN_POINT('Ctrl Pts',(-0.810556943749999,39.6979166676226,1.40392580900275));
#5193=CARTESIAN_POINT('Ctrl Pts',(-1.6211138875,39.6395833342893,0.935950539335167));
#5194=CARTESIAN_POINT('Ctrl Pts',(-1.6211138875,39.5812500009559,0.));
#5195=CARTESIAN_POINT('Ctrl Pts',(-1.6211138875,39.5229166676226,-0.935950539335166));
#5196=CARTESIAN_POINT('Ctrl Pts',(-0.81055694375,39.4645833342893,-1.40392580900275));
#5197=CARTESIAN_POINT('Ctrl Pts',(-1.14620883215705E-16,39.4062500009559,
-1.87190107867033));
#5198=CARTESIAN_POINT('Ctrl Pts',(0.81055694375,39.3479166676226,-1.40392580900275));
#5199=CARTESIAN_POINT('Ctrl Pts',(1.6211138875,39.2895833342892,-0.935950539335166));
#5200=CARTESIAN_POINT('Ctrl Pts',(1.6211138875,39.2312500009559,-1.9852919333802E-16));
#5201=CARTESIAN_POINT('Ctrl Pts',(1.6211138875,39.1729166676226,0.935950539335165));
#5202=CARTESIAN_POINT('Ctrl Pts',(0.810556943750001,39.1145833342893,1.40392580900275));
#5203=CARTESIAN_POINT('Ctrl Pts',(3.43862649647115E-16,39.0562500009559,
1.87190107867033));
#5204=CARTESIAN_POINT('Ctrl Pts',(-0.810556943749999,38.9979166676226,1.40392580900275));
#5205=CARTESIAN_POINT('Ctrl Pts',(-1.6211138875,38.9395833342893,0.935950539335167));
#5206=CARTESIAN_POINT('Ctrl Pts',(-1.6211138875,38.8812500009559,0.));
#5207=CARTESIAN_POINT('Ctrl Pts',(-1.6211138875,38.8229166676226,-0.935950539335166));
#5208=CARTESIAN_POINT('Ctrl Pts',(-0.81055694375,38.7645833342893,-1.40392580900275));
#5209=CARTESIAN_POINT('Ctrl Pts',(-1.14620883215705E-16,38.7062500009559,
-1.87190107867033));
#5210=CARTESIAN_POINT('Ctrl Pts',(0.81055694375,38.6479166676226,-1.40392580900275));
#5211=CARTESIAN_POINT('Ctrl Pts',(1.6211138875,38.5895833342893,-0.935950539335166));
#5212=CARTESIAN_POINT('Ctrl Pts',(1.6211138875,38.5312500009559,-1.9852919333802E-16));
#5213=CARTESIAN_POINT('Ctrl Pts',(1.6211138875,38.4729166676226,0.935950539335165));
#5214=CARTESIAN_POINT('Ctrl Pts',(0.810556943750001,38.4145833342893,1.40392580900275));
#5215=CARTESIAN_POINT('Ctrl Pts',(3.43862649647115E-16,38.3562500009559,
1.87190107867033));
#5216=CARTESIAN_POINT('Ctrl Pts',(-0.810556943749999,38.2979166676226,1.40392580900275));
#5217=CARTESIAN_POINT('Ctrl Pts',(-1.6211138875,38.2395833342893,0.935950539335167));
#5218=CARTESIAN_POINT('Ctrl Pts',(-1.6211138875,38.1812500009559,0.));
#5219=CARTESIAN_POINT('Ctrl Pts',(-1.6211138875,38.1229166676226,-0.935950539335166));
#5220=CARTESIAN_POINT('Ctrl Pts',(-0.81055694375,38.0645833342893,-1.40392580900275));
#5221=CARTESIAN_POINT('Ctrl Pts',(-1.14620883215705E-16,38.0062500009559,
-1.87190107867033));
#5222=CARTESIAN_POINT('Ctrl Pts',(0.81055694375,37.9479166676226,-1.40392580900275));
#5223=CARTESIAN_POINT('Ctrl Pts',(1.6211138875,37.8895833342893,-0.935950539335166));
#5224=CARTESIAN_POINT('Ctrl Pts',(1.6211138875,37.8312500009559,-1.9852919333802E-16));
#5225=CARTESIAN_POINT('Ctrl Pts',(1.6211138875,37.7729166676226,0.935950539335165));
#5226=CARTESIAN_POINT('Ctrl Pts',(0.810556943750001,37.7145833342893,1.40392580900275));
#5227=CARTESIAN_POINT('Ctrl Pts',(3.43862649647115E-16,37.6562500009559,
1.87190107867033));
#5228=CARTESIAN_POINT('Ctrl Pts',(-0.810556943749999,37.5979166676226,1.40392580900275));
#5229=CARTESIAN_POINT('Ctrl Pts',(-1.6211138875,37.5395833342893,0.935950539335167));
#5230=CARTESIAN_POINT('Ctrl Pts',(-1.6211138875,37.4812500009559,0.));
#5231=CARTESIAN_POINT('Ctrl Pts',(-1.6211138875,37.4229166676226,-0.935950539335166));
#5232=CARTESIAN_POINT('Ctrl Pts',(-0.81055694375,37.3645833342893,-1.40392580900275));
#5233=CARTESIAN_POINT('Ctrl Pts',(-1.14620883215705E-16,37.3062500009559,
-1.87190107867033));
#5234=CARTESIAN_POINT('Ctrl Pts',(0.81055694375,37.2479166676226,-1.40392580900275));
#5235=CARTESIAN_POINT('Ctrl Pts',(1.6211138875,37.1895833342893,-0.935950539335166));
#5236=CARTESIAN_POINT('Ctrl Pts',(1.6211138875,37.1312500009559,-1.9852919333802E-16));
#5237=CARTESIAN_POINT('Ctrl Pts',(1.6211138875,37.0729166676226,0.935950539335165));
#5238=CARTESIAN_POINT('Ctrl Pts',(0.810556943750001,37.0145833342893,1.40392580900275));
#5239=CARTESIAN_POINT('Ctrl Pts',(3.43862649647115E-16,36.9562500009559,
1.87190107867033));
#5240=CARTESIAN_POINT('Ctrl Pts',(-0.810556943749999,36.8979166676226,1.40392580900275));
#5241=CARTESIAN_POINT('Ctrl Pts',(-1.6211138875,36.8395833342893,0.935950539335167));
#5242=CARTESIAN_POINT('Ctrl Pts',(-1.6211138875,36.7812500009559,0.));
#5243=CARTESIAN_POINT('Ctrl Pts',(-1.6211138875,36.7229166676226,-0.935950539335166));
#5244=CARTESIAN_POINT('Ctrl Pts',(-0.81055694375,36.6645833342893,-1.40392580900275));
#5245=CARTESIAN_POINT('Ctrl Pts',(-1.14620883215705E-16,36.6062500009559,
-1.87190107867033));
#5246=CARTESIAN_POINT('Ctrl Pts',(0.81055694375,36.5479166676226,-1.40392580900275));
#5247=CARTESIAN_POINT('Ctrl Pts',(1.6211138875,36.4895833342893,-0.935950539335166));
#5248=CARTESIAN_POINT('Ctrl Pts',(1.6211138875,36.4312500009559,-1.9852919333802E-16));
#5249=CARTESIAN_POINT('Ctrl Pts',(1.6211138875,36.3729166676226,0.935950539335165));
#5250=CARTESIAN_POINT('Ctrl Pts',(0.810556943750001,36.3145833342893,1.40392580900275));
#5251=CARTESIAN_POINT('Ctrl Pts',(3.43862649647115E-16,36.2562500009559,
1.87190107867033));
#5252=CARTESIAN_POINT('Ctrl Pts',(-0.810556943749999,36.1979166676226,1.40392580900275));
#5253=CARTESIAN_POINT('Ctrl Pts',(-1.6211138875,36.1395833342893,0.935950539335167));
#5254=CARTESIAN_POINT('Ctrl Pts',(-1.6211138875,36.0812500009559,0.));
#5255=CARTESIAN_POINT('Ctrl Pts',(-1.6211138875,36.0229166676226,-0.935950539335166));
#5256=CARTESIAN_POINT('Ctrl Pts',(-0.81055694375,35.9645833342893,-1.40392580900275));
#5257=CARTESIAN_POINT('Ctrl Pts',(-1.14620883215705E-16,35.9062500009559,
-1.87190107867033));
#5258=CARTESIAN_POINT('Ctrl Pts',(0.81055694375,35.8479166676226,-1.40392580900275));
#5259=CARTESIAN_POINT('Ctrl Pts',(1.6211138875,35.7895833342893,-0.935950539335166));
#5260=CARTESIAN_POINT('Ctrl Pts',(1.6211138875,35.7312500009559,-1.9852919333802E-16));
#5261=CARTESIAN_POINT('Ctrl Pts',(1.6211138875,35.6729166676226,0.935950539335165));
#5262=CARTESIAN_POINT('Ctrl Pts',(0.810556943750001,35.6145833342893,1.40392580900275));
#5263=CARTESIAN_POINT('Ctrl Pts',(3.43862649647115E-16,35.5562500009559,
1.87190107867033));
#5264=CARTESIAN_POINT('Ctrl Pts',(-0.810556943749999,35.4979166676226,1.40392580900275));
#5265=CARTESIAN_POINT('Ctrl Pts',(-1.6211138875,35.4395833342893,0.935950539335167));
#5266=CARTESIAN_POINT('Ctrl Pts',(-1.6211138875,35.3812500009559,0.));
#5267=CARTESIAN_POINT('Ctrl Pts',(-1.6211138875,35.3229166676226,-0.935950539335166));
#5268=CARTESIAN_POINT('Ctrl Pts',(-0.81055694375,35.2645833342893,-1.40392580900275));
#5269=CARTESIAN_POINT('Ctrl Pts',(-1.14620883215705E-16,35.2062500009559,
-1.87190107867033));
#5270=CARTESIAN_POINT('Ctrl Pts',(0.81055694375,35.1479166676226,-1.40392580900275));
#5271=CARTESIAN_POINT('Ctrl Pts',(1.6211138875,35.0895833342893,-0.935950539335166));
#5272=CARTESIAN_POINT('Ctrl Pts',(1.6211138875,35.0312500009559,-1.9852919333802E-16));
#5273=CARTESIAN_POINT('Ctrl Pts',(1.6211138875,34.9729166676226,0.935950539335165));
#5274=CARTESIAN_POINT('Ctrl Pts',(0.810556943750001,34.9145833342893,1.40392580900275));
#5275=CARTESIAN_POINT('Ctrl Pts',(3.43862649647115E-16,34.8562500009559,
1.87190107867033));
#5276=CARTESIAN_POINT('Ctrl Pts',(-0.810556943749999,34.7979166676226,1.40392580900275));
#5277=CARTESIAN_POINT('Ctrl Pts',(-1.6211138875,34.7395833342893,0.935950539335167));
#5278=CARTESIAN_POINT('Ctrl Pts',(-1.6211138875,34.6812500009559,0.));
#5279=CARTESIAN_POINT('Ctrl Pts',(-1.6211138875,34.6229166676226,-0.935950539335166));
#5280=CARTESIAN_POINT('Ctrl Pts',(-0.81055694375,34.5645833342893,-1.40392580900275));
#5281=CARTESIAN_POINT('Ctrl Pts',(-1.14620883215705E-16,34.5062500009559,
-1.87190107867033));
#5282=CARTESIAN_POINT('Ctrl Pts',(0.81055694375,34.4479166676226,-1.40392580900275));
#5283=CARTESIAN_POINT('Ctrl Pts',(1.6211138875,34.3895833342893,-0.935950539335166));
#5284=CARTESIAN_POINT('Ctrl Pts',(1.6211138875,34.3312500009559,-1.9852919333802E-16));
#5285=CARTESIAN_POINT('Ctrl Pts',(1.6211138875,34.2729166676226,0.935950539335165));
#5286=CARTESIAN_POINT('Ctrl Pts',(0.810556943750001,34.2145833342893,1.40392580900275));
#5287=CARTESIAN_POINT('Ctrl Pts',(3.43862649647115E-16,34.1562500009559,
1.87190107867033));
#5288=CARTESIAN_POINT('Ctrl Pts',(-0.810556943749999,34.0979166676226,1.40392580900275));
#5289=CARTESIAN_POINT('Ctrl Pts',(-1.6211138875,34.0395833342892,0.935950539335167));
#5290=CARTESIAN_POINT('Ctrl Pts',(-1.6211138875,33.9812500009559,0.));
#5291=CARTESIAN_POINT('Ctrl Pts',(-1.6211138875,33.9229166676226,-0.935950539335166));
#5292=CARTESIAN_POINT('Ctrl Pts',(-0.81055694375,33.8645833342893,-1.40392580900275));
#5293=CARTESIAN_POINT('Ctrl Pts',(-1.14620883215705E-16,33.8062500009559,
-1.87190107867033));
#5294=CARTESIAN_POINT('Ctrl Pts',(0.81055694375,33.7479166676226,-1.40392580900275));
#5295=CARTESIAN_POINT('Ctrl Pts',(1.6211138875,33.6895833342892,-0.935950539335166));
#5296=CARTESIAN_POINT('Ctrl Pts',(1.6211138875,33.6312500009559,-1.9852919333802E-16));
#5297=CARTESIAN_POINT('Ctrl Pts',(1.6211138875,33.5729166676226,0.935950539335165));
#5298=CARTESIAN_POINT('Ctrl Pts',(0.810556943750001,33.5145833342893,1.40392580900275));
#5299=CARTESIAN_POINT('Ctrl Pts',(3.43862649647115E-16,33.4562500009559,
1.87190107867033));
#5300=CARTESIAN_POINT('Ctrl Pts',(-0.810556943749999,33.3979166676226,1.40392580900275));
#5301=CARTESIAN_POINT('Ctrl Pts',(-1.6211138875,33.3395833342893,0.935950539335167));
#5302=CARTESIAN_POINT('Ctrl Pts',(-1.6211138875,33.2812500009559,0.));
#5303=CARTESIAN_POINT('Ctrl Pts',(-1.6211138875,33.2229166676226,-0.935950539335166));
#5304=CARTESIAN_POINT('Ctrl Pts',(-0.81055694375,33.1645833342893,-1.40392580900275));
#5305=CARTESIAN_POINT('Ctrl Pts',(-1.14620883215705E-16,33.1062500009559,
-1.87190107867033));
#5306=CARTESIAN_POINT('Ctrl Pts',(0.81055694375,33.0479166676226,-1.40392580900275));
#5307=CARTESIAN_POINT('Ctrl Pts',(1.6211138875,32.9895833342893,-0.935950539335166));
#5308=CARTESIAN_POINT('Ctrl Pts',(1.6211138875,32.9312500009559,-1.9852919333802E-16));
#5309=CARTESIAN_POINT('Ctrl Pts',(1.6211138875,32.8729166676226,0.935950539335165));
#5310=CARTESIAN_POINT('Ctrl Pts',(0.810556943750001,32.8145833342893,1.40392580900275));
#5311=CARTESIAN_POINT('Ctrl Pts',(3.43862649647115E-16,32.7562500009559,
1.87190107867033));
#5312=CARTESIAN_POINT('Ctrl Pts',(-0.810556943749999,32.6979166676226,1.40392580900275));
#5313=CARTESIAN_POINT('Ctrl Pts',(-1.6211138875,32.6395833342893,0.935950539335167));
#5314=CARTESIAN_POINT('Ctrl Pts',(-1.6211138875,32.5812500009559,0.));
#5315=CARTESIAN_POINT('Ctrl Pts',(-1.6211138875,32.5229166676226,-0.935950539335166));
#5316=CARTESIAN_POINT('Ctrl Pts',(-0.81055694375,32.4645833342893,-1.40392580900275));
#5317=CARTESIAN_POINT('Ctrl Pts',(-1.14620883215705E-16,32.4062500009559,
-1.87190107867033));
#5318=CARTESIAN_POINT('Ctrl Pts',(0.81055694375,32.3479166676226,-1.40392580900275));
#5319=CARTESIAN_POINT('Ctrl Pts',(1.6211138875,32.2895833342893,-0.935950539335166));
#5320=CARTESIAN_POINT('Ctrl Pts',(1.6211138875,32.2312500009559,-1.9852919333802E-16));
#5321=CARTESIAN_POINT('Ctrl Pts',(1.6211138875,32.1729166676226,0.935950539335165));
#5322=CARTESIAN_POINT('Ctrl Pts',(0.810556943750001,32.1145833342893,1.40392580900275));
#5323=CARTESIAN_POINT('Ctrl Pts',(3.43862649647115E-16,32.0562500009559,
1.87190107867033));
#5324=CARTESIAN_POINT('Ctrl Pts',(-0.810556943749999,31.9979166676226,1.40392580900275));
#5325=CARTESIAN_POINT('Ctrl Pts',(-1.6211138875,31.9395833342893,0.935950539335167));
#5326=CARTESIAN_POINT('Ctrl Pts',(-1.6211138875,31.8812500009559,0.));
#5327=CARTESIAN_POINT('Ctrl Pts',(-1.6211138875,31.8229166676226,-0.935950539335166));
#5328=CARTESIAN_POINT('Ctrl Pts',(-0.81055694375,31.7645833342893,-1.40392580900275));
#5329=CARTESIAN_POINT('Ctrl Pts',(-1.14620883215705E-16,31.7062500009559,
-1.87190107867033));
#5330=CARTESIAN_POINT('Ctrl Pts',(0.81055694375,31.6479166676226,-1.40392580900275));
#5331=CARTESIAN_POINT('Ctrl Pts',(1.6211138875,31.5895833342893,-0.935950539335166));
#5332=CARTESIAN_POINT('Ctrl Pts',(1.6211138875,31.5312500009559,-1.9852919333802E-16));
#5333=CARTESIAN_POINT('Ctrl Pts',(1.6211138875,31.4729166676226,0.935950539335165));
#5334=CARTESIAN_POINT('Ctrl Pts',(0.810556943750001,31.4145833342893,1.40392580900275));
#5335=CARTESIAN_POINT('Ctrl Pts',(3.43862649647115E-16,31.3562500009559,
1.87190107867033));
#5336=CARTESIAN_POINT('Ctrl Pts',(-0.810556943749999,31.2979166676226,1.40392580900275));
#5337=CARTESIAN_POINT('Ctrl Pts',(-1.6211138875,31.2395833342893,0.935950539335167));
#5338=CARTESIAN_POINT('Ctrl Pts',(-1.6211138875,31.1812500009559,0.));
#5339=CARTESIAN_POINT('Ctrl Pts',(-1.6211138875,31.1229166676226,-0.935950539335166));
#5340=CARTESIAN_POINT('Ctrl Pts',(-0.81055694375,31.0645833342893,-1.40392580900275));
#5341=CARTESIAN_POINT('Ctrl Pts',(-1.14620883215705E-16,31.0062500009559,
-1.87190107867033));
#5342=CARTESIAN_POINT('Ctrl Pts',(0.81055694375,30.9479166676226,-1.40392580900275));
#5343=CARTESIAN_POINT('Ctrl Pts',(1.6211138875,30.8895833342893,-0.935950539335166));
#5344=CARTESIAN_POINT('Ctrl Pts',(1.6211138875,30.8312500009559,-1.9852919333802E-16));
#5345=CARTESIAN_POINT('Ctrl Pts',(1.6211138875,30.7729166676226,0.935950539335165));
#5346=CARTESIAN_POINT('Ctrl Pts',(0.810556943750001,30.7145833342893,1.40392580900275));
#5347=CARTESIAN_POINT('Ctrl Pts',(3.43862649647115E-16,30.6562500009559,
1.87190107867033));
#5348=CARTESIAN_POINT('Ctrl Pts',(-0.810556943749999,30.5979166676226,1.40392580900275));
#5349=CARTESIAN_POINT('Ctrl Pts',(-1.6211138875,30.5395833342893,0.935950539335167));
#5350=CARTESIAN_POINT('Ctrl Pts',(-1.6211138875,30.4812500009559,0.));
#5351=CARTESIAN_POINT('Ctrl Pts',(-1.6211138875,30.4229166676226,-0.935950539335166));
#5352=CARTESIAN_POINT('Ctrl Pts',(-0.81055694375,30.3645833342893,-1.40392580900275));
#5353=CARTESIAN_POINT('Ctrl Pts',(-1.14620883215705E-16,30.3062500009559,
-1.87190107867033));
#5354=CARTESIAN_POINT('Ctrl Pts',(0.81055694375,30.2479166676226,-1.40392580900275));
#5355=CARTESIAN_POINT('Ctrl Pts',(1.6211138875,30.1895833342893,-0.935950539335166));
#5356=CARTESIAN_POINT('Ctrl Pts',(1.6211138875,30.1312500009559,-1.9852919333802E-16));
#5357=CARTESIAN_POINT('Ctrl Pts',(1.6211138875,30.0729166676226,0.935950539335165));
#5358=CARTESIAN_POINT('Ctrl Pts',(0.810556943750001,30.0145833342893,1.40392580900275));
#5359=CARTESIAN_POINT('Ctrl Pts',(3.43862649647115E-16,29.9562500009559,
1.87190107867033));
#5360=CARTESIAN_POINT('Ctrl Pts',(-0.810556943749999,29.8979166676226,1.40392580900275));
#5361=CARTESIAN_POINT('Ctrl Pts',(-1.6211138875,29.8395833342892,0.935950539335167));
#5362=CARTESIAN_POINT('Ctrl Pts',(-1.6211138875,29.7812500009559,0.));
#5363=CARTESIAN_POINT('Ctrl Pts',(-1.6211138875,29.7229166676226,-0.935950539335166));
#5364=CARTESIAN_POINT('Ctrl Pts',(-0.81055694375,29.6645833342893,-1.40392580900275));
#5365=CARTESIAN_POINT('Ctrl Pts',(-1.14620883215705E-16,29.6062500009559,
-1.87190107867033));
#5366=CARTESIAN_POINT('Ctrl Pts',(0.81055694375,29.5479166676226,-1.40392580900275));
#5367=CARTESIAN_POINT('Ctrl Pts',(1.6211138875,29.4895833342893,-0.935950539335166));
#5368=CARTESIAN_POINT('Ctrl Pts',(1.6211138875,29.4312500009559,-1.9852919333802E-16));
#5369=CARTESIAN_POINT('Ctrl Pts',(1.6211138875,29.3729166676226,0.935950539335165));
#5370=CARTESIAN_POINT('Ctrl Pts',(0.810556943750001,29.3145833342893,1.40392580900275));
#5371=CARTESIAN_POINT('Ctrl Pts',(3.43862649647115E-16,29.2562500009559,
1.87190107867033));
#5372=CARTESIAN_POINT('Ctrl Pts',(-0.810556943749999,29.1979166676226,1.40392580900275));
#5373=CARTESIAN_POINT('Ctrl Pts',(-1.6211138875,29.1395833342893,0.935950539335167));
#5374=CARTESIAN_POINT('Ctrl Pts',(-1.6211138875,29.0812500009559,0.));
#5375=CARTESIAN_POINT('Ctrl Pts',(-1.6211138875,29.0229166676226,-0.935950539335166));
#5376=CARTESIAN_POINT('Ctrl Pts',(-0.81055694375,28.9645833342893,-1.40392580900275));
#5377=CARTESIAN_POINT('Ctrl Pts',(-1.14620883215705E-16,28.9062500009559,
-1.87190107867033));
#5378=CARTESIAN_POINT('Ctrl Pts',(0.81055694375,28.8479166676226,-1.40392580900275));
#5379=CARTESIAN_POINT('Ctrl Pts',(1.6211138875,28.7895833342893,-0.935950539335166));
#5380=CARTESIAN_POINT('Ctrl Pts',(1.6211138875,28.7312500009559,-1.9852919333802E-16));
#5381=CARTESIAN_POINT('Ctrl Pts',(1.6211138875,28.6729166676226,0.935950539335165));
#5382=CARTESIAN_POINT('Ctrl Pts',(0.810556943750001,28.6145833342893,1.40392580900275));
#5383=CARTESIAN_POINT('Ctrl Pts',(3.43862649647115E-16,28.5562500009559,
1.87190107867033));
#5384=CARTESIAN_POINT('Ctrl Pts',(-0.810556943749999,28.4979166676226,1.40392580900275));
#5385=CARTESIAN_POINT('Ctrl Pts',(-1.6211138875,28.4395833342893,0.935950539335167));
#5386=CARTESIAN_POINT('Ctrl Pts',(-1.6211138875,28.3812500009559,0.));
#5387=CARTESIAN_POINT('Ctrl Pts',(-1.6211138875,28.3229166676226,-0.935950539335166));
#5388=CARTESIAN_POINT('Ctrl Pts',(-0.81055694375,28.2645833342893,-1.40392580900275));
#5389=CARTESIAN_POINT('Ctrl Pts',(-1.14620883215705E-16,28.2062500009559,
-1.87190107867033));
#5390=CARTESIAN_POINT('Ctrl Pts',(0.81055694375,28.1479166676226,-1.40392580900275));
#5391=CARTESIAN_POINT('Ctrl Pts',(1.6211138875,28.0895833342893,-0.935950539335166));
#5392=CARTESIAN_POINT('Ctrl Pts',(1.6211138875,28.0312500009559,-1.9852919333802E-16));
#5393=CARTESIAN_POINT('Ctrl Pts',(1.6211138875,27.9729166676226,0.935950539335165));
#5394=CARTESIAN_POINT('Ctrl Pts',(0.810556943750001,27.9145833342893,1.40392580900275));
#5395=CARTESIAN_POINT('Ctrl Pts',(3.43862649647115E-16,27.8562500009559,
1.87190107867033));
#5396=CARTESIAN_POINT('Ctrl Pts',(-0.810556943749999,27.7979166676226,1.40392580900275));
#5397=CARTESIAN_POINT('Ctrl Pts',(-1.6211138875,27.7395833342893,0.935950539335167));
#5398=CARTESIAN_POINT('Ctrl Pts',(-1.6211138875,27.6812500009559,0.));
#5399=CARTESIAN_POINT('Ctrl Pts',(-1.6211138875,27.6229166676226,-0.935950539335166));
#5400=CARTESIAN_POINT('Ctrl Pts',(-0.81055694375,27.5645833342893,-1.40392580900275));
#5401=CARTESIAN_POINT('Ctrl Pts',(-1.14620883215705E-16,27.5062500009559,
-1.87190107867033));
#5402=CARTESIAN_POINT('Ctrl Pts',(0.81055694375,27.4479166676226,-1.40392580900275));
#5403=CARTESIAN_POINT('Ctrl Pts',(1.6211138875,27.3895833342893,-0.935950539335166));
#5404=CARTESIAN_POINT('Ctrl Pts',(1.6211138875,27.3312500009559,-1.9852919333802E-16));
#5405=CARTESIAN_POINT('Ctrl Pts',(1.6211138875,27.2729166676226,0.935950539335165));
#5406=CARTESIAN_POINT('Ctrl Pts',(0.810556943750001,27.2145833342893,1.40392580900275));
#5407=CARTESIAN_POINT('Ctrl Pts',(3.43862649647115E-16,27.1562500009559,
1.87190107867033));
#5408=CARTESIAN_POINT('Ctrl Pts',(-0.810556943749999,27.0979166676226,1.40392580900275));
#5409=CARTESIAN_POINT('Ctrl Pts',(-1.6211138875,27.0395833342893,0.935950539335167));
#5410=CARTESIAN_POINT('Ctrl Pts',(-1.6211138875,26.9812500009559,0.));
#5411=CARTESIAN_POINT('Ctrl Pts',(-1.6211138875,26.9229166676226,-0.935950539335166));
#5412=CARTESIAN_POINT('Ctrl Pts',(-0.81055694375,26.8645833342893,-1.40392580900275));
#5413=CARTESIAN_POINT('Ctrl Pts',(-1.14620883215705E-16,26.8062500009559,
-1.87190107867033));
#5414=CARTESIAN_POINT('Ctrl Pts',(0.81055694375,26.7479166676226,-1.40392580900275));
#5415=CARTESIAN_POINT('Ctrl Pts',(1.6211138875,26.6895833342893,-0.935950539335166));
#5416=CARTESIAN_POINT('Ctrl Pts',(1.6211138875,26.6312500009559,-1.9852919333802E-16));
#5417=CARTESIAN_POINT('Ctrl Pts',(1.6211138875,26.5729166676226,0.935950539335165));
#5418=CARTESIAN_POINT('Ctrl Pts',(0.810556943750001,26.5145833342893,1.40392580900275));
#5419=CARTESIAN_POINT('Ctrl Pts',(3.43862649647115E-16,26.4562500009559,
1.87190107867033));
#5420=CARTESIAN_POINT('Ctrl Pts',(-0.810556943749999,26.3979166676226,1.40392580900275));
#5421=CARTESIAN_POINT('Ctrl Pts',(-1.6211138875,26.3395833342893,0.935950539335167));
#5422=CARTESIAN_POINT('Ctrl Pts',(-1.6211138875,26.2812500009559,0.));
#5423=CARTESIAN_POINT('Ctrl Pts',(-1.6211138875,26.2229166676226,-0.935950539335166));
#5424=CARTESIAN_POINT('Ctrl Pts',(-0.81055694375,26.1645833342893,-1.40392580900275));
#5425=CARTESIAN_POINT('Ctrl Pts',(-1.14620883215705E-16,26.1062500009559,
-1.87190107867033));
#5426=CARTESIAN_POINT('Ctrl Pts',(0.81055694375,26.0479166676226,-1.40392580900275));
#5427=CARTESIAN_POINT('Ctrl Pts',(1.6211138875,25.9895833342893,-0.935950539335166));
#5428=CARTESIAN_POINT('Ctrl Pts',(1.6211138875,25.9312500009559,-1.9852919333802E-16));
#5429=CARTESIAN_POINT('Ctrl Pts',(1.6211138875,25.8729166676226,0.935950539335165));
#5430=CARTESIAN_POINT('Ctrl Pts',(0.810556943750001,25.8145833342892,1.40392580900275));
#5431=CARTESIAN_POINT('Ctrl Pts',(3.43862649647115E-16,25.7562500009559,
1.87190107867033));
#5432=CARTESIAN_POINT('Ctrl Pts',(-0.810556943749999,25.6979166676226,1.40392580900275));
#5433=CARTESIAN_POINT('Ctrl Pts',(-1.6211138875,25.6395833342893,0.935950539335167));
#5434=CARTESIAN_POINT('Ctrl Pts',(-1.6211138875,25.5812500009559,0.));
#5435=CARTESIAN_POINT('Ctrl Pts',(-1.6211138875,25.5229166676226,-0.935950539335166));
#5436=CARTESIAN_POINT('Ctrl Pts',(-0.81055694375,25.4645833342893,-1.40392580900275));
#5437=CARTESIAN_POINT('Ctrl Pts',(-1.14620883215705E-16,25.4062500009559,
-1.87190107867033));
#5438=CARTESIAN_POINT('Ctrl Pts',(0.81055694375,25.3479166676226,-1.40392580900275));
#5439=CARTESIAN_POINT('Ctrl Pts',(1.6211138875,25.2895833342893,-0.935950539335166));
#5440=CARTESIAN_POINT('Ctrl Pts',(1.6211138875,25.2312500009559,-1.9852919333802E-16));
#5441=CARTESIAN_POINT('Ctrl Pts',(1.6211138875,25.1729166676226,0.935950539335165));
#5442=CARTESIAN_POINT('Ctrl Pts',(0.810556943750001,25.1145833342893,1.40392580900275));
#5443=CARTESIAN_POINT('Ctrl Pts',(3.43862649647115E-16,25.0562500009559,
1.87190107867033));
#5444=CARTESIAN_POINT('Ctrl Pts',(-0.810556943749999,24.9979166676226,1.40392580900275));
#5445=CARTESIAN_POINT('Ctrl Pts',(-1.6211138875,24.9395833342893,0.935950539335167));
#5446=CARTESIAN_POINT('Ctrl Pts',(-1.6211138875,24.8812500009559,0.));
#5447=CARTESIAN_POINT('Ctrl Pts',(-1.6211138875,24.8229166676226,-0.935950539335166));
#5448=CARTESIAN_POINT('Ctrl Pts',(-0.81055694375,24.7645833342893,-1.40392580900275));
#5449=CARTESIAN_POINT('Ctrl Pts',(-1.14620883215705E-16,24.7062500009559,
-1.87190107867033));
#5450=CARTESIAN_POINT('Ctrl Pts',(0.81055694375,24.6479166676226,-1.40392580900275));
#5451=CARTESIAN_POINT('Ctrl Pts',(1.6211138875,24.5895833342893,-0.935950539335166));
#5452=CARTESIAN_POINT('Ctrl Pts',(1.6211138875,24.5312500009559,-1.9852919333802E-16));
#5453=CARTESIAN_POINT('Ctrl Pts',(1.6211138875,24.4729166676226,0.935950539335165));
#5454=CARTESIAN_POINT('Ctrl Pts',(0.810556943750001,24.4145833342893,1.40392580900275));
#5455=CARTESIAN_POINT('Ctrl Pts',(3.43862649647115E-16,24.3562500009559,
1.87190107867033));
#5456=CARTESIAN_POINT('Ctrl Pts',(-0.810556943749999,24.2979166676226,1.40392580900275));
#5457=CARTESIAN_POINT('Ctrl Pts',(-1.6211138875,24.2395833342893,0.935950539335167));
#5458=CARTESIAN_POINT('Ctrl Pts',(-1.6211138875,24.1812500009559,0.));
#5459=CARTESIAN_POINT('Ctrl Pts',(-1.6211138875,24.1229166676226,-0.935950539335166));
#5460=CARTESIAN_POINT('Ctrl Pts',(-0.81055694375,24.0645833342893,-1.40392580900275));
#5461=CARTESIAN_POINT('Ctrl Pts',(-1.14620883215705E-16,24.0062500009559,
-1.87190107867033));
#5462=CARTESIAN_POINT('Ctrl Pts',(0.81055694375,23.9479166676226,-1.40392580900275));
#5463=CARTESIAN_POINT('Ctrl Pts',(1.6211138875,23.8895833342893,-0.935950539335166));
#5464=CARTESIAN_POINT('Ctrl Pts',(1.6211138875,23.8312500009559,-1.9852919333802E-16));
#5465=CARTESIAN_POINT('Ctrl Pts',(1.6211138875,23.7729166676226,0.935950539335165));
#5466=CARTESIAN_POINT('Ctrl Pts',(0.810556943750001,23.7145833342893,1.40392580900275));
#5467=CARTESIAN_POINT('Ctrl Pts',(3.43862649647115E-16,23.6562500009559,
1.87190107867033));
#5468=CARTESIAN_POINT('Ctrl Pts',(-0.810556943749999,23.5979166676226,1.40392580900275));
#5469=CARTESIAN_POINT('Ctrl Pts',(-1.6211138875,23.5395833342893,0.935950539335167));
#5470=CARTESIAN_POINT('Ctrl Pts',(-1.6211138875,23.4812500009559,0.));
#5471=CARTESIAN_POINT('Ctrl Pts',(-1.6211138875,23.4229166676226,-0.935950539335166));
#5472=CARTESIAN_POINT('Ctrl Pts',(-0.81055694375,23.3645833342893,-1.40392580900275));
#5473=CARTESIAN_POINT('Ctrl Pts',(-1.14620883215705E-16,23.3062500009559,
-1.87190107867033));
#5474=CARTESIAN_POINT('Ctrl Pts',(0.81055694375,23.2479166676226,-1.40392580900275));
#5475=CARTESIAN_POINT('Ctrl Pts',(1.6211138875,23.1895833342893,-0.935950539335166));
#5476=CARTESIAN_POINT('Ctrl Pts',(1.6211138875,23.1312500009559,-1.9852919333802E-16));
#5477=CARTESIAN_POINT('Ctrl Pts',(1.6211138875,23.0729166676226,0.935950539335165));
#5478=CARTESIAN_POINT('Ctrl Pts',(0.810556943750001,23.0145833342893,1.40392580900275));
#5479=CARTESIAN_POINT('Ctrl Pts',(3.43862649647115E-16,22.9562500009559,
1.87190107867033));
#5480=CARTESIAN_POINT('Ctrl Pts',(-0.810556943749999,22.8979166676226,1.40392580900275));
#5481=CARTESIAN_POINT('Ctrl Pts',(-1.6211138875,22.8395833342893,0.935950539335167));
#5482=CARTESIAN_POINT('Ctrl Pts',(-1.6211138875,22.7812500009559,0.));
#5483=CARTESIAN_POINT('Ctrl Pts',(-1.6211138875,22.7229166676226,-0.935950539335166));
#5484=CARTESIAN_POINT('Ctrl Pts',(-0.81055694375,22.6645833342893,-1.40392580900275));
#5485=CARTESIAN_POINT('Ctrl Pts',(-1.14620883215705E-16,22.6062500009559,
-1.87190107867033));
#5486=CARTESIAN_POINT('Ctrl Pts',(0.81055694375,22.5479166676226,-1.40392580900275));
#5487=CARTESIAN_POINT('Ctrl Pts',(1.6211138875,22.4895833342893,-0.935950539335166));
#5488=CARTESIAN_POINT('Ctrl Pts',(1.6211138875,22.4312500009559,-1.9852919333802E-16));
#5489=CARTESIAN_POINT('Ctrl Pts',(1.6211138875,22.3729166676226,0.935950539335165));
#5490=CARTESIAN_POINT('Ctrl Pts',(0.810556943750001,22.3145833342893,1.40392580900275));
#5491=CARTESIAN_POINT('Ctrl Pts',(3.43862649647115E-16,22.2562500009559,
1.87190107867033));
#5492=CARTESIAN_POINT('Ctrl Pts',(-0.810556943749999,22.1979166676226,1.40392580900275));
#5493=CARTESIAN_POINT('Ctrl Pts',(-1.6211138875,22.1395833342893,0.935950539335167));
#5494=CARTESIAN_POINT('Ctrl Pts',(-1.6211138875,22.0812500009559,0.));
#5495=CARTESIAN_POINT('Ctrl Pts',(-1.6211138875,22.0229166676226,-0.935950539335166));
#5496=CARTESIAN_POINT('Ctrl Pts',(-0.81055694375,21.9645833342893,-1.40392580900275));
#5497=CARTESIAN_POINT('Ctrl Pts',(-1.14620883215705E-16,21.9062500009559,
-1.87190107867033));
#5498=CARTESIAN_POINT('Ctrl Pts',(0.81055694375,21.8479166676226,-1.40392580900275));
#5499=CARTESIAN_POINT('Ctrl Pts',(1.6211138875,21.7895833342893,-0.935950539335166));
#5500=CARTESIAN_POINT('Ctrl Pts',(1.6211138875,21.7312500009559,-1.9852919333802E-16));
#5501=CARTESIAN_POINT('Ctrl Pts',(1.6211138875,21.6729166676226,0.935950539335165));
#5502=CARTESIAN_POINT('Ctrl Pts',(0.810556943750001,21.6145833342893,1.40392580900275));
#5503=CARTESIAN_POINT('Ctrl Pts',(3.43862649647115E-16,21.5562500009559,
1.87190107867033));
#5504=CARTESIAN_POINT('Ctrl Pts',(-0.810556943749999,21.4979166676226,1.40392580900275));
#5505=CARTESIAN_POINT('Ctrl Pts',(-1.6211138875,21.4395833342893,0.935950539335167));
#5506=CARTESIAN_POINT('Ctrl Pts',(-1.6211138875,21.3812500009559,0.));
#5507=CARTESIAN_POINT('Ctrl Pts',(-1.6211138875,21.3229166676226,-0.935950539335166));
#5508=CARTESIAN_POINT('Ctrl Pts',(-0.81055694375,21.2645833342893,-1.40392580900275));
#5509=CARTESIAN_POINT('Ctrl Pts',(-1.14620883215705E-16,21.2062500009559,
-1.87190107867033));
#5510=CARTESIAN_POINT('Ctrl Pts',(0.81055694375,21.1479166676226,-1.40392580900275));
#5511=CARTESIAN_POINT('Ctrl Pts',(1.6211138875,21.0895833342892,-0.935950539335166));
#5512=CARTESIAN_POINT('Ctrl Pts',(1.6211138875,21.0312500009559,-1.9852919333802E-16));
#5513=CARTESIAN_POINT('Ctrl Pts',(1.6211138875,20.9729166676226,0.935950539335165));
#5514=CARTESIAN_POINT('Ctrl Pts',(0.810556943750001,20.9145833342893,1.40392580900275));
#5515=CARTESIAN_POINT('Ctrl Pts',(3.43862649647115E-16,20.8562500009559,
1.87190107867033));
#5516=CARTESIAN_POINT('Ctrl Pts',(-0.810556943749999,20.7979166676226,1.40392580900275));
#5517=CARTESIAN_POINT('Ctrl Pts',(-1.6211138875,20.7395833342893,0.935950539335167));
#5518=CARTESIAN_POINT('Ctrl Pts',(-1.6211138875,20.6812500009559,0.));
#5519=CARTESIAN_POINT('Ctrl Pts',(-1.6211138875,20.6229166676226,-0.935950539335166));
#5520=CARTESIAN_POINT('Ctrl Pts',(-0.81055694375,20.5645833342893,-1.40392580900275));
#5521=CARTESIAN_POINT('Ctrl Pts',(-1.14620883215705E-16,20.5062500009559,
-1.87190107867033));
#5522=CARTESIAN_POINT('Ctrl Pts',(0.81055694375,20.4479166676226,-1.40392580900275));
#5523=CARTESIAN_POINT('Ctrl Pts',(1.6211138875,20.3895833342893,-0.935950539335166));
#5524=CARTESIAN_POINT('Ctrl Pts',(1.6211138875,20.3312500009559,-1.9852919333802E-16));
#5525=CARTESIAN_POINT('Ctrl Pts',(1.6211138875,20.2729166676226,0.935950539335165));
#5526=CARTESIAN_POINT('Ctrl Pts',(0.810556943750001,20.2145833342893,1.40392580900275));
#5527=CARTESIAN_POINT('Ctrl Pts',(3.43862649647115E-16,20.1562500009559,
1.87190107867033));
#5528=CARTESIAN_POINT('Ctrl Pts',(-0.810556943749999,20.0979166676226,1.40392580900275));
#5529=CARTESIAN_POINT('Ctrl Pts',(-1.6211138875,20.0395833342893,0.935950539335167));
#5530=CARTESIAN_POINT('Ctrl Pts',(-1.6211138875,19.9812500009559,0.));
#5531=CARTESIAN_POINT('Ctrl Pts',(-1.6211138875,19.9229166676226,-0.935950539335166));
#5532=CARTESIAN_POINT('Ctrl Pts',(-0.81055694375,19.8645833342893,-1.40392580900275));
#5533=CARTESIAN_POINT('Ctrl Pts',(-1.14620883215705E-16,19.8062500009559,
-1.87190107867033));
#5534=CARTESIAN_POINT('Ctrl Pts',(0.81055694375,19.7479166676226,-1.40392580900275));
#5535=CARTESIAN_POINT('Ctrl Pts',(1.6211138875,19.6895833342893,-0.935950539335166));
#5536=CARTESIAN_POINT('Ctrl Pts',(1.6211138875,19.6312500009559,-1.9852919333802E-16));
#5537=CARTESIAN_POINT('Ctrl Pts',(1.6211138875,19.5729166676226,0.935950539335165));
#5538=CARTESIAN_POINT('Ctrl Pts',(0.810556943750001,19.5145833342893,1.40392580900275));
#5539=CARTESIAN_POINT('Ctrl Pts',(3.43862649647115E-16,19.4562500009559,
1.87190107867033));
#5540=CARTESIAN_POINT('Ctrl Pts',(-0.810556943749999,19.3979166676226,1.40392580900275));
#5541=CARTESIAN_POINT('Ctrl Pts',(-1.6211138875,19.3395833342893,0.935950539335167));
#5542=CARTESIAN_POINT('Ctrl Pts',(-1.6211138875,19.2812500009559,0.));
#5543=CARTESIAN_POINT('Ctrl Pts',(-1.6211138875,19.2229166676226,-0.935950539335166));
#5544=CARTESIAN_POINT('Ctrl Pts',(-0.81055694375,19.1645833342893,-1.40392580900275));
#5545=CARTESIAN_POINT('Ctrl Pts',(-1.14620883215705E-16,19.1062500009559,
-1.87190107867033));
#5546=CARTESIAN_POINT('Ctrl Pts',(0.81055694375,19.0479166676226,-1.40392580900275));
#5547=CARTESIAN_POINT('Ctrl Pts',(1.6211138875,18.9895833342893,-0.935950539335166));
#5548=CARTESIAN_POINT('Ctrl Pts',(1.6211138875,18.9312500009559,-1.9852919333802E-16));
#5549=CARTESIAN_POINT('Ctrl Pts',(1.6211138875,18.8729166676226,0.935950539335165));
#5550=CARTESIAN_POINT('Ctrl Pts',(0.810556943750001,18.8145833342893,1.40392580900275));
#5551=CARTESIAN_POINT('Ctrl Pts',(3.43862649647115E-16,18.7562500009559,
1.87190107867033));
#5552=CARTESIAN_POINT('Ctrl Pts',(-0.810556943749999,18.6979166676226,1.40392580900275));
#5553=CARTESIAN_POINT('Ctrl Pts',(-1.6211138875,18.6395833342893,0.935950539335167));
#5554=CARTESIAN_POINT('Ctrl Pts',(-1.6211138875,18.5812500009559,0.));
#5555=CARTESIAN_POINT('Ctrl Pts',(-1.6211138875,18.5229166676226,-0.935950539335166));
#5556=CARTESIAN_POINT('Ctrl Pts',(-0.81055694375,18.4645833342893,-1.40392580900275));
#5557=CARTESIAN_POINT('Ctrl Pts',(-1.14620883215705E-16,18.4062500009559,
-1.87190107867033));
#5558=CARTESIAN_POINT('Ctrl Pts',(0.81055694375,18.3479166676226,-1.40392580900275));
#5559=CARTESIAN_POINT('Ctrl Pts',(1.6211138875,18.2895833342893,-0.935950539335166));
#5560=CARTESIAN_POINT('Ctrl Pts',(1.6211138875,18.2312500009559,-1.9852919333802E-16));
#5561=CARTESIAN_POINT('Ctrl Pts',(1.6211138875,18.1729166676226,0.935950539335165));
#5562=CARTESIAN_POINT('Ctrl Pts',(0.810556943750001,18.1145833342893,1.40392580900275));
#5563=CARTESIAN_POINT('Ctrl Pts',(3.43862649647115E-16,18.0562500009559,
1.87190107867033));
#5564=CARTESIAN_POINT('Ctrl Pts',(-0.810556943749999,17.9979166676226,1.40392580900275));
#5565=CARTESIAN_POINT('Ctrl Pts',(-1.6211138875,17.9395833342893,0.935950539335167));
#5566=CARTESIAN_POINT('Ctrl Pts',(-1.6211138875,17.8812500009559,0.));
#5567=CARTESIAN_POINT('Ctrl Pts',(-1.6211138875,17.8229166676226,-0.935950539335166));
#5568=CARTESIAN_POINT('Ctrl Pts',(-0.81055694375,17.7645833342893,-1.40392580900275));
#5569=CARTESIAN_POINT('Ctrl Pts',(-1.14620883215705E-16,17.7062500009559,
-1.87190107867033));
#5570=CARTESIAN_POINT('Ctrl Pts',(0.81055694375,17.6479166676226,-1.40392580900275));
#5571=CARTESIAN_POINT('Ctrl Pts',(1.6211138875,17.5895833342893,-0.935950539335166));
#5572=CARTESIAN_POINT('Ctrl Pts',(1.6211138875,17.5312500009559,-1.9852919333802E-16));
#5573=CARTESIAN_POINT('Ctrl Pts',(1.6211138875,17.4729166676226,0.935950539335165));
#5574=CARTESIAN_POINT('Ctrl Pts',(0.810556943750001,17.4145833342893,1.40392580900275));
#5575=CARTESIAN_POINT('Ctrl Pts',(3.43862649647115E-16,17.3562500009559,
1.87190107867033));
#5576=CARTESIAN_POINT('Ctrl Pts',(-0.810556943749999,17.2979166676226,1.40392580900275));
#5577=CARTESIAN_POINT('Ctrl Pts',(-1.6211138875,17.2395833342893,0.935950539335167));
#5578=CARTESIAN_POINT('Ctrl Pts',(-1.6211138875,17.1812500009559,0.));
#5579=CARTESIAN_POINT('Ctrl Pts',(-1.6211138875,17.1229166676226,-0.935950539335166));
#5580=CARTESIAN_POINT('Ctrl Pts',(-0.81055694375,17.0645833342893,-1.40392580900275));
#5581=CARTESIAN_POINT('Ctrl Pts',(-1.14620883215705E-16,17.0062500009559,
-1.87190107867033));
#5582=CARTESIAN_POINT('Ctrl Pts',(0.81055694375,16.9479166676226,-1.40392580900275));
#5583=CARTESIAN_POINT('Ctrl Pts',(1.6211138875,16.8895833342893,-0.935950539335166));
#5584=CARTESIAN_POINT('Ctrl Pts',(1.6211138875,16.8312500009559,-1.9852919333802E-16));
#5585=CARTESIAN_POINT('Ctrl Pts',(1.6211138875,16.7729166676226,0.935950539335165));
#5586=CARTESIAN_POINT('Ctrl Pts',(0.810556943750001,16.7145833342893,1.40392580900275));
#5587=CARTESIAN_POINT('Ctrl Pts',(3.43862649647115E-16,16.6562500009559,
1.87190107867033));
#5588=CARTESIAN_POINT('Ctrl Pts',(-0.810556943749999,16.5979166676226,1.40392580900275));
#5589=CARTESIAN_POINT('Ctrl Pts',(-1.6211138875,16.5395833342893,0.935950539335167));
#5590=CARTESIAN_POINT('Ctrl Pts',(-1.6211138875,16.4812500009559,0.));
#5591=CARTESIAN_POINT('Ctrl Pts',(-1.6211138875,16.4229166676226,-0.935950539335166));
#5592=CARTESIAN_POINT('Ctrl Pts',(-0.81055694375,16.3645833342893,-1.40392580900275));
#5593=CARTESIAN_POINT('Ctrl Pts',(-1.14620883215705E-16,16.3062500009559,
-1.87190107867033));
#5594=CARTESIAN_POINT('Ctrl Pts',(0.81055694375,16.2479166676226,-1.40392580900275));
#5595=CARTESIAN_POINT('Ctrl Pts',(1.6211138875,16.1895833342893,-0.935950539335166));
#5596=CARTESIAN_POINT('Ctrl Pts',(1.6211138875,16.1312500009559,-1.9852919333802E-16));
#5597=CARTESIAN_POINT('Ctrl Pts',(1.6211138875,16.0729166676226,0.935950539335165));
#5598=CARTESIAN_POINT('Ctrl Pts',(0.810556943750001,16.0145833342893,1.40392580900275));
#5599=CARTESIAN_POINT('Ctrl Pts',(3.43862649647115E-16,15.9562500009559,
1.87190107867033));
#5600=CARTESIAN_POINT('Ctrl Pts',(-0.810556943749999,15.8979166676226,1.40392580900275));
#5601=CARTESIAN_POINT('Ctrl Pts',(-1.6211138875,15.8395833342893,0.935950539335167));
#5602=CARTESIAN_POINT('Ctrl Pts',(-1.6211138875,15.7812500009559,0.));
#5603=CARTESIAN_POINT('Ctrl Pts',(-1.6211138875,15.7229166676226,-0.935950539335166));
#5604=CARTESIAN_POINT('Ctrl Pts',(-0.81055694375,15.6645833342893,-1.40392580900275));
#5605=CARTESIAN_POINT('Ctrl Pts',(-1.14620883215705E-16,15.6062500009559,
-1.87190107867033));
#5606=CARTESIAN_POINT('Ctrl Pts',(0.81055694375,15.5479166676226,-1.40392580900275));
#5607=CARTESIAN_POINT('Ctrl Pts',(1.6211138875,15.4895833342893,-0.935950539335166));
#5608=CARTESIAN_POINT('Ctrl Pts',(1.6211138875,15.4312500009559,-1.9852919333802E-16));
#5609=CARTESIAN_POINT('Ctrl Pts',(1.6211138875,15.3729166676226,0.935950539335165));
#5610=CARTESIAN_POINT('Ctrl Pts',(0.810556943750001,15.3145833342893,1.40392580900275));
#5611=CARTESIAN_POINT('Ctrl Pts',(3.43862649647115E-16,15.2562500009559,
1.87190107867033));
#5612=CARTESIAN_POINT('Ctrl Pts',(-0.810556943749999,15.1979166676226,1.40392580900275));
#5613=CARTESIAN_POINT('Ctrl Pts',(-1.6211138875,15.1395833342893,0.935950539335167));
#5614=CARTESIAN_POINT('Ctrl Pts',(-1.6211138875,15.0812500009559,0.));
#5615=CARTESIAN_POINT('Ctrl Pts',(-1.6211138875,15.0229166676226,-0.935950539335166));
#5616=CARTESIAN_POINT('Ctrl Pts',(-0.81055694375,14.9645833342893,-1.40392580900275));
#5617=CARTESIAN_POINT('Ctrl Pts',(-1.14620883215705E-16,14.9062500009559,
-1.87190107867033));
#5618=CARTESIAN_POINT('Ctrl Pts',(0.81055694375,14.8479166676226,-1.40392580900275));
#5619=CARTESIAN_POINT('Ctrl Pts',(1.6211138875,14.7895833342893,-0.935950539335166));
#5620=CARTESIAN_POINT('Ctrl Pts',(1.6211138875,14.7312500009559,-1.9852919333802E-16));
#5621=CARTESIAN_POINT('Ctrl Pts',(1.6211138875,14.6729166676226,0.935950539335165));
#5622=CARTESIAN_POINT('Ctrl Pts',(0.810556943750001,14.6145833342893,1.40392580900275));
#5623=CARTESIAN_POINT('Ctrl Pts',(3.43862649647115E-16,14.5562500009559,
1.87190107867033));
#5624=CARTESIAN_POINT('Ctrl Pts',(-0.810556943749999,14.4979166676226,1.40392580900275));
#5625=CARTESIAN_POINT('Ctrl Pts',(-1.6211138875,14.4395833342893,0.935950539335167));
#5626=CARTESIAN_POINT('Ctrl Pts',(-1.6211138875,14.3812500009559,0.));
#5627=CARTESIAN_POINT('Ctrl Pts',(-1.6211138875,14.3229166676226,-0.935950539335166));
#5628=CARTESIAN_POINT('Ctrl Pts',(-0.81055694375,14.2645833342893,-1.40392580900275));
#5629=CARTESIAN_POINT('Ctrl Pts',(-1.14620883215705E-16,14.2062500009559,
-1.87190107867033));
#5630=CARTESIAN_POINT('Ctrl Pts',(0.81055694375,14.1479166676226,-1.40392580900275));
#5631=CARTESIAN_POINT('Ctrl Pts',(1.6211138875,14.0895833342893,-0.935950539335166));
#5632=CARTESIAN_POINT('Ctrl Pts',(1.6211138875,14.0312500009559,-1.9852919333802E-16));
#5633=CARTESIAN_POINT('Ctrl Pts',(1.6211138875,13.9729166676226,0.935950539335165));
#5634=CARTESIAN_POINT('Ctrl Pts',(0.810556943750001,13.9145833342893,1.40392580900275));
#5635=CARTESIAN_POINT('Ctrl Pts',(3.43862649647115E-16,13.8562500009559,
1.87190107867033));
#5636=CARTESIAN_POINT('Ctrl Pts',(-0.810556943749999,13.7979166676226,1.40392580900275));
#5637=CARTESIAN_POINT('Ctrl Pts',(-1.6211138875,13.7395833342893,0.935950539335167));
#5638=CARTESIAN_POINT('Ctrl Pts',(-1.6211138875,13.6812500009559,0.));
#5639=CARTESIAN_POINT('Ctrl Pts',(-1.6211138875,13.6229166676226,-0.935950539335166));
#5640=CARTESIAN_POINT('Ctrl Pts',(-0.81055694375,13.5645833342893,-1.40392580900275));
#5641=CARTESIAN_POINT('Ctrl Pts',(-1.14620883215705E-16,13.5062500009559,
-1.87190107867033));
#5642=CARTESIAN_POINT('Ctrl Pts',(0.81055694375,13.4479166676226,-1.40392580900275));
#5643=CARTESIAN_POINT('Ctrl Pts',(1.6211138875,13.3895833342893,-0.935950539335166));
#5644=CARTESIAN_POINT('Ctrl Pts',(1.6211138875,13.3312500009559,-1.9852919333802E-16));
#5645=CARTESIAN_POINT('Ctrl Pts',(1.6211138875,13.2729166676226,0.935950539335165));
#5646=CARTESIAN_POINT('Ctrl Pts',(0.810556943750001,13.2145833342893,1.40392580900275));
#5647=CARTESIAN_POINT('Ctrl Pts',(3.43862649647115E-16,13.1562500009559,
1.87190107867033));
#5648=CARTESIAN_POINT('Ctrl Pts',(-0.810556943749999,13.0979166676226,1.40392580900275));
#5649=CARTESIAN_POINT('Ctrl Pts',(-1.6211138875,13.0395833342893,0.935950539335167));
#5650=CARTESIAN_POINT('Ctrl Pts',(-1.6211138875,12.9812500009559,0.));
#5651=CARTESIAN_POINT('Ctrl Pts',(-1.6211138875,12.9229166676226,-0.935950539335166));
#5652=CARTESIAN_POINT('Ctrl Pts',(-0.81055694375,12.8645833342893,-1.40392580900275));
#5653=CARTESIAN_POINT('Ctrl Pts',(-1.14620883215705E-16,12.8062500009559,
-1.87190107867033));
#5654=CARTESIAN_POINT('Ctrl Pts',(0.81055694375,12.7479166676226,-1.40392580900275));
#5655=CARTESIAN_POINT('Ctrl Pts',(1.6211138875,12.6895833342893,-0.935950539335166));
#5656=CARTESIAN_POINT('Ctrl Pts',(1.6211138875,12.6312500009559,-1.9852919333802E-16));
#5657=CARTESIAN_POINT('Ctrl Pts',(1.6211138875,12.5729166676226,0.935950539335165));
#5658=CARTESIAN_POINT('Ctrl Pts',(0.810556943750001,12.5145833342893,1.40392580900275));
#5659=CARTESIAN_POINT('Ctrl Pts',(3.43862649647115E-16,12.4562500009559,
1.87190107867033));
#5660=CARTESIAN_POINT('Ctrl Pts',(-0.810556943749999,12.3979166676226,1.40392580900275));
#5661=CARTESIAN_POINT('Ctrl Pts',(-1.6211138875,12.3395833342893,0.935950539335167));
#5662=CARTESIAN_POINT('Ctrl Pts',(-1.6211138875,12.2812500009559,0.));
#5663=CARTESIAN_POINT('Ctrl Pts',(-1.6211138875,12.2229166676226,-0.935950539335166));
#5664=CARTESIAN_POINT('Ctrl Pts',(-0.81055694375,12.1645833342893,-1.40392580900275));
#5665=CARTESIAN_POINT('Ctrl Pts',(-1.14620883215705E-16,12.1062500009559,
-1.87190107867033));
#5666=CARTESIAN_POINT('Ctrl Pts',(0.81055694375,12.0479166676226,-1.40392580900275));
#5667=CARTESIAN_POINT('Ctrl Pts',(1.6211138875,11.9895833342893,-0.935950539335166));
#5668=CARTESIAN_POINT('Ctrl Pts',(1.6211138875,11.9312500009559,-1.9852919333802E-16));
#5669=CARTESIAN_POINT('Ctrl Pts',(1.6211138875,11.8729166676226,0.935950539335165));
#5670=CARTESIAN_POINT('Ctrl Pts',(0.810556943750001,11.8145833342893,1.40392580900275));
#5671=CARTESIAN_POINT('Ctrl Pts',(3.43862649647115E-16,11.7562500009559,
1.87190107867033));
#5672=CARTESIAN_POINT('Ctrl Pts',(-0.810556943749999,11.6979166676226,1.40392580900275));
#5673=CARTESIAN_POINT('Ctrl Pts',(-1.6211138875,11.6395833342893,0.935950539335167));
#5674=CARTESIAN_POINT('Ctrl Pts',(-1.6211138875,11.5812500009559,0.));
#5675=CARTESIAN_POINT('Ctrl Pts',(-1.6211138875,11.5229166676226,-0.935950539335166));
#5676=CARTESIAN_POINT('Ctrl Pts',(-0.81055694375,11.4645833342893,-1.40392580900275));
#5677=CARTESIAN_POINT('Ctrl Pts',(-1.14620883215705E-16,11.4062500009559,
-1.87190107867033));
#5678=CARTESIAN_POINT('Ctrl Pts',(0.81055694375,11.3479166676226,-1.40392580900275));
#5679=CARTESIAN_POINT('Ctrl Pts',(1.6211138875,11.2895833342893,-0.935950539335166));
#5680=CARTESIAN_POINT('Ctrl Pts',(1.6211138875,11.2312500009559,-1.9852919333802E-16));
#5681=CARTESIAN_POINT('Ctrl Pts',(1.6211138875,11.1729166676226,0.935950539335165));
#5682=CARTESIAN_POINT('Ctrl Pts',(0.810556943750001,11.1145833342893,1.40392580900275));
#5683=CARTESIAN_POINT('Ctrl Pts',(3.43862649647115E-16,11.0562500009559,
1.87190107867033));
#5684=CARTESIAN_POINT('Ctrl Pts',(-0.810556943749999,10.9979166676226,1.40392580900275));
#5685=CARTESIAN_POINT('Ctrl Pts',(-1.6211138875,10.9395833342893,0.935950539335167));
#5686=CARTESIAN_POINT('Ctrl Pts',(-1.6211138875,10.8812500009559,0.));
#5687=CARTESIAN_POINT('Ctrl Pts',(-1.6211138875,10.8229166676226,-0.935950539335166));
#5688=CARTESIAN_POINT('Ctrl Pts',(-0.81055694375,10.7645833342893,-1.40392580900275));
#5689=CARTESIAN_POINT('Ctrl Pts',(-1.14620883215705E-16,10.7062500009559,
-1.87190107867033));
#5690=CARTESIAN_POINT('Ctrl Pts',(0.81055694375,10.6479166676226,-1.40392580900275));
#5691=CARTESIAN_POINT('Ctrl Pts',(1.6211138875,10.5895833342893,-0.935950539335166));
#5692=CARTESIAN_POINT('Ctrl Pts',(1.6211138875,10.5312500009559,-1.9852919333802E-16));
#5693=CARTESIAN_POINT('Ctrl Pts',(1.6211138875,10.4729166676226,0.935950539335165));
#5694=CARTESIAN_POINT('Ctrl Pts',(0.810556943750001,10.4145833342893,1.40392580900275));
#5695=CARTESIAN_POINT('Ctrl Pts',(3.43862649647115E-16,10.3562500009559,
1.87190107867033));
#5696=CARTESIAN_POINT('Ctrl Pts',(-0.810556943749999,10.2979166676226,1.40392580900275));
#5697=CARTESIAN_POINT('Ctrl Pts',(-1.6211138875,10.2395833342893,0.935950539335167));
#5698=CARTESIAN_POINT('Ctrl Pts',(-1.6211138875,10.1812500009559,0.));
#5699=CARTESIAN_POINT('Ctrl Pts',(-1.6211138875,10.1229166676226,-0.935950539335166));
#5700=CARTESIAN_POINT('Ctrl Pts',(-0.81055694375,10.0645833342893,-1.40392580900275));
#5701=CARTESIAN_POINT('Ctrl Pts',(-1.14620883215705E-16,10.0062500009559,
-1.87190107867033));
#5702=CARTESIAN_POINT('Ctrl Pts',(0.81055694375,9.94791666762259,-1.40392580900275));
#5703=CARTESIAN_POINT('Ctrl Pts',(1.6211138875,9.88958333428926,-0.935950539335166));
#5704=CARTESIAN_POINT('Ctrl Pts',(1.6211138875,9.83125000095592,-1.9852919333802E-16));
#5705=CARTESIAN_POINT('Ctrl Pts',(1.6211138875,9.77291666762259,0.935950539335165));
#5706=CARTESIAN_POINT('Ctrl Pts',(0.810556943750001,9.71458333428926,1.40392580900275));
#5707=CARTESIAN_POINT('Ctrl Pts',(3.43862649647115E-16,9.65625000095592,
1.87190107867033));
#5708=CARTESIAN_POINT('Ctrl Pts',(-0.810556943749999,9.59791666762259,1.40392580900275));
#5709=CARTESIAN_POINT('Ctrl Pts',(-1.6211138875,9.53958333428925,0.935950539335167));
#5710=CARTESIAN_POINT('Ctrl Pts',(-1.6211138875,9.48125000095592,0.));
#5711=CARTESIAN_POINT('Ctrl Pts',(-1.6211138875,9.42291666762259,-0.935950539335166));
#5712=CARTESIAN_POINT('Ctrl Pts',(-0.81055694375,9.36458333428925,-1.40392580900275));
#5713=CARTESIAN_POINT('Ctrl Pts',(-1.14620883215705E-16,9.30625000095592,
-1.87190107867033));
#5714=CARTESIAN_POINT('Ctrl Pts',(0.81055694375,9.24791666762259,-1.40392580900275));
#5715=CARTESIAN_POINT('Ctrl Pts',(1.6211138875,9.18958333428925,-0.935950539335166));
#5716=CARTESIAN_POINT('Ctrl Pts',(1.6211138875,9.13125000095592,-1.9852919333802E-16));
#5717=CARTESIAN_POINT('Ctrl Pts',(1.6211138875,9.07291666762258,0.935950539335165));
#5718=CARTESIAN_POINT('Ctrl Pts',(0.810556943750001,9.01458333428926,1.40392580900275));
#5719=CARTESIAN_POINT('Ctrl Pts',(3.43862649647115E-16,8.95625000095592,
1.87190107867033));
#5720=CARTESIAN_POINT('Ctrl Pts',(-0.810556943749999,8.89791666762259,1.40392580900275));
#5721=CARTESIAN_POINT('Ctrl Pts',(-1.6211138875,8.83958333428926,0.935950539335167));
#5722=CARTESIAN_POINT('Ctrl Pts',(-1.6211138875,8.78125000095592,0.));
#5723=CARTESIAN_POINT('Ctrl Pts',(-1.6211138875,8.72291666762259,-0.935950539335166));
#5724=CARTESIAN_POINT('Ctrl Pts',(-0.81055694375,8.66458333428925,-1.40392580900275));
#5725=CARTESIAN_POINT('Ctrl Pts',(-1.14620883215705E-16,8.60625000095592,
-1.87190107867033));
#5726=CARTESIAN_POINT('Ctrl Pts',(0.81055694375,8.54791666762259,-1.40392580900275));
#5727=CARTESIAN_POINT('Ctrl Pts',(1.6211138875,8.48958333428926,-0.935950539335166));
#5728=CARTESIAN_POINT('Ctrl Pts',(1.6211138875,8.43125000095592,-1.9852919333802E-16));
#5729=CARTESIAN_POINT('Ctrl Pts',(1.6211138875,8.37291666762259,0.935950539335165));
#5730=CARTESIAN_POINT('Ctrl Pts',(0.810556943750001,8.31458333428925,1.40392580900275));
#5731=CARTESIAN_POINT('Ctrl Pts',(3.43862649647115E-16,8.25625000095592,
1.87190107867033));
#5732=CARTESIAN_POINT('Ctrl Pts',(-0.810556943749999,8.19791666762258,1.40392580900275));
#5733=CARTESIAN_POINT('Ctrl Pts',(-1.6211138875,8.13958333428925,0.935950539335167));
#5734=CARTESIAN_POINT('Ctrl Pts',(-1.6211138875,8.08125000095593,0.));
#5735=CARTESIAN_POINT('Ctrl Pts',(-1.6211138875,8.02291666762259,-0.935950539335166));
#5736=CARTESIAN_POINT('Ctrl Pts',(-0.81055694375,7.96458333428926,-1.40392580900275));
#5737=CARTESIAN_POINT('Ctrl Pts',(-1.14620883215705E-16,7.90625000095592,
-1.87190107867033));
#5738=CARTESIAN_POINT('Ctrl Pts',(0.81055694375,7.84791666762259,-1.40392580900275));
#5739=CARTESIAN_POINT('Ctrl Pts',(1.6211138875,7.78958333428925,-0.935950539335166));
#5740=CARTESIAN_POINT('Ctrl Pts',(1.6211138875,7.73125000095592,-1.9852919333802E-16));
#5741=CARTESIAN_POINT('Ctrl Pts',(1.6211138875,7.67291666762258,0.935950539335165));
#5742=CARTESIAN_POINT('Ctrl Pts',(0.810556943750001,7.61458333428926,1.40392580900275));
#5743=CARTESIAN_POINT('Ctrl Pts',(3.43862649647115E-16,7.55625000095592,
1.87190107867033));
#5744=CARTESIAN_POINT('Ctrl Pts',(-0.810556943749999,7.49791666762259,1.40392580900275));
#5745=CARTESIAN_POINT('Ctrl Pts',(-1.6211138875,7.43958333428925,0.935950539335167));
#5746=CARTESIAN_POINT('Ctrl Pts',(-1.6211138875,7.38125000095592,0.));
#5747=CARTESIAN_POINT('Ctrl Pts',(-1.6211138875,7.3229166676226,-0.935950539335166));
#5748=CARTESIAN_POINT('Ctrl Pts',(-0.81055694375,7.26458333428925,-1.40392580900275));
#5749=CARTESIAN_POINT('Ctrl Pts',(-1.14620883215705E-16,7.20625000095593,
-1.87190107867033));
#5750=CARTESIAN_POINT('Ctrl Pts',(0.81055694375,7.14791666762259,-1.40392580900275));
#5751=CARTESIAN_POINT('Ctrl Pts',(1.6211138875,7.08958333428926,-0.935950539335166));
#5752=CARTESIAN_POINT('Ctrl Pts',(1.6211138875,7.03125000095592,-1.9852919333802E-16));
#5753=CARTESIAN_POINT('Ctrl Pts',(1.6211138875,6.97291666762259,0.935950539335165));
#5754=CARTESIAN_POINT('Ctrl Pts',(0.810556943750001,6.91458333428925,1.40392580900275));
#5755=CARTESIAN_POINT('Ctrl Pts',(3.43862649647115E-16,6.85625000095592,
1.87190107867033));
#5756=CARTESIAN_POINT('Ctrl Pts',(-0.810556943749999,6.79791666762258,1.40392580900275));
#5757=CARTESIAN_POINT('Ctrl Pts',(-1.6211138875,6.73958333428926,0.935950539335167));
#5758=CARTESIAN_POINT('Ctrl Pts',(-1.6211138875,6.68125000095592,0.));
#5759=CARTESIAN_POINT('Ctrl Pts',(-1.6211138875,6.62291666762259,-0.935950539335166));
#5760=CARTESIAN_POINT('Ctrl Pts',(-0.81055694375,6.56458333428925,-1.40392580900275));
#5761=CARTESIAN_POINT('Ctrl Pts',(-1.14620883215705E-16,6.50625000095592,
-1.87190107867033));
#5762=CARTESIAN_POINT('Ctrl Pts',(0.81055694375,6.44791666762259,-1.40392580900275));
#5763=CARTESIAN_POINT('Ctrl Pts',(1.6211138875,6.38958333428925,-0.935950539335166));
#5764=CARTESIAN_POINT('Ctrl Pts',(1.6211138875,6.33125000095593,-1.9852919333802E-16));
#5765=CARTESIAN_POINT('Ctrl Pts',(1.6211138875,6.27291666762259,0.935950539335165));
#5766=CARTESIAN_POINT('Ctrl Pts',(0.810556943750001,6.21458333428926,1.40392580900275));
#5767=CARTESIAN_POINT('Ctrl Pts',(3.43862649647115E-16,6.15625000095592,
1.87190107867033));
#5768=CARTESIAN_POINT('Ctrl Pts',(-0.810556943749999,6.09791666762259,1.40392580900275));
#5769=CARTESIAN_POINT('Ctrl Pts',(-1.6211138875,6.03958333428925,0.935950539335167));
#5770=CARTESIAN_POINT('Ctrl Pts',(-1.6211138875,5.98125000095592,0.));
#5771=CARTESIAN_POINT('Ctrl Pts',(-1.6211138875,5.92291666762258,-0.935950539335166));
#5772=CARTESIAN_POINT('Ctrl Pts',(-0.81055694375,5.86458333428926,-1.40392580900275));
#5773=CARTESIAN_POINT('Ctrl Pts',(-1.14620883215705E-16,5.80625000095591,
-1.87190107867033));
#5774=CARTESIAN_POINT('Ctrl Pts',(0.81055694375,5.74791666762259,-1.40392580900275));
#5775=CARTESIAN_POINT('Ctrl Pts',(1.6211138875,5.68958333428926,-0.935950539335166));
#5776=CARTESIAN_POINT('Ctrl Pts',(1.6211138875,5.63125000095592,-1.9852919333802E-16));
#5777=CARTESIAN_POINT('Ctrl Pts',(1.6211138875,5.57291666762259,0.935950539335165));
#5778=CARTESIAN_POINT('Ctrl Pts',(0.810556943750001,5.51458333428925,1.40392580900275));
#5779=CARTESIAN_POINT('Ctrl Pts',(3.43862649647115E-16,5.45625000095593,
1.87190107867033));
#5780=CARTESIAN_POINT('Ctrl Pts',(-0.810556943749999,5.39791666762259,1.40392580900275));
#5781=CARTESIAN_POINT('Ctrl Pts',(-1.6211138875,5.33958333428926,0.935950539335167));
#5782=CARTESIAN_POINT('Ctrl Pts',(-1.6211138875,5.28125000095592,0.));
#5783=CARTESIAN_POINT('Ctrl Pts',(-1.6211138875,5.22291666762259,-0.935950539335166));
#5784=CARTESIAN_POINT('Ctrl Pts',(-0.81055694375,5.16458333428925,-1.40392580900275));
#5785=CARTESIAN_POINT('Ctrl Pts',(-1.14620883215705E-16,5.10625000095592,
-1.87190107867033));
#5786=CARTESIAN_POINT('Ctrl Pts',(0.81055694375,5.04791666762258,-1.40392580900275));
#5787=CARTESIAN_POINT('Ctrl Pts',(1.6211138875,4.98958333428925,-0.935950539335166));
#5788=CARTESIAN_POINT('Ctrl Pts',(1.6211138875,4.93125000095593,-1.9852919333802E-16));
#5789=CARTESIAN_POINT('Ctrl Pts',(1.6211138875,4.87291666762259,0.935950539335165));
#5790=CARTESIAN_POINT('Ctrl Pts',(0.810556943750001,4.81458333428926,1.40392580900275));
#5791=CARTESIAN_POINT('Ctrl Pts',(3.43862649647115E-16,4.75625000095592,
1.87190107867033));
#5792=CARTESIAN_POINT('Ctrl Pts',(-0.810556943749999,4.69791666762259,1.40392580900275));
#5793=CARTESIAN_POINT('Ctrl Pts',(-1.6211138875,4.63958333428925,0.935950539335167));
#5794=CARTESIAN_POINT('Ctrl Pts',(-1.6211138875,4.58125000095593,0.));
#5795=CARTESIAN_POINT('Ctrl Pts',(-1.6211138875,4.52291666762258,-0.935950539335166));
#5796=CARTESIAN_POINT('Ctrl Pts',(-0.81055694375,4.46458333428926,-1.40392580900275));
#5797=CARTESIAN_POINT('Ctrl Pts',(-1.14620883215705E-16,4.40625000095592,
-1.87190107867033));
#5798=CARTESIAN_POINT('Ctrl Pts',(0.81055694375,4.34791666762259,-1.40392580900275));
#5799=CARTESIAN_POINT('Ctrl Pts',(1.6211138875,4.28958333428925,-0.935950539335166));
#5800=CARTESIAN_POINT('Ctrl Pts',(1.6211138875,4.23125000095592,-1.9852919333802E-16));
#5801=CARTESIAN_POINT('Ctrl Pts',(1.6211138875,4.1729166676226,0.935950539335165));
#5802=CARTESIAN_POINT('Ctrl Pts',(0.810556943750001,4.11458333428925,1.40392580900275));
#5803=CARTESIAN_POINT('Ctrl Pts',(3.43862649647115E-16,4.05625000095593,
1.87190107867033));
#5804=CARTESIAN_POINT('Ctrl Pts',(-0.810556943749999,3.99791666762259,1.40392580900275));
#5805=CARTESIAN_POINT('Ctrl Pts',(-1.6211138875,3.93958333428926,0.935950539335167));
#5806=CARTESIAN_POINT('Ctrl Pts',(-1.6211138875,3.88125000095592,0.));
#5807=CARTESIAN_POINT('Ctrl Pts',(-1.6211138875,3.82291666762259,-0.935950539335166));
#5808=CARTESIAN_POINT('Ctrl Pts',(-0.81055694375,3.76458333428925,-1.40392580900275));
#5809=CARTESIAN_POINT('Ctrl Pts',(-1.14620883215705E-16,3.70625000095592,
-1.87190107867033));
#5810=CARTESIAN_POINT('Ctrl Pts',(0.81055694375,3.64791666762258,-1.40392580900275));
#5811=CARTESIAN_POINT('Ctrl Pts',(1.6211138875,3.58958333428926,-0.935950539335166));
#5812=CARTESIAN_POINT('Ctrl Pts',(1.6211138875,3.53125000095592,-1.9852919333802E-16));
#5813=CARTESIAN_POINT('Ctrl Pts',(1.6211138875,3.47291666762259,0.935950539335165));
#5814=CARTESIAN_POINT('Ctrl Pts',(0.810556943750001,3.41458333428925,1.40392580900275));
#5815=CARTESIAN_POINT('Ctrl Pts',(3.43862649647115E-16,3.35625000095592,
1.87190107867033));
#5816=CARTESIAN_POINT('Ctrl Pts',(-0.810556943749999,3.29791666762259,1.40392580900275));
#5817=CARTESIAN_POINT('Ctrl Pts',(-1.6211138875,3.23958333428925,0.935950539335167));
#5818=CARTESIAN_POINT('Ctrl Pts',(-1.6211138875,3.18125000095593,0.));
#5819=CARTESIAN_POINT('Ctrl Pts',(-1.6211138875,3.12291666762259,-0.935950539335166));
#5820=CARTESIAN_POINT('Ctrl Pts',(-0.81055694375,3.06458333428926,-1.40392580900275));
#5821=CARTESIAN_POINT('Ctrl Pts',(-1.14620883215705E-16,3.00625000095592,
-1.87190107867033));
#5822=CARTESIAN_POINT('Ctrl Pts',(0.81055694375,2.94791666762259,-1.40392580900275));
#5823=CARTESIAN_POINT('Ctrl Pts',(1.6211138875,2.88958333428925,-0.935950539335166));
#5824=CARTESIAN_POINT('Ctrl Pts',(1.6211138875,2.83125000095592,-1.9852919333802E-16));
#5825=CARTESIAN_POINT('Ctrl Pts',(1.6211138875,2.77291666762258,0.935950539335165));
#5826=CARTESIAN_POINT('Ctrl Pts',(0.810556943750001,2.71458333428926,1.40392580900275));
#5827=CARTESIAN_POINT('Ctrl Pts',(3.43862649647115E-16,2.65625000095591,
1.87190107867033));
#5828=CARTESIAN_POINT('Ctrl Pts',(-0.810556943749999,2.59791666762259,1.40392580900275));
#5829=CARTESIAN_POINT('Ctrl Pts',(-1.6211138875,2.53958333428926,0.935950539335167));
#5830=CARTESIAN_POINT('Ctrl Pts',(-1.6211138875,2.48125000095592,0.));
#5831=CARTESIAN_POINT('Ctrl Pts',(-1.6211138875,2.42291666762259,-0.935950539335166));
#5832=CARTESIAN_POINT('Ctrl Pts',(-0.81055694375,2.36458333428925,-1.40392580900275));
#5833=CARTESIAN_POINT('Ctrl Pts',(-1.14620883215705E-16,2.30625000095593,
-1.87190107867033));
#5834=CARTESIAN_POINT('Ctrl Pts',(0.81055694375,2.24791666762258,-1.40392580900275));
#5835=CARTESIAN_POINT('Ctrl Pts',(1.6211138875,2.18958333428926,-0.935950539335166));
#5836=CARTESIAN_POINT('Ctrl Pts',(1.6211138875,2.13125000095592,-1.9852919333802E-16));
#5837=CARTESIAN_POINT('Ctrl Pts',(1.6211138875,2.07291666762259,0.935950539335165));
#5838=CARTESIAN_POINT('Ctrl Pts',(0.810556943750001,2.01458333428925,1.40392580900275));
#5839=CARTESIAN_POINT('Ctrl Pts',(3.43862649647115E-16,1.95625000095592,
1.87190107867033));
#5840=CARTESIAN_POINT('Ctrl Pts',(-0.810556943749999,1.89791666762258,1.40392580900275));
#5841=CARTESIAN_POINT('Ctrl Pts',(-1.6211138875,1.83958333428925,0.935950539335167));
#5842=CARTESIAN_POINT('Ctrl Pts',(-1.6211138875,1.78125000095593,0.));
#5843=CARTESIAN_POINT('Ctrl Pts',(-1.6211138875,1.72291666762259,-0.935950539335166));
#5844=CARTESIAN_POINT('Ctrl Pts',(-0.81055694375,1.66458333428926,-1.40392580900275));
#5845=CARTESIAN_POINT('Ctrl Pts',(-1.14620883215705E-16,1.60625000095592,
-1.87190107867033));
#5846=CARTESIAN_POINT('Ctrl Pts',(0.81055694375,1.54791666762259,-1.40392580900275));
#5847=CARTESIAN_POINT('Ctrl Pts',(1.6211138875,1.48958333428925,-0.935950539335166));
#5848=CARTESIAN_POINT('Ctrl Pts',(1.6211138875,1.43125000095592,-1.9852919333802E-16));
#5849=CARTESIAN_POINT('Ctrl Pts',(1.6211138875,1.37291666762258,0.935950539335165));
#5850=CARTESIAN_POINT('Ctrl Pts',(0.810556943750001,1.31458333428926,1.40392580900275));
#5851=CARTESIAN_POINT('Ctrl Pts',(3.43862649647115E-16,1.25625000095592,
1.87190107867033));
#5852=CARTESIAN_POINT('Ctrl Pts',(-0.810556943749999,1.19791666762259,1.40392580900275));
#5853=CARTESIAN_POINT('Ctrl Pts',(-1.6211138875,1.13958333428925,0.935950539335167));
#5854=CARTESIAN_POINT('Ctrl Pts',(-1.6211138875,1.08125000095592,0.));
#5855=CARTESIAN_POINT('Ctrl Pts',(-1.6211138875,1.02291666762259,-0.935950539335166));
#5856=CARTESIAN_POINT('Ctrl Pts',(-0.81055694375,0.964583334289254,-1.40392580900275));
#5857=CARTESIAN_POINT('Ctrl Pts',(-1.14620883215705E-16,0.906250000955927,
-1.87190107867033));
#5858=CARTESIAN_POINT('Ctrl Pts',(0.81055694375,0.847916667622586,-1.40392580900275));
#5859=CARTESIAN_POINT('Ctrl Pts',(1.6211138875,0.789583334289259,-0.935950539335166));
#5860=CARTESIAN_POINT('Ctrl Pts',(1.6211138875,0.731250000955919,-1.9852919333802E-16));
#5861=CARTESIAN_POINT('Ctrl Pts',(1.6211138875,0.672916667622592,0.935950539335165));
#5862=CARTESIAN_POINT('Ctrl Pts',(0.810556943750001,0.614583334289251,1.40392580900275));
#5863=CARTESIAN_POINT('Ctrl Pts',(3.43862649647115E-16,0.556250000955924,
1.87190107867033));
#5864=CARTESIAN_POINT('Ctrl Pts',(-0.810556943749999,0.497916667622583,
1.40392580900275));
#5865=CARTESIAN_POINT('Ctrl Pts',(-1.6211138875,0.439583334289256,0.935950539335167));
#5866=CARTESIAN_POINT('Ctrl Pts',(-1.6211138875,0.381250000955916,0.));
#5867=CARTESIAN_POINT('Ctrl Pts',(-1.6211138875,0.322916667622589,-0.935950539335166));
#5868=CARTESIAN_POINT('Ctrl Pts',(-0.81055694375,0.264583334289248,-1.40392580900275));
#5869=CARTESIAN_POINT('Ctrl Pts',(-1.14620883215705E-16,0.206250000955921,
-1.87190107867033));
#5870=CARTESIAN_POINT('Ctrl Pts',(0.81055694375,0.147916667622594,-1.40392580900275));
#5871=CARTESIAN_POINT('Ctrl Pts',(1.6211138875,0.0895833342892532,-0.935950539335166));
#5872=CARTESIAN_POINT('Ctrl Pts',(1.6211138875,0.0312500009559263,-1.9852919333802E-16));
#5873=CARTESIAN_POINT('Ctrl Pts',(1.6211138875,-0.0270833323774144,0.935950539335165));
#5874=CARTESIAN_POINT('Ctrl Pts',(0.810556943750001,-0.0854166657107414,
1.40392580900275));
#5875=CARTESIAN_POINT('Ctrl Pts',(3.43862649647115E-16,-0.143749999044082,
1.87190107867033));
#5876=CARTESIAN_POINT('Ctrl Pts',(-0.810556943749999,-0.202083332377409,
1.40392580900275));
#5877=CARTESIAN_POINT('Ctrl Pts',(-1.6211138875,-0.26041666571075,0.935950539335167));
#5878=CARTESIAN_POINT('Ctrl Pts',(-1.6211138875,-0.318749999044077,0.));
#5879=CARTESIAN_POINT('Ctrl Pts',(-1.6211138875,-0.377083332377417,-0.935950539335166));
#5880=CARTESIAN_POINT('Ctrl Pts',(-0.81055694375,-0.435416665710744,-1.40392580900275));
#5881=CARTESIAN_POINT('Ctrl Pts',(-1.14620883215705E-16,-0.493749999044085,
-1.87190107867033));
#5882=CARTESIAN_POINT('Ctrl Pts',(0.81055694375,-0.552083332377412,-1.40392580900275));
#5883=CARTESIAN_POINT('Ctrl Pts',(1.6211138875,-0.610416665710739,-0.935950539335166));
#5884=CARTESIAN_POINT('Ctrl Pts',(1.6211138875,-0.66874999904408,-1.9852919333802E-16));
#5885=CARTESIAN_POINT('Ctrl Pts',(1.6211138875,-0.727083332377407,0.935950539335165));
#5886=CARTESIAN_POINT('Ctrl Pts',(0.810556943750001,-0.785416665710748,
1.40392580900275));
#5887=CARTESIAN_POINT('Ctrl Pts',(3.43862649647115E-16,-0.843749999044074,
1.87190107867033));
#5888=CARTESIAN_POINT('Ctrl Pts',(-0.810556943749999,-0.902083332377415,
1.40392580900275));
#5889=CARTESIAN_POINT('Ctrl Pts',(-1.6211138875,-0.960416665710742,0.935950539335167));
#5890=CARTESIAN_POINT('Ctrl Pts',(-1.6211138875,-1.01874999904408,0.));
#5891=CARTESIAN_POINT('Ctrl Pts',(-1.6211138875,-1.07708333237741,-0.935950539335166));
#5892=CARTESIAN_POINT('Ctrl Pts',(-0.81055694375,-1.13541666571075,-1.40392580900275));
#5893=CARTESIAN_POINT('Ctrl Pts',(-1.14620883215705E-16,-1.19374999904408,
-1.87190107867033));
#5894=CARTESIAN_POINT('Ctrl Pts',(0.81055694375,-1.25208333237742,-1.40392580900275));
#5895=CARTESIAN_POINT('Ctrl Pts',(1.6211138875,-1.31041666571075,-0.935950539335166));
#5896=CARTESIAN_POINT('Ctrl Pts',(1.6211138875,-1.36874999904407,-1.9852919333802E-16));
#5897=CARTESIAN_POINT('Ctrl Pts',(1.6211138875,-1.42708333237741,0.935950539335165));
#5898=CARTESIAN_POINT('Ctrl Pts',(0.810556943750001,-1.48541666571074,1.40392580900275));
#5899=CARTESIAN_POINT('Ctrl Pts',(3.43862649647115E-16,-1.54374999904408,
1.87190107867033));
#5900=CARTESIAN_POINT('Ctrl Pts',(-0.810556943749999,-1.60208333237741,
1.40392580900275));
#5901=CARTESIAN_POINT('Ctrl Pts',(-1.6211138875,-1.66041666571075,0.935950539335167));
#5902=CARTESIAN_POINT('Ctrl Pts',(-1.6211138875,-1.71874999904408,0.));
#5903=CARTESIAN_POINT('Ctrl Pts',(-1.6211138875,-1.77708333237742,-0.935950539335166));
#5904=CARTESIAN_POINT('Ctrl Pts',(-0.81055694375,-1.83541666571074,-1.40392580900275));
#5905=CARTESIAN_POINT('Ctrl Pts',(-1.14620883215705E-16,-1.89374999904408,
-1.87190107867033));
#5906=CARTESIAN_POINT('Ctrl Pts',(0.81055694375,-1.95208333237741,-1.40392580900275));
#5907=CARTESIAN_POINT('Ctrl Pts',(1.6211138875,-2.01041666571075,-0.935950539335166));
#5908=CARTESIAN_POINT('Ctrl Pts',(1.6211138875,-2.06874999904408,-1.9852919333802E-16));
#5909=CARTESIAN_POINT('Ctrl Pts',(1.6211138875,-2.12708333237741,0.935950539335165));
#5910=CARTESIAN_POINT('Ctrl Pts',(0.810556943750001,-2.18541666571075,1.40392580900275));
#5911=CARTESIAN_POINT('Ctrl Pts',(0.598919469048119,-2.20064757509077,1.52611476199249));
#5912=CARTESIAN_POINT('Ctrl Pts',(0.360666377423904,-2.217793929975,1.58048410319158));
#5913=CARTESIAN_POINT('Ctrl Pts',(-2.00000000049539,72.000000000286,0.));
#5914=CARTESIAN_POINT('Ctrl Pts',(-2.00000000049539,71.9416666669527,-1.15470053866527));
#5915=CARTESIAN_POINT('Ctrl Pts',(-1.0000000002477,71.8833333336194,-1.7320508079979));
#5916=CARTESIAN_POINT('Ctrl Pts',(-1.41410031865014E-16,71.825000000286,
-2.30940107733053));
#5917=CARTESIAN_POINT('Ctrl Pts',(1.0000000002477,71.7666666669527,-1.7320508079979));
#5918=CARTESIAN_POINT('Ctrl Pts',(2.00000000049539,71.7083333336194,-1.15470053866527));
#5919=CARTESIAN_POINT('Ctrl Pts',(2.00000000049539,71.650000000286,-2.44929359890139E-16));
#5920=CARTESIAN_POINT('Ctrl Pts',(2.00000000049539,71.5916666669527,1.15470053866527));
#5921=CARTESIAN_POINT('Ctrl Pts',(1.0000000002477,71.5333333336193,1.7320508079979));
#5922=CARTESIAN_POINT('Ctrl Pts',(4.24230095595043E-16,71.475000000286,
2.30940107733053));
#5923=CARTESIAN_POINT('Ctrl Pts',(-1.0000000002477,71.4166666669527,1.7320508079979));
#5924=CARTESIAN_POINT('Ctrl Pts',(-2.00000000049539,71.3583333336194,1.15470053866527));
#5925=CARTESIAN_POINT('Ctrl Pts',(-2.00000000049539,71.300000000286,0.));
#5926=CARTESIAN_POINT('Ctrl Pts',(-2.00000000049539,71.2416666669527,-1.15470053866527));
#5927=CARTESIAN_POINT('Ctrl Pts',(-1.0000000002477,71.1833333336194,-1.7320508079979));
#5928=CARTESIAN_POINT('Ctrl Pts',(-1.41410031865014E-16,71.125000000286,
-2.30940107733053));
#5929=CARTESIAN_POINT('Ctrl Pts',(1.0000000002477,71.0666666669527,-1.7320508079979));
#5930=CARTESIAN_POINT('Ctrl Pts',(2.00000000049539,71.0083333336193,-1.15470053866527));
#5931=CARTESIAN_POINT('Ctrl Pts',(2.00000000049539,70.950000000286,-2.44929359890139E-16));
#5932=CARTESIAN_POINT('Ctrl Pts',(2.00000000049539,70.8916666669527,1.15470053866527));
#5933=CARTESIAN_POINT('Ctrl Pts',(1.0000000002477,70.8333333336194,1.7320508079979));
#5934=CARTESIAN_POINT('Ctrl Pts',(4.24230095595043E-16,70.775000000286,
2.30940107733053));
#5935=CARTESIAN_POINT('Ctrl Pts',(-1.0000000002477,70.7166666669527,1.7320508079979));
#5936=CARTESIAN_POINT('Ctrl Pts',(-2.00000000049539,70.6583333336194,1.15470053866527));
#5937=CARTESIAN_POINT('Ctrl Pts',(-2.00000000049539,70.600000000286,0.));
#5938=CARTESIAN_POINT('Ctrl Pts',(-2.00000000049539,70.5416666669527,-1.15470053866527));
#5939=CARTESIAN_POINT('Ctrl Pts',(-1.0000000002477,70.4833333336194,-1.7320508079979));
#5940=CARTESIAN_POINT('Ctrl Pts',(-1.41410031865014E-16,70.425000000286,
-2.30940107733053));
#5941=CARTESIAN_POINT('Ctrl Pts',(1.0000000002477,70.3666666669527,-1.7320508079979));
#5942=CARTESIAN_POINT('Ctrl Pts',(2.00000000049539,70.3083333336194,-1.15470053866527));
#5943=CARTESIAN_POINT('Ctrl Pts',(2.00000000049539,70.250000000286,-2.44929359890139E-16));
#5944=CARTESIAN_POINT('Ctrl Pts',(2.00000000049539,70.1916666669527,1.15470053866527));
#5945=CARTESIAN_POINT('Ctrl Pts',(1.0000000002477,70.1333333336194,1.7320508079979));
#5946=CARTESIAN_POINT('Ctrl Pts',(4.24230095595043E-16,70.075000000286,
2.30940107733053));
#5947=CARTESIAN_POINT('Ctrl Pts',(-1.0000000002477,70.0166666669527,1.7320508079979));
#5948=CARTESIAN_POINT('Ctrl Pts',(-2.00000000049539,69.9583333336194,1.15470053866527));
#5949=CARTESIAN_POINT('Ctrl Pts',(-2.00000000049539,69.900000000286,0.));
#5950=CARTESIAN_POINT('Ctrl Pts',(-2.00000000049539,69.8416666669527,-1.15470053866527));
#5951=CARTESIAN_POINT('Ctrl Pts',(-1.0000000002477,69.7833333336193,-1.7320508079979));
#5952=CARTESIAN_POINT('Ctrl Pts',(-1.41410031865014E-16,69.725000000286,
-2.30940107733053));
#5953=CARTESIAN_POINT('Ctrl Pts',(1.0000000002477,69.6666666669527,-1.7320508079979));
#5954=CARTESIAN_POINT('Ctrl Pts',(2.00000000049539,69.6083333336193,-1.15470053866527));
#5955=CARTESIAN_POINT('Ctrl Pts',(2.00000000049539,69.550000000286,-2.44929359890139E-16));
#5956=CARTESIAN_POINT('Ctrl Pts',(2.00000000049539,69.4916666669527,1.15470053866527));
#5957=CARTESIAN_POINT('Ctrl Pts',(1.0000000002477,69.4333333336194,1.7320508079979));
#5958=CARTESIAN_POINT('Ctrl Pts',(4.24230095595043E-16,69.375000000286,
2.30940107733053));
#5959=CARTESIAN_POINT('Ctrl Pts',(-1.0000000002477,69.3166666669527,1.7320508079979));
#5960=CARTESIAN_POINT('Ctrl Pts',(-2.00000000049539,69.2583333336193,1.15470053866527));
#5961=CARTESIAN_POINT('Ctrl Pts',(-2.00000000049539,69.200000000286,0.));
#5962=CARTESIAN_POINT('Ctrl Pts',(-2.00000000049539,69.1416666669527,-1.15470053866527));
#5963=CARTESIAN_POINT('Ctrl Pts',(-1.0000000002477,69.0833333336194,-1.7320508079979));
#5964=CARTESIAN_POINT('Ctrl Pts',(-1.41410031865014E-16,69.025000000286,
-2.30940107733053));
#5965=CARTESIAN_POINT('Ctrl Pts',(1.0000000002477,68.9666666669527,-1.7320508079979));
#5966=CARTESIAN_POINT('Ctrl Pts',(2.00000000049539,68.9083333336194,-1.15470053866527));
#5967=CARTESIAN_POINT('Ctrl Pts',(2.00000000049539,68.850000000286,-2.44929359890139E-16));
#5968=CARTESIAN_POINT('Ctrl Pts',(2.00000000049539,68.7916666669527,1.15470053866527));
#5969=CARTESIAN_POINT('Ctrl Pts',(1.0000000002477,68.7333333336194,1.7320508079979));
#5970=CARTESIAN_POINT('Ctrl Pts',(4.24230095595043E-16,68.675000000286,
2.30940107733053));
#5971=CARTESIAN_POINT('Ctrl Pts',(-1.0000000002477,68.6166666669527,1.7320508079979));
#5972=CARTESIAN_POINT('Ctrl Pts',(-2.00000000049539,68.5583333336194,1.15470053866527));
#5973=CARTESIAN_POINT('Ctrl Pts',(-2.00000000049539,68.500000000286,0.));
#5974=CARTESIAN_POINT('Ctrl Pts',(-2.00000000049539,68.4416666669527,-1.15470053866527));
#5975=CARTESIAN_POINT('Ctrl Pts',(-1.0000000002477,68.3833333336194,-1.7320508079979));
#5976=CARTESIAN_POINT('Ctrl Pts',(-1.41410031865014E-16,68.325000000286,
-2.30940107733053));
#5977=CARTESIAN_POINT('Ctrl Pts',(1.0000000002477,68.2666666669527,-1.7320508079979));
#5978=CARTESIAN_POINT('Ctrl Pts',(2.00000000049539,68.2083333336194,-1.15470053866527));
#5979=CARTESIAN_POINT('Ctrl Pts',(2.00000000049539,68.150000000286,-2.44929359890139E-16));
#5980=CARTESIAN_POINT('Ctrl Pts',(2.00000000049539,68.0916666669527,1.15470053866527));
#5981=CARTESIAN_POINT('Ctrl Pts',(1.0000000002477,68.0333333336194,1.7320508079979));
#5982=CARTESIAN_POINT('Ctrl Pts',(4.24230095595043E-16,67.975000000286,
2.30940107733053));
#5983=CARTESIAN_POINT('Ctrl Pts',(-1.0000000002477,67.9166666669527,1.7320508079979));
#5984=CARTESIAN_POINT('Ctrl Pts',(-2.00000000049539,67.8583333336194,1.15470053866527));
#5985=CARTESIAN_POINT('Ctrl Pts',(-2.00000000049539,67.800000000286,0.));
#5986=CARTESIAN_POINT('Ctrl Pts',(-2.00000000049539,67.7416666669527,-1.15470053866527));
#5987=CARTESIAN_POINT('Ctrl Pts',(-1.0000000002477,67.6833333336194,-1.7320508079979));
#5988=CARTESIAN_POINT('Ctrl Pts',(-1.41410031865014E-16,67.625000000286,
-2.30940107733053));
#5989=CARTESIAN_POINT('Ctrl Pts',(1.0000000002477,67.5666666669527,-1.7320508079979));
#5990=CARTESIAN_POINT('Ctrl Pts',(2.00000000049539,67.5083333336193,-1.15470053866527));
#5991=CARTESIAN_POINT('Ctrl Pts',(2.00000000049539,67.450000000286,-2.44929359890139E-16));
#5992=CARTESIAN_POINT('Ctrl Pts',(2.00000000049539,67.3916666669527,1.15470053866527));
#5993=CARTESIAN_POINT('Ctrl Pts',(1.0000000002477,67.3333333336194,1.7320508079979));
#5994=CARTESIAN_POINT('Ctrl Pts',(4.24230095595043E-16,67.275000000286,
2.30940107733053));
#5995=CARTESIAN_POINT('Ctrl Pts',(-1.0000000002477,67.2166666669527,1.7320508079979));
#5996=CARTESIAN_POINT('Ctrl Pts',(-2.00000000049539,67.1583333336194,1.15470053866527));
#5997=CARTESIAN_POINT('Ctrl Pts',(-2.00000000049539,67.100000000286,0.));
#5998=CARTESIAN_POINT('Ctrl Pts',(-2.00000000049539,67.0416666669527,-1.15470053866527));
#5999=CARTESIAN_POINT('Ctrl Pts',(-1.0000000002477,66.9833333336194,-1.7320508079979));
#6000=CARTESIAN_POINT('Ctrl Pts',(-1.41410031865014E-16,66.925000000286,
-2.30940107733053));
#6001=CARTESIAN_POINT('Ctrl Pts',(1.0000000002477,66.8666666669527,-1.7320508079979));
#6002=CARTESIAN_POINT('Ctrl Pts',(2.00000000049539,66.8083333336194,-1.15470053866527));
#6003=CARTESIAN_POINT('Ctrl Pts',(2.00000000049539,66.750000000286,-2.44929359890139E-16));
#6004=CARTESIAN_POINT('Ctrl Pts',(2.00000000049539,66.6916666669527,1.15470053866527));
#6005=CARTESIAN_POINT('Ctrl Pts',(1.0000000002477,66.6333333336194,1.7320508079979));
#6006=CARTESIAN_POINT('Ctrl Pts',(4.24230095595043E-16,66.575000000286,
2.30940107733053));
#6007=CARTESIAN_POINT('Ctrl Pts',(-1.0000000002477,66.5166666669527,1.7320508079979));
#6008=CARTESIAN_POINT('Ctrl Pts',(-2.00000000049539,66.4583333336194,1.15470053866527));
#6009=CARTESIAN_POINT('Ctrl Pts',(-2.00000000049539,66.400000000286,0.));
#6010=CARTESIAN_POINT('Ctrl Pts',(-2.00000000049539,66.3416666669527,-1.15470053866527));
#6011=CARTESIAN_POINT('Ctrl Pts',(-1.0000000002477,66.2833333336194,-1.7320508079979));
#6012=CARTESIAN_POINT('Ctrl Pts',(-1.41410031865014E-16,66.225000000286,
-2.30940107733053));
#6013=CARTESIAN_POINT('Ctrl Pts',(1.0000000002477,66.1666666669527,-1.7320508079979));
#6014=CARTESIAN_POINT('Ctrl Pts',(2.00000000049539,66.1083333336194,-1.15470053866527));
#6015=CARTESIAN_POINT('Ctrl Pts',(2.00000000049539,66.050000000286,-2.44929359890139E-16));
#6016=CARTESIAN_POINT('Ctrl Pts',(2.00000000049539,65.9916666669527,1.15470053866527));
#6017=CARTESIAN_POINT('Ctrl Pts',(1.0000000002477,65.9333333336193,1.7320508079979));
#6018=CARTESIAN_POINT('Ctrl Pts',(4.24230095595043E-16,65.875000000286,
2.30940107733053));
#6019=CARTESIAN_POINT('Ctrl Pts',(-1.0000000002477,65.8166666669527,1.7320508079979));
#6020=CARTESIAN_POINT('Ctrl Pts',(-2.00000000049539,65.7583333336193,1.15470053866527));
#6021=CARTESIAN_POINT('Ctrl Pts',(-2.00000000049539,65.700000000286,0.));
#6022=CARTESIAN_POINT('Ctrl Pts',(-2.00000000049539,65.6416666669527,-1.15470053866527));
#6023=CARTESIAN_POINT('Ctrl Pts',(-1.0000000002477,65.5833333336194,-1.7320508079979));
#6024=CARTESIAN_POINT('Ctrl Pts',(-1.41410031865014E-16,65.525000000286,
-2.30940107733053));
#6025=CARTESIAN_POINT('Ctrl Pts',(1.0000000002477,65.4666666669527,-1.7320508079979));
#6026=CARTESIAN_POINT('Ctrl Pts',(2.00000000049539,65.4083333336194,-1.15470053866527));
#6027=CARTESIAN_POINT('Ctrl Pts',(2.00000000049539,65.350000000286,-2.44929359890139E-16));
#6028=CARTESIAN_POINT('Ctrl Pts',(2.00000000049539,65.2916666669527,1.15470053866527));
#6029=CARTESIAN_POINT('Ctrl Pts',(1.0000000002477,65.2333333336193,1.7320508079979));
#6030=CARTESIAN_POINT('Ctrl Pts',(4.24230095595043E-16,65.175000000286,
2.30940107733053));
#6031=CARTESIAN_POINT('Ctrl Pts',(-1.0000000002477,65.1166666669527,1.7320508079979));
#6032=CARTESIAN_POINT('Ctrl Pts',(-2.00000000049539,65.0583333336194,1.15470053866527));
#6033=CARTESIAN_POINT('Ctrl Pts',(-2.00000000049539,65.000000000286,0.));
#6034=CARTESIAN_POINT('Ctrl Pts',(-2.00000000049539,64.9416666669527,-1.15470053866527));
#6035=CARTESIAN_POINT('Ctrl Pts',(-1.0000000002477,64.8833333336194,-1.7320508079979));
#6036=CARTESIAN_POINT('Ctrl Pts',(-1.41410031865014E-16,64.825000000286,
-2.30940107733053));
#6037=CARTESIAN_POINT('Ctrl Pts',(1.0000000002477,64.7666666669527,-1.7320508079979));
#6038=CARTESIAN_POINT('Ctrl Pts',(2.00000000049539,64.7083333336194,-1.15470053866527));
#6039=CARTESIAN_POINT('Ctrl Pts',(2.00000000049539,64.650000000286,-2.44929359890139E-16));
#6040=CARTESIAN_POINT('Ctrl Pts',(2.00000000049539,64.5916666669527,1.15470053866527));
#6041=CARTESIAN_POINT('Ctrl Pts',(1.0000000002477,64.5333333336194,1.7320508079979));
#6042=CARTESIAN_POINT('Ctrl Pts',(4.24230095595043E-16,64.475000000286,
2.30940107733053));
#6043=CARTESIAN_POINT('Ctrl Pts',(-1.0000000002477,64.4166666669527,1.7320508079979));
#6044=CARTESIAN_POINT('Ctrl Pts',(-2.00000000049539,64.3583333336194,1.15470053866527));
#6045=CARTESIAN_POINT('Ctrl Pts',(-2.00000000049539,64.300000000286,0.));
#6046=CARTESIAN_POINT('Ctrl Pts',(-2.00000000049539,64.2416666669527,-1.15470053866527));
#6047=CARTESIAN_POINT('Ctrl Pts',(-1.0000000002477,64.1833333336193,-1.7320508079979));
#6048=CARTESIAN_POINT('Ctrl Pts',(-1.41410031865014E-16,64.125000000286,
-2.30940107733053));
#6049=CARTESIAN_POINT('Ctrl Pts',(1.0000000002477,64.0666666669527,-1.7320508079979));
#6050=CARTESIAN_POINT('Ctrl Pts',(2.00000000049539,64.0083333336194,-1.15470053866527));
#6051=CARTESIAN_POINT('Ctrl Pts',(2.00000000049539,63.950000000286,-2.44929359890139E-16));
#6052=CARTESIAN_POINT('Ctrl Pts',(2.00000000049539,63.8916666669527,1.15470053866527));
#6053=CARTESIAN_POINT('Ctrl Pts',(1.0000000002477,63.8333333336194,1.7320508079979));
#6054=CARTESIAN_POINT('Ctrl Pts',(4.24230095595043E-16,63.775000000286,
2.30940107733053));
#6055=CARTESIAN_POINT('Ctrl Pts',(-1.0000000002477,63.7166666669527,1.7320508079979));
#6056=CARTESIAN_POINT('Ctrl Pts',(-2.00000000049539,63.6583333336194,1.15470053866527));
#6057=CARTESIAN_POINT('Ctrl Pts',(-2.00000000049539,63.600000000286,0.));
#6058=CARTESIAN_POINT('Ctrl Pts',(-2.00000000049539,63.5416666669527,-1.15470053866527));
#6059=CARTESIAN_POINT('Ctrl Pts',(-1.0000000002477,63.4833333336193,-1.7320508079979));
#6060=CARTESIAN_POINT('Ctrl Pts',(-1.41410031865014E-16,63.425000000286,
-2.30940107733053));
#6061=CARTESIAN_POINT('Ctrl Pts',(1.0000000002477,63.3666666669527,-1.7320508079979));
#6062=CARTESIAN_POINT('Ctrl Pts',(2.00000000049539,63.3083333336194,-1.15470053866527));
#6063=CARTESIAN_POINT('Ctrl Pts',(2.00000000049539,63.250000000286,-2.44929359890139E-16));
#6064=CARTESIAN_POINT('Ctrl Pts',(2.00000000049539,63.1916666669527,1.15470053866527));
#6065=CARTESIAN_POINT('Ctrl Pts',(1.0000000002477,63.1333333336194,1.7320508079979));
#6066=CARTESIAN_POINT('Ctrl Pts',(4.24230095595043E-16,63.075000000286,
2.30940107733053));
#6067=CARTESIAN_POINT('Ctrl Pts',(-1.0000000002477,63.0166666669527,1.7320508079979));
#6068=CARTESIAN_POINT('Ctrl Pts',(-2.00000000049539,62.9583333336194,1.15470053866527));
#6069=CARTESIAN_POINT('Ctrl Pts',(-2.00000000049539,62.900000000286,0.));
#6070=CARTESIAN_POINT('Ctrl Pts',(-2.00000000049539,62.8416666669527,-1.15470053866527));
#6071=CARTESIAN_POINT('Ctrl Pts',(-1.0000000002477,62.7833333336194,-1.7320508079979));
#6072=CARTESIAN_POINT('Ctrl Pts',(-1.41410031865014E-16,62.725000000286,
-2.30940107733053));
#6073=CARTESIAN_POINT('Ctrl Pts',(1.0000000002477,62.6666666669527,-1.7320508079979));
#6074=CARTESIAN_POINT('Ctrl Pts',(2.00000000049539,62.6083333336194,-1.15470053866527));
#6075=CARTESIAN_POINT('Ctrl Pts',(2.00000000049539,62.550000000286,-2.44929359890139E-16));
#6076=CARTESIAN_POINT('Ctrl Pts',(2.00000000049539,62.4916666669527,1.15470053866527));
#6077=CARTESIAN_POINT('Ctrl Pts',(1.0000000002477,62.4333333336194,1.7320508079979));
#6078=CARTESIAN_POINT('Ctrl Pts',(4.24230095595043E-16,62.375000000286,
2.30940107733053));
#6079=CARTESIAN_POINT('Ctrl Pts',(-1.0000000002477,62.3166666669527,1.7320508079979));
#6080=CARTESIAN_POINT('Ctrl Pts',(-2.00000000049539,62.2583333336194,1.15470053866527));
#6081=CARTESIAN_POINT('Ctrl Pts',(-2.00000000049539,62.200000000286,0.));
#6082=CARTESIAN_POINT('Ctrl Pts',(-2.00000000049539,62.1416666669527,-1.15470053866527));
#6083=CARTESIAN_POINT('Ctrl Pts',(-1.0000000002477,62.0833333336194,-1.7320508079979));
#6084=CARTESIAN_POINT('Ctrl Pts',(-1.41410031865014E-16,62.025000000286,
-2.30940107733053));
#6085=CARTESIAN_POINT('Ctrl Pts',(1.0000000002477,61.9666666669527,-1.7320508079979));
#6086=CARTESIAN_POINT('Ctrl Pts',(2.00000000049539,61.9083333336194,-1.15470053866527));
#6087=CARTESIAN_POINT('Ctrl Pts',(2.00000000049539,61.850000000286,-2.44929359890139E-16));
#6088=CARTESIAN_POINT('Ctrl Pts',(2.00000000049539,61.7916666669527,1.15470053866527));
#6089=CARTESIAN_POINT('Ctrl Pts',(1.0000000002477,61.7333333336194,1.7320508079979));
#6090=CARTESIAN_POINT('Ctrl Pts',(4.24230095595043E-16,61.675000000286,
2.30940107733053));
#6091=CARTESIAN_POINT('Ctrl Pts',(-1.0000000002477,61.6166666669527,1.7320508079979));
#6092=CARTESIAN_POINT('Ctrl Pts',(-2.00000000049539,61.5583333336193,1.15470053866527));
#6093=CARTESIAN_POINT('Ctrl Pts',(-2.00000000049539,61.500000000286,0.));
#6094=CARTESIAN_POINT('Ctrl Pts',(-2.00000000049539,61.4416666669527,-1.15470053866527));
#6095=CARTESIAN_POINT('Ctrl Pts',(-1.0000000002477,61.3833333336194,-1.7320508079979));
#6096=CARTESIAN_POINT('Ctrl Pts',(-1.41410031865014E-16,61.325000000286,
-2.30940107733053));
#6097=CARTESIAN_POINT('Ctrl Pts',(1.0000000002477,61.2666666669527,-1.7320508079979));
#6098=CARTESIAN_POINT('Ctrl Pts',(2.00000000049539,61.2083333336194,-1.15470053866527));
#6099=CARTESIAN_POINT('Ctrl Pts',(2.00000000049539,61.150000000286,-2.44929359890139E-16));
#6100=CARTESIAN_POINT('Ctrl Pts',(2.00000000049539,61.0916666669527,1.15470053866527));
#6101=CARTESIAN_POINT('Ctrl Pts',(1.0000000002477,61.0333333336194,1.7320508079979));
#6102=CARTESIAN_POINT('Ctrl Pts',(4.24230095595043E-16,60.975000000286,
2.30940107733053));
#6103=CARTESIAN_POINT('Ctrl Pts',(-1.0000000002477,60.9166666669527,1.7320508079979));
#6104=CARTESIAN_POINT('Ctrl Pts',(-2.00000000049539,60.8583333336194,1.15470053866527));
#6105=CARTESIAN_POINT('Ctrl Pts',(-2.00000000049539,60.800000000286,0.));
#6106=CARTESIAN_POINT('Ctrl Pts',(-2.00000000049539,60.7416666669527,-1.15470053866527));
#6107=CARTESIAN_POINT('Ctrl Pts',(-1.0000000002477,60.6833333336194,-1.7320508079979));
#6108=CARTESIAN_POINT('Ctrl Pts',(-1.41410031865014E-16,60.625000000286,
-2.30940107733053));
#6109=CARTESIAN_POINT('Ctrl Pts',(1.0000000002477,60.5666666669527,-1.7320508079979));
#6110=CARTESIAN_POINT('Ctrl Pts',(2.00000000049539,60.5083333336194,-1.15470053866527));
#6111=CARTESIAN_POINT('Ctrl Pts',(2.00000000049539,60.450000000286,-2.44929359890139E-16));
#6112=CARTESIAN_POINT('Ctrl Pts',(2.00000000049539,60.3916666669527,1.15470053866527));
#6113=CARTESIAN_POINT('Ctrl Pts',(1.0000000002477,60.3333333336194,1.7320508079979));
#6114=CARTESIAN_POINT('Ctrl Pts',(4.24230095595043E-16,60.275000000286,
2.30940107733053));
#6115=CARTESIAN_POINT('Ctrl Pts',(-1.0000000002477,60.2166666669527,1.7320508079979));
#6116=CARTESIAN_POINT('Ctrl Pts',(-2.00000000049539,60.1583333336194,1.15470053866527));
#6117=CARTESIAN_POINT('Ctrl Pts',(-2.00000000049539,60.100000000286,0.));
#6118=CARTESIAN_POINT('Ctrl Pts',(-2.00000000049539,60.0416666669527,-1.15470053866527));
#6119=CARTESIAN_POINT('Ctrl Pts',(-1.0000000002477,59.9833333336194,-1.7320508079979));
#6120=CARTESIAN_POINT('Ctrl Pts',(-1.41410031865014E-16,59.925000000286,
-2.30940107733053));
#6121=CARTESIAN_POINT('Ctrl Pts',(1.0000000002477,59.8666666669527,-1.7320508079979));
#6122=CARTESIAN_POINT('Ctrl Pts',(2.00000000049539,59.8083333336194,-1.15470053866527));
#6123=CARTESIAN_POINT('Ctrl Pts',(2.00000000049539,59.750000000286,-2.44929359890139E-16));
#6124=CARTESIAN_POINT('Ctrl Pts',(2.00000000049539,59.6916666669527,1.15470053866527));
#6125=CARTESIAN_POINT('Ctrl Pts',(1.0000000002477,59.6333333336194,1.7320508079979));
#6126=CARTESIAN_POINT('Ctrl Pts',(4.24230095595043E-16,59.575000000286,
2.30940107733053));
#6127=CARTESIAN_POINT('Ctrl Pts',(-1.0000000002477,59.5166666669527,1.7320508079979));
#6128=CARTESIAN_POINT('Ctrl Pts',(-2.00000000049539,59.4583333336194,1.15470053866527));
#6129=CARTESIAN_POINT('Ctrl Pts',(-2.00000000049539,59.400000000286,0.));
#6130=CARTESIAN_POINT('Ctrl Pts',(-2.00000000049539,59.3416666669527,-1.15470053866527));
#6131=CARTESIAN_POINT('Ctrl Pts',(-1.0000000002477,59.2833333336194,-1.7320508079979));
#6132=CARTESIAN_POINT('Ctrl Pts',(-1.41410031865014E-16,59.225000000286,
-2.30940107733053));
#6133=CARTESIAN_POINT('Ctrl Pts',(1.0000000002477,59.1666666669527,-1.7320508079979));
#6134=CARTESIAN_POINT('Ctrl Pts',(2.00000000049539,59.1083333336194,-1.15470053866527));
#6135=CARTESIAN_POINT('Ctrl Pts',(2.00000000049539,59.050000000286,-2.44929359890139E-16));
#6136=CARTESIAN_POINT('Ctrl Pts',(2.00000000049539,58.9916666669527,1.15470053866527));
#6137=CARTESIAN_POINT('Ctrl Pts',(1.0000000002477,58.9333333336194,1.7320508079979));
#6138=CARTESIAN_POINT('Ctrl Pts',(4.24230095595043E-16,58.875000000286,
2.30940107733053));
#6139=CARTESIAN_POINT('Ctrl Pts',(-1.0000000002477,58.8166666669527,1.7320508079979));
#6140=CARTESIAN_POINT('Ctrl Pts',(-2.00000000049539,58.7583333336194,1.15470053866527));
#6141=CARTESIAN_POINT('Ctrl Pts',(-2.00000000049539,58.700000000286,0.));
#6142=CARTESIAN_POINT('Ctrl Pts',(-2.00000000049539,58.6416666669527,-1.15470053866527));
#6143=CARTESIAN_POINT('Ctrl Pts',(-1.0000000002477,58.5833333336194,-1.7320508079979));
#6144=CARTESIAN_POINT('Ctrl Pts',(-1.41410031865014E-16,58.525000000286,
-2.30940107733053));
#6145=CARTESIAN_POINT('Ctrl Pts',(1.0000000002477,58.4666666669527,-1.7320508079979));
#6146=CARTESIAN_POINT('Ctrl Pts',(2.00000000049539,58.4083333336194,-1.15470053866527));
#6147=CARTESIAN_POINT('Ctrl Pts',(2.00000000049539,58.350000000286,-2.44929359890139E-16));
#6148=CARTESIAN_POINT('Ctrl Pts',(2.00000000049539,58.2916666669527,1.15470053866527));
#6149=CARTESIAN_POINT('Ctrl Pts',(1.0000000002477,58.2333333336194,1.7320508079979));
#6150=CARTESIAN_POINT('Ctrl Pts',(4.24230095595043E-16,58.175000000286,
2.30940107733053));
#6151=CARTESIAN_POINT('Ctrl Pts',(-1.0000000002477,58.1166666669527,1.7320508079979));
#6152=CARTESIAN_POINT('Ctrl Pts',(-2.00000000049539,58.0583333336194,1.15470053866527));
#6153=CARTESIAN_POINT('Ctrl Pts',(-2.00000000049539,58.000000000286,0.));
#6154=CARTESIAN_POINT('Ctrl Pts',(-2.00000000049539,57.9416666669527,-1.15470053866527));
#6155=CARTESIAN_POINT('Ctrl Pts',(-1.0000000002477,57.8833333336193,-1.7320508079979));
#6156=CARTESIAN_POINT('Ctrl Pts',(-1.41410031865014E-16,57.825000000286,
-2.30940107733053));
#6157=CARTESIAN_POINT('Ctrl Pts',(1.0000000002477,57.7666666669527,-1.7320508079979));
#6158=CARTESIAN_POINT('Ctrl Pts',(2.00000000049539,57.7083333336194,-1.15470053866527));
#6159=CARTESIAN_POINT('Ctrl Pts',(2.00000000049539,57.650000000286,-2.44929359890139E-16));
#6160=CARTESIAN_POINT('Ctrl Pts',(2.00000000049539,57.5916666669527,1.15470053866527));
#6161=CARTESIAN_POINT('Ctrl Pts',(1.0000000002477,57.5333333336194,1.7320508079979));
#6162=CARTESIAN_POINT('Ctrl Pts',(4.24230095595043E-16,57.475000000286,
2.30940107733053));
#6163=CARTESIAN_POINT('Ctrl Pts',(-1.0000000002477,57.4166666669527,1.7320508079979));
#6164=CARTESIAN_POINT('Ctrl Pts',(-2.00000000049539,57.3583333336194,1.15470053866527));
#6165=CARTESIAN_POINT('Ctrl Pts',(-2.00000000049539,57.300000000286,0.));
#6166=CARTESIAN_POINT('Ctrl Pts',(-2.00000000049539,57.2416666669527,-1.15470053866527));
#6167=CARTESIAN_POINT('Ctrl Pts',(-1.0000000002477,57.1833333336194,-1.7320508079979));
#6168=CARTESIAN_POINT('Ctrl Pts',(-1.41410031865014E-16,57.125000000286,
-2.30940107733053));
#6169=CARTESIAN_POINT('Ctrl Pts',(1.0000000002477,57.0666666669527,-1.7320508079979));
#6170=CARTESIAN_POINT('Ctrl Pts',(2.00000000049539,57.0083333336194,-1.15470053866527));
#6171=CARTESIAN_POINT('Ctrl Pts',(2.00000000049539,56.950000000286,-2.44929359890139E-16));
#6172=CARTESIAN_POINT('Ctrl Pts',(2.00000000049539,56.8916666669527,1.15470053866527));
#6173=CARTESIAN_POINT('Ctrl Pts',(1.0000000002477,56.8333333336194,1.7320508079979));
#6174=CARTESIAN_POINT('Ctrl Pts',(4.24230095595043E-16,56.775000000286,
2.30940107733053));
#6175=CARTESIAN_POINT('Ctrl Pts',(-1.0000000002477,56.7166666669527,1.7320508079979));
#6176=CARTESIAN_POINT('Ctrl Pts',(-2.00000000049539,56.6583333336194,1.15470053866527));
#6177=CARTESIAN_POINT('Ctrl Pts',(-2.00000000049539,56.600000000286,0.));
#6178=CARTESIAN_POINT('Ctrl Pts',(-2.00000000049539,56.5416666669527,-1.15470053866527));
#6179=CARTESIAN_POINT('Ctrl Pts',(-1.0000000002477,56.4833333336194,-1.7320508079979));
#6180=CARTESIAN_POINT('Ctrl Pts',(-1.41410031865014E-16,56.425000000286,
-2.30940107733053));
#6181=CARTESIAN_POINT('Ctrl Pts',(1.0000000002477,56.3666666669527,-1.7320508079979));
#6182=CARTESIAN_POINT('Ctrl Pts',(2.00000000049539,56.3083333336194,-1.15470053866527));
#6183=CARTESIAN_POINT('Ctrl Pts',(2.00000000049539,56.250000000286,-2.44929359890139E-16));
#6184=CARTESIAN_POINT('Ctrl Pts',(2.00000000049539,56.1916666669527,1.15470053866527));
#6185=CARTESIAN_POINT('Ctrl Pts',(1.0000000002477,56.1333333336194,1.7320508079979));
#6186=CARTESIAN_POINT('Ctrl Pts',(4.24230095595043E-16,56.075000000286,
2.30940107733053));
#6187=CARTESIAN_POINT('Ctrl Pts',(-1.0000000002477,56.0166666669527,1.7320508079979));
#6188=CARTESIAN_POINT('Ctrl Pts',(-2.00000000049539,55.9583333336194,1.15470053866527));
#6189=CARTESIAN_POINT('Ctrl Pts',(-2.00000000049539,55.900000000286,0.));
#6190=CARTESIAN_POINT('Ctrl Pts',(-2.00000000049539,55.8416666669527,-1.15470053866527));
#6191=CARTESIAN_POINT('Ctrl Pts',(-1.0000000002477,55.7833333336194,-1.7320508079979));
#6192=CARTESIAN_POINT('Ctrl Pts',(-1.41410031865014E-16,55.725000000286,
-2.30940107733053));
#6193=CARTESIAN_POINT('Ctrl Pts',(1.0000000002477,55.6666666669527,-1.7320508079979));
#6194=CARTESIAN_POINT('Ctrl Pts',(2.00000000049539,55.6083333336194,-1.15470053866527));
#6195=CARTESIAN_POINT('Ctrl Pts',(2.00000000049539,55.550000000286,-2.44929359890139E-16));
#6196=CARTESIAN_POINT('Ctrl Pts',(2.00000000049539,55.4916666669527,1.15470053866527));
#6197=CARTESIAN_POINT('Ctrl Pts',(1.0000000002477,55.4333333336194,1.7320508079979));
#6198=CARTESIAN_POINT('Ctrl Pts',(4.24230095595043E-16,55.375000000286,
2.30940107733053));
#6199=CARTESIAN_POINT('Ctrl Pts',(-1.0000000002477,55.3166666669527,1.7320508079979));
#6200=CARTESIAN_POINT('Ctrl Pts',(-2.00000000049539,55.2583333336194,1.15470053866527));
#6201=CARTESIAN_POINT('Ctrl Pts',(-2.00000000049539,55.200000000286,0.));
#6202=CARTESIAN_POINT('Ctrl Pts',(-2.00000000049539,55.1416666669527,-1.15470053866527));
#6203=CARTESIAN_POINT('Ctrl Pts',(-1.0000000002477,55.0833333336194,-1.7320508079979));
#6204=CARTESIAN_POINT('Ctrl Pts',(-1.41410031865014E-16,55.025000000286,
-2.30940107733053));
#6205=CARTESIAN_POINT('Ctrl Pts',(1.0000000002477,54.9666666669527,-1.7320508079979));
#6206=CARTESIAN_POINT('Ctrl Pts',(2.00000000049539,54.9083333336194,-1.15470053866527));
#6207=CARTESIAN_POINT('Ctrl Pts',(2.00000000049539,54.850000000286,-2.44929359890139E-16));
#6208=CARTESIAN_POINT('Ctrl Pts',(2.00000000049539,54.7916666669527,1.15470053866527));
#6209=CARTESIAN_POINT('Ctrl Pts',(1.0000000002477,54.7333333336194,1.7320508079979));
#6210=CARTESIAN_POINT('Ctrl Pts',(4.24230095595043E-16,54.675000000286,
2.30940107733053));
#6211=CARTESIAN_POINT('Ctrl Pts',(-1.0000000002477,54.6166666669527,1.7320508079979));
#6212=CARTESIAN_POINT('Ctrl Pts',(-2.00000000049539,54.5583333336194,1.15470053866527));
#6213=CARTESIAN_POINT('Ctrl Pts',(-2.00000000049539,54.500000000286,0.));
#6214=CARTESIAN_POINT('Ctrl Pts',(-2.00000000049539,54.4416666669527,-1.15470053866527));
#6215=CARTESIAN_POINT('Ctrl Pts',(-1.0000000002477,54.3833333336194,-1.7320508079979));
#6216=CARTESIAN_POINT('Ctrl Pts',(-1.41410031865014E-16,54.325000000286,
-2.30940107733053));
#6217=CARTESIAN_POINT('Ctrl Pts',(1.0000000002477,54.2666666669527,-1.7320508079979));
#6218=CARTESIAN_POINT('Ctrl Pts',(2.00000000049539,54.2083333336194,-1.15470053866527));
#6219=CARTESIAN_POINT('Ctrl Pts',(2.00000000049539,54.150000000286,-2.44929359890139E-16));
#6220=CARTESIAN_POINT('Ctrl Pts',(2.00000000049539,54.0916666669527,1.15470053866527));
#6221=CARTESIAN_POINT('Ctrl Pts',(1.0000000002477,54.0333333336194,1.7320508079979));
#6222=CARTESIAN_POINT('Ctrl Pts',(4.24230095595043E-16,53.975000000286,
2.30940107733053));
#6223=CARTESIAN_POINT('Ctrl Pts',(-1.0000000002477,53.9166666669527,1.7320508079979));
#6224=CARTESIAN_POINT('Ctrl Pts',(-2.00000000049539,53.8583333336194,1.15470053866527));
#6225=CARTESIAN_POINT('Ctrl Pts',(-2.00000000049539,53.800000000286,0.));
#6226=CARTESIAN_POINT('Ctrl Pts',(-2.00000000049539,53.7416666669527,-1.15470053866527));
#6227=CARTESIAN_POINT('Ctrl Pts',(-1.0000000002477,53.6833333336194,-1.7320508079979));
#6228=CARTESIAN_POINT('Ctrl Pts',(-1.41410031865014E-16,53.625000000286,
-2.30940107733053));
#6229=CARTESIAN_POINT('Ctrl Pts',(1.0000000002477,53.5666666669527,-1.7320508079979));
#6230=CARTESIAN_POINT('Ctrl Pts',(2.00000000049539,53.5083333336194,-1.15470053866527));
#6231=CARTESIAN_POINT('Ctrl Pts',(2.00000000049539,53.450000000286,-2.44929359890139E-16));
#6232=CARTESIAN_POINT('Ctrl Pts',(2.00000000049539,53.3916666669527,1.15470053866527));
#6233=CARTESIAN_POINT('Ctrl Pts',(1.0000000002477,53.3333333336194,1.7320508079979));
#6234=CARTESIAN_POINT('Ctrl Pts',(4.24230095595043E-16,53.275000000286,
2.30940107733053));
#6235=CARTESIAN_POINT('Ctrl Pts',(-1.0000000002477,53.2166666669527,1.7320508079979));
#6236=CARTESIAN_POINT('Ctrl Pts',(-2.00000000049539,53.1583333336194,1.15470053866527));
#6237=CARTESIAN_POINT('Ctrl Pts',(-2.00000000049539,53.100000000286,0.));
#6238=CARTESIAN_POINT('Ctrl Pts',(-2.00000000049539,53.0416666669527,-1.15470053866527));
#6239=CARTESIAN_POINT('Ctrl Pts',(-1.0000000002477,52.9833333336194,-1.7320508079979));
#6240=CARTESIAN_POINT('Ctrl Pts',(-1.41410031865014E-16,52.925000000286,
-2.30940107733053));
#6241=CARTESIAN_POINT('Ctrl Pts',(1.0000000002477,52.8666666669527,-1.7320508079979));
#6242=CARTESIAN_POINT('Ctrl Pts',(2.00000000049539,52.8083333336193,-1.15470053866527));
#6243=CARTESIAN_POINT('Ctrl Pts',(2.00000000049539,52.750000000286,-2.44929359890139E-16));
#6244=CARTESIAN_POINT('Ctrl Pts',(2.00000000049539,52.6916666669527,1.15470053866527));
#6245=CARTESIAN_POINT('Ctrl Pts',(1.0000000002477,52.6333333336194,1.7320508079979));
#6246=CARTESIAN_POINT('Ctrl Pts',(4.24230095595043E-16,52.575000000286,
2.30940107733053));
#6247=CARTESIAN_POINT('Ctrl Pts',(-1.0000000002477,52.5166666669527,1.7320508079979));
#6248=CARTESIAN_POINT('Ctrl Pts',(-2.00000000049539,52.4583333336194,1.15470053866527));
#6249=CARTESIAN_POINT('Ctrl Pts',(-2.00000000049539,52.400000000286,0.));
#6250=CARTESIAN_POINT('Ctrl Pts',(-2.00000000049539,52.3416666669527,-1.15470053866527));
#6251=CARTESIAN_POINT('Ctrl Pts',(-1.0000000002477,52.2833333336194,-1.7320508079979));
#6252=CARTESIAN_POINT('Ctrl Pts',(-1.41410031865014E-16,52.225000000286,
-2.30940107733053));
#6253=CARTESIAN_POINT('Ctrl Pts',(1.0000000002477,52.1666666669527,-1.7320508079979));
#6254=CARTESIAN_POINT('Ctrl Pts',(2.00000000049539,52.1083333336194,-1.15470053866527));
#6255=CARTESIAN_POINT('Ctrl Pts',(2.00000000049539,52.050000000286,-2.44929359890139E-16));
#6256=CARTESIAN_POINT('Ctrl Pts',(2.00000000049539,51.9916666669527,1.15470053866527));
#6257=CARTESIAN_POINT('Ctrl Pts',(1.0000000002477,51.9333333336194,1.7320508079979));
#6258=CARTESIAN_POINT('Ctrl Pts',(4.24230095595043E-16,51.875000000286,
2.30940107733053));
#6259=CARTESIAN_POINT('Ctrl Pts',(-1.0000000002477,51.8166666669527,1.7320508079979));
#6260=CARTESIAN_POINT('Ctrl Pts',(-2.00000000049539,51.7583333336194,1.15470053866527));
#6261=CARTESIAN_POINT('Ctrl Pts',(-2.00000000049539,51.700000000286,0.));
#6262=CARTESIAN_POINT('Ctrl Pts',(-2.00000000049539,51.6416666669527,-1.15470053866527));
#6263=CARTESIAN_POINT('Ctrl Pts',(-1.0000000002477,51.5833333336194,-1.7320508079979));
#6264=CARTESIAN_POINT('Ctrl Pts',(-1.41410031865014E-16,51.525000000286,
-2.30940107733053));
#6265=CARTESIAN_POINT('Ctrl Pts',(1.0000000002477,51.4666666669527,-1.7320508079979));
#6266=CARTESIAN_POINT('Ctrl Pts',(2.00000000049539,51.4083333336194,-1.15470053866527));
#6267=CARTESIAN_POINT('Ctrl Pts',(2.00000000049539,51.350000000286,-2.44929359890139E-16));
#6268=CARTESIAN_POINT('Ctrl Pts',(2.00000000049539,51.2916666669527,1.15470053866527));
#6269=CARTESIAN_POINT('Ctrl Pts',(1.0000000002477,51.2333333336194,1.7320508079979));
#6270=CARTESIAN_POINT('Ctrl Pts',(4.24230095595043E-16,51.175000000286,
2.30940107733053));
#6271=CARTESIAN_POINT('Ctrl Pts',(-1.0000000002477,51.1166666669527,1.7320508079979));
#6272=CARTESIAN_POINT('Ctrl Pts',(-2.00000000049539,51.0583333336194,1.15470053866527));
#6273=CARTESIAN_POINT('Ctrl Pts',(-2.00000000049539,51.000000000286,0.));
#6274=CARTESIAN_POINT('Ctrl Pts',(-2.00000000049539,50.9416666669527,-1.15470053866527));
#6275=CARTESIAN_POINT('Ctrl Pts',(-1.0000000002477,50.8833333336194,-1.7320508079979));
#6276=CARTESIAN_POINT('Ctrl Pts',(-1.41410031865014E-16,50.825000000286,
-2.30940107733053));
#6277=CARTESIAN_POINT('Ctrl Pts',(1.0000000002477,50.7666666669527,-1.7320508079979));
#6278=CARTESIAN_POINT('Ctrl Pts',(2.00000000049539,50.7083333336194,-1.15470053866527));
#6279=CARTESIAN_POINT('Ctrl Pts',(2.00000000049539,50.650000000286,-2.44929359890139E-16));
#6280=CARTESIAN_POINT('Ctrl Pts',(2.00000000049539,50.5916666669527,1.15470053866527));
#6281=CARTESIAN_POINT('Ctrl Pts',(1.0000000002477,50.5333333336194,1.7320508079979));
#6282=CARTESIAN_POINT('Ctrl Pts',(4.24230095595043E-16,50.475000000286,
2.30940107733053));
#6283=CARTESIAN_POINT('Ctrl Pts',(-1.0000000002477,50.4166666669527,1.7320508079979));
#6284=CARTESIAN_POINT('Ctrl Pts',(-2.00000000049539,50.3583333336194,1.15470053866527));
#6285=CARTESIAN_POINT('Ctrl Pts',(-2.00000000049539,50.300000000286,0.));
#6286=CARTESIAN_POINT('Ctrl Pts',(-2.00000000049539,50.2416666669527,-1.15470053866527));
#6287=CARTESIAN_POINT('Ctrl Pts',(-1.0000000002477,50.1833333336194,-1.7320508079979));
#6288=CARTESIAN_POINT('Ctrl Pts',(-1.41410031865014E-16,50.125000000286,
-2.30940107733053));
#6289=CARTESIAN_POINT('Ctrl Pts',(1.0000000002477,50.0666666669527,-1.7320508079979));
#6290=CARTESIAN_POINT('Ctrl Pts',(2.00000000049539,50.0083333336194,-1.15470053866527));
#6291=CARTESIAN_POINT('Ctrl Pts',(2.00000000049539,49.950000000286,-2.44929359890139E-16));
#6292=CARTESIAN_POINT('Ctrl Pts',(2.00000000049539,49.8916666669527,1.15470053866527));
#6293=CARTESIAN_POINT('Ctrl Pts',(1.0000000002477,49.8333333336194,1.7320508079979));
#6294=CARTESIAN_POINT('Ctrl Pts',(4.24230095595043E-16,49.775000000286,
2.30940107733053));
#6295=CARTESIAN_POINT('Ctrl Pts',(-1.0000000002477,49.7166666669527,1.7320508079979));
#6296=CARTESIAN_POINT('Ctrl Pts',(-2.00000000049539,49.6583333336194,1.15470053866527));
#6297=CARTESIAN_POINT('Ctrl Pts',(-2.00000000049539,49.600000000286,0.));
#6298=CARTESIAN_POINT('Ctrl Pts',(-2.00000000049539,49.5416666669527,-1.15470053866527));
#6299=CARTESIAN_POINT('Ctrl Pts',(-1.0000000002477,49.4833333336194,-1.7320508079979));
#6300=CARTESIAN_POINT('Ctrl Pts',(-1.41410031865014E-16,49.425000000286,
-2.30940107733053));
#6301=CARTESIAN_POINT('Ctrl Pts',(1.0000000002477,49.3666666669527,-1.7320508079979));
#6302=CARTESIAN_POINT('Ctrl Pts',(2.00000000049539,49.3083333336194,-1.15470053866527));
#6303=CARTESIAN_POINT('Ctrl Pts',(2.00000000049539,49.250000000286,-2.44929359890139E-16));
#6304=CARTESIAN_POINT('Ctrl Pts',(2.00000000049539,49.1916666669527,1.15470053866527));
#6305=CARTESIAN_POINT('Ctrl Pts',(1.0000000002477,49.1333333336194,1.7320508079979));
#6306=CARTESIAN_POINT('Ctrl Pts',(4.24230095595043E-16,49.075000000286,
2.30940107733053));
#6307=CARTESIAN_POINT('Ctrl Pts',(-1.0000000002477,49.0166666669527,1.7320508079979));
#6308=CARTESIAN_POINT('Ctrl Pts',(-2.00000000049539,48.9583333336194,1.15470053866527));
#6309=CARTESIAN_POINT('Ctrl Pts',(-2.00000000049539,48.900000000286,0.));
#6310=CARTESIAN_POINT('Ctrl Pts',(-2.00000000049539,48.8416666669527,-1.15470053866527));
#6311=CARTESIAN_POINT('Ctrl Pts',(-1.0000000002477,48.7833333336194,-1.7320508079979));
#6312=CARTESIAN_POINT('Ctrl Pts',(-1.41410031865014E-16,48.725000000286,
-2.30940107733053));
#6313=CARTESIAN_POINT('Ctrl Pts',(1.0000000002477,48.6666666669527,-1.7320508079979));
#6314=CARTESIAN_POINT('Ctrl Pts',(2.00000000049539,48.6083333336194,-1.15470053866527));
#6315=CARTESIAN_POINT('Ctrl Pts',(2.00000000049539,48.550000000286,-2.44929359890139E-16));
#6316=CARTESIAN_POINT('Ctrl Pts',(2.00000000049539,48.4916666669527,1.15470053866527));
#6317=CARTESIAN_POINT('Ctrl Pts',(1.0000000002477,48.4333333336194,1.7320508079979));
#6318=CARTESIAN_POINT('Ctrl Pts',(4.24230095595043E-16,48.375000000286,
2.30940107733053));
#6319=CARTESIAN_POINT('Ctrl Pts',(-1.0000000002477,48.3166666669527,1.7320508079979));
#6320=CARTESIAN_POINT('Ctrl Pts',(-2.00000000049539,48.2583333336193,1.15470053866527));
#6321=CARTESIAN_POINT('Ctrl Pts',(-2.00000000049539,48.200000000286,0.));
#6322=CARTESIAN_POINT('Ctrl Pts',(-2.00000000049539,48.1416666669527,-1.15470053866527));
#6323=CARTESIAN_POINT('Ctrl Pts',(-1.0000000002477,48.0833333336194,-1.7320508079979));
#6324=CARTESIAN_POINT('Ctrl Pts',(-1.41410031865014E-16,48.025000000286,
-2.30940107733053));
#6325=CARTESIAN_POINT('Ctrl Pts',(1.0000000002477,47.9666666669527,-1.7320508079979));
#6326=CARTESIAN_POINT('Ctrl Pts',(2.00000000049539,47.9083333336194,-1.15470053866527));
#6327=CARTESIAN_POINT('Ctrl Pts',(2.00000000049539,47.850000000286,-2.44929359890139E-16));
#6328=CARTESIAN_POINT('Ctrl Pts',(2.00000000049539,47.7916666669527,1.15470053866527));
#6329=CARTESIAN_POINT('Ctrl Pts',(1.0000000002477,47.7333333336194,1.7320508079979));
#6330=CARTESIAN_POINT('Ctrl Pts',(4.24230095595043E-16,47.675000000286,
2.30940107733053));
#6331=CARTESIAN_POINT('Ctrl Pts',(-1.0000000002477,47.6166666669527,1.7320508079979));
#6332=CARTESIAN_POINT('Ctrl Pts',(-2.00000000049539,47.5583333336194,1.15470053866527));
#6333=CARTESIAN_POINT('Ctrl Pts',(-2.00000000049539,47.500000000286,0.));
#6334=CARTESIAN_POINT('Ctrl Pts',(-2.00000000049539,47.4416666669527,-1.15470053866527));
#6335=CARTESIAN_POINT('Ctrl Pts',(-1.0000000002477,47.3833333336194,-1.7320508079979));
#6336=CARTESIAN_POINT('Ctrl Pts',(-1.41410031865014E-16,47.325000000286,
-2.30940107733053));
#6337=CARTESIAN_POINT('Ctrl Pts',(1.0000000002477,47.2666666669527,-1.7320508079979));
#6338=CARTESIAN_POINT('Ctrl Pts',(2.00000000049539,47.2083333336194,-1.15470053866527));
#6339=CARTESIAN_POINT('Ctrl Pts',(2.00000000049539,47.150000000286,-2.44929359890139E-16));
#6340=CARTESIAN_POINT('Ctrl Pts',(2.00000000049539,47.0916666669527,1.15470053866527));
#6341=CARTESIAN_POINT('Ctrl Pts',(1.0000000002477,47.0333333336194,1.7320508079979));
#6342=CARTESIAN_POINT('Ctrl Pts',(4.24230095595043E-16,46.975000000286,
2.30940107733053));
#6343=CARTESIAN_POINT('Ctrl Pts',(-1.0000000002477,46.9166666669527,1.7320508079979));
#6344=CARTESIAN_POINT('Ctrl Pts',(-2.00000000049539,46.8583333336193,1.15470053866527));
#6345=CARTESIAN_POINT('Ctrl Pts',(-2.00000000049539,46.800000000286,0.));
#6346=CARTESIAN_POINT('Ctrl Pts',(-2.00000000049539,46.7416666669527,-1.15470053866527));
#6347=CARTESIAN_POINT('Ctrl Pts',(-1.0000000002477,46.6833333336194,-1.7320508079979));
#6348=CARTESIAN_POINT('Ctrl Pts',(-1.41410031865014E-16,46.625000000286,
-2.30940107733053));
#6349=CARTESIAN_POINT('Ctrl Pts',(1.0000000002477,46.5666666669527,-1.7320508079979));
#6350=CARTESIAN_POINT('Ctrl Pts',(2.00000000049539,46.5083333336194,-1.15470053866527));
#6351=CARTESIAN_POINT('Ctrl Pts',(2.00000000049539,46.450000000286,-2.44929359890139E-16));
#6352=CARTESIAN_POINT('Ctrl Pts',(2.00000000049539,46.3916666669527,1.15470053866527));
#6353=CARTESIAN_POINT('Ctrl Pts',(1.0000000002477,46.3333333336194,1.7320508079979));
#6354=CARTESIAN_POINT('Ctrl Pts',(4.24230095595043E-16,46.275000000286,
2.30940107733053));
#6355=CARTESIAN_POINT('Ctrl Pts',(-1.0000000002477,46.2166666669527,1.7320508079979));
#6356=CARTESIAN_POINT('Ctrl Pts',(-2.00000000049539,46.1583333336193,1.15470053866527));
#6357=CARTESIAN_POINT('Ctrl Pts',(-2.00000000049539,46.100000000286,0.));
#6358=CARTESIAN_POINT('Ctrl Pts',(-2.00000000049539,46.0416666669527,-1.15470053866527));
#6359=CARTESIAN_POINT('Ctrl Pts',(-1.0000000002477,45.9833333336194,-1.7320508079979));
#6360=CARTESIAN_POINT('Ctrl Pts',(-1.41410031865014E-16,45.925000000286,
-2.30940107733053));
#6361=CARTESIAN_POINT('Ctrl Pts',(1.0000000002477,45.8666666669527,-1.7320508079979));
#6362=CARTESIAN_POINT('Ctrl Pts',(2.00000000049539,45.8083333336194,-1.15470053866527));
#6363=CARTESIAN_POINT('Ctrl Pts',(2.00000000049539,45.750000000286,-2.44929359890139E-16));
#6364=CARTESIAN_POINT('Ctrl Pts',(2.00000000049539,45.6916666669527,1.15470053866527));
#6365=CARTESIAN_POINT('Ctrl Pts',(1.0000000002477,45.6333333336194,1.7320508079979));
#6366=CARTESIAN_POINT('Ctrl Pts',(4.24230095595043E-16,45.575000000286,
2.30940107733053));
#6367=CARTESIAN_POINT('Ctrl Pts',(-1.0000000002477,45.5166666669527,1.7320508079979));
#6368=CARTESIAN_POINT('Ctrl Pts',(-2.00000000049539,45.4583333336194,1.15470053866527));
#6369=CARTESIAN_POINT('Ctrl Pts',(-2.00000000049539,45.400000000286,0.));
#6370=CARTESIAN_POINT('Ctrl Pts',(-2.00000000049539,45.3416666669527,-1.15470053866527));
#6371=CARTESIAN_POINT('Ctrl Pts',(-1.0000000002477,45.2833333336194,-1.7320508079979));
#6372=CARTESIAN_POINT('Ctrl Pts',(-1.41410031865014E-16,45.225000000286,
-2.30940107733053));
#6373=CARTESIAN_POINT('Ctrl Pts',(1.0000000002477,45.1666666669527,-1.7320508079979));
#6374=CARTESIAN_POINT('Ctrl Pts',(2.00000000049539,45.1083333336194,-1.15470053866527));
#6375=CARTESIAN_POINT('Ctrl Pts',(2.00000000049539,45.050000000286,-2.44929359890139E-16));
#6376=CARTESIAN_POINT('Ctrl Pts',(2.00000000049539,44.9916666669527,1.15470053866527));
#6377=CARTESIAN_POINT('Ctrl Pts',(1.0000000002477,44.9333333336194,1.7320508079979));
#6378=CARTESIAN_POINT('Ctrl Pts',(4.24230095595043E-16,44.875000000286,
2.30940107733053));
#6379=CARTESIAN_POINT('Ctrl Pts',(-1.0000000002477,44.8166666669527,1.7320508079979));
#6380=CARTESIAN_POINT('Ctrl Pts',(-2.00000000049539,44.7583333336194,1.15470053866527));
#6381=CARTESIAN_POINT('Ctrl Pts',(-2.00000000049539,44.700000000286,0.));
#6382=CARTESIAN_POINT('Ctrl Pts',(-2.00000000049539,44.6416666669527,-1.15470053866527));
#6383=CARTESIAN_POINT('Ctrl Pts',(-1.0000000002477,44.5833333336194,-1.7320508079979));
#6384=CARTESIAN_POINT('Ctrl Pts',(-1.41410031865014E-16,44.525000000286,
-2.30940107733053));
#6385=CARTESIAN_POINT('Ctrl Pts',(1.0000000002477,44.4666666669527,-1.7320508079979));
#6386=CARTESIAN_POINT('Ctrl Pts',(2.00000000049539,44.4083333336194,-1.15470053866527));
#6387=CARTESIAN_POINT('Ctrl Pts',(2.00000000049539,44.350000000286,-2.44929359890139E-16));
#6388=CARTESIAN_POINT('Ctrl Pts',(2.00000000049539,44.2916666669527,1.15470053866527));
#6389=CARTESIAN_POINT('Ctrl Pts',(1.0000000002477,44.2333333336194,1.7320508079979));
#6390=CARTESIAN_POINT('Ctrl Pts',(4.24230095595043E-16,44.175000000286,
2.30940107733053));
#6391=CARTESIAN_POINT('Ctrl Pts',(-1.0000000002477,44.1166666669527,1.7320508079979));
#6392=CARTESIAN_POINT('Ctrl Pts',(-2.00000000049539,44.0583333336194,1.15470053866527));
#6393=CARTESIAN_POINT('Ctrl Pts',(-2.00000000049539,44.000000000286,0.));
#6394=CARTESIAN_POINT('Ctrl Pts',(-2.00000000049539,43.9416666669527,-1.15470053866527));
#6395=CARTESIAN_POINT('Ctrl Pts',(-1.0000000002477,43.8833333336194,-1.7320508079979));
#6396=CARTESIAN_POINT('Ctrl Pts',(-1.41410031865014E-16,43.825000000286,
-2.30940107733053));
#6397=CARTESIAN_POINT('Ctrl Pts',(1.0000000002477,43.7666666669527,-1.7320508079979));
#6398=CARTESIAN_POINT('Ctrl Pts',(2.00000000049539,43.7083333336194,-1.15470053866527));
#6399=CARTESIAN_POINT('Ctrl Pts',(2.00000000049539,43.650000000286,-2.44929359890139E-16));
#6400=CARTESIAN_POINT('Ctrl Pts',(2.00000000049539,43.5916666669527,1.15470053866527));
#6401=CARTESIAN_POINT('Ctrl Pts',(1.0000000002477,43.5333333336194,1.7320508079979));
#6402=CARTESIAN_POINT('Ctrl Pts',(4.24230095595043E-16,43.475000000286,
2.30940107733053));
#6403=CARTESIAN_POINT('Ctrl Pts',(-1.0000000002477,43.4166666669527,1.7320508079979));
#6404=CARTESIAN_POINT('Ctrl Pts',(-2.00000000049539,43.3583333336194,1.15470053866527));
#6405=CARTESIAN_POINT('Ctrl Pts',(-2.00000000049539,43.300000000286,0.));
#6406=CARTESIAN_POINT('Ctrl Pts',(-2.00000000049539,43.2416666669527,-1.15470053866527));
#6407=CARTESIAN_POINT('Ctrl Pts',(-1.0000000002477,43.1833333336194,-1.7320508079979));
#6408=CARTESIAN_POINT('Ctrl Pts',(-1.41410031865014E-16,43.125000000286,
-2.30940107733053));
#6409=CARTESIAN_POINT('Ctrl Pts',(1.0000000002477,43.0666666669527,-1.7320508079979));
#6410=CARTESIAN_POINT('Ctrl Pts',(2.00000000049539,43.0083333336194,-1.15470053866527));
#6411=CARTESIAN_POINT('Ctrl Pts',(2.00000000049539,42.950000000286,-2.44929359890139E-16));
#6412=CARTESIAN_POINT('Ctrl Pts',(2.00000000049539,42.8916666669527,1.15470053866527));
#6413=CARTESIAN_POINT('Ctrl Pts',(1.0000000002477,42.8333333336194,1.7320508079979));
#6414=CARTESIAN_POINT('Ctrl Pts',(4.24230095595043E-16,42.775000000286,
2.30940107733053));
#6415=CARTESIAN_POINT('Ctrl Pts',(-1.0000000002477,42.7166666669527,1.7320508079979));
#6416=CARTESIAN_POINT('Ctrl Pts',(-2.00000000049539,42.6583333336194,1.15470053866527));
#6417=CARTESIAN_POINT('Ctrl Pts',(-2.00000000049539,42.600000000286,0.));
#6418=CARTESIAN_POINT('Ctrl Pts',(-2.00000000049539,42.5416666669527,-1.15470053866527));
#6419=CARTESIAN_POINT('Ctrl Pts',(-1.0000000002477,42.4833333336194,-1.7320508079979));
#6420=CARTESIAN_POINT('Ctrl Pts',(-1.41410031865014E-16,42.425000000286,
-2.30940107733053));
#6421=CARTESIAN_POINT('Ctrl Pts',(1.0000000002477,42.3666666669527,-1.7320508079979));
#6422=CARTESIAN_POINT('Ctrl Pts',(2.00000000049539,42.3083333336194,-1.15470053866527));
#6423=CARTESIAN_POINT('Ctrl Pts',(2.00000000049539,42.250000000286,-2.44929359890139E-16));
#6424=CARTESIAN_POINT('Ctrl Pts',(2.00000000049539,42.1916666669527,1.15470053866527));
#6425=CARTESIAN_POINT('Ctrl Pts',(1.0000000002477,42.1333333336194,1.7320508079979));
#6426=CARTESIAN_POINT('Ctrl Pts',(4.24230095595043E-16,42.075000000286,
2.30940107733053));
#6427=CARTESIAN_POINT('Ctrl Pts',(-1.0000000002477,42.0166666669527,1.7320508079979));
#6428=CARTESIAN_POINT('Ctrl Pts',(-2.00000000049539,41.9583333336194,1.15470053866527));
#6429=CARTESIAN_POINT('Ctrl Pts',(-2.00000000049539,41.900000000286,0.));
#6430=CARTESIAN_POINT('Ctrl Pts',(-2.00000000049539,41.8416666669527,-1.15470053866527));
#6431=CARTESIAN_POINT('Ctrl Pts',(-1.0000000002477,41.7833333336194,-1.7320508079979));
#6432=CARTESIAN_POINT('Ctrl Pts',(-1.41410031865014E-16,41.725000000286,
-2.30940107733053));
#6433=CARTESIAN_POINT('Ctrl Pts',(1.0000000002477,41.6666666669527,-1.7320508079979));
#6434=CARTESIAN_POINT('Ctrl Pts',(2.00000000049539,41.6083333336194,-1.15470053866527));
#6435=CARTESIAN_POINT('Ctrl Pts',(2.00000000049539,41.550000000286,-2.44929359890139E-16));
#6436=CARTESIAN_POINT('Ctrl Pts',(2.00000000049539,41.4916666669527,1.15470053866527));
#6437=CARTESIAN_POINT('Ctrl Pts',(1.0000000002477,41.4333333336194,1.7320508079979));
#6438=CARTESIAN_POINT('Ctrl Pts',(4.24230095595043E-16,41.375000000286,
2.30940107733053));
#6439=CARTESIAN_POINT('Ctrl Pts',(-1.0000000002477,41.3166666669527,1.7320508079979));
#6440=CARTESIAN_POINT('Ctrl Pts',(-2.00000000049539,41.2583333336194,1.15470053866527));
#6441=CARTESIAN_POINT('Ctrl Pts',(-2.00000000049539,41.200000000286,0.));
#6442=CARTESIAN_POINT('Ctrl Pts',(-2.00000000049539,41.1416666669527,-1.15470053866527));
#6443=CARTESIAN_POINT('Ctrl Pts',(-1.0000000002477,41.0833333336194,-1.7320508079979));
#6444=CARTESIAN_POINT('Ctrl Pts',(-1.41410031865014E-16,41.025000000286,
-2.30940107733053));
#6445=CARTESIAN_POINT('Ctrl Pts',(1.0000000002477,40.9666666669527,-1.7320508079979));
#6446=CARTESIAN_POINT('Ctrl Pts',(2.00000000049539,40.9083333336194,-1.15470053866527));
#6447=CARTESIAN_POINT('Ctrl Pts',(2.00000000049539,40.850000000286,-2.44929359890139E-16));
#6448=CARTESIAN_POINT('Ctrl Pts',(2.00000000049539,40.7916666669527,1.15470053866527));
#6449=CARTESIAN_POINT('Ctrl Pts',(1.0000000002477,40.7333333336194,1.7320508079979));
#6450=CARTESIAN_POINT('Ctrl Pts',(4.24230095595043E-16,40.675000000286,
2.30940107733053));
#6451=CARTESIAN_POINT('Ctrl Pts',(-1.0000000002477,40.6166666669527,1.7320508079979));
#6452=CARTESIAN_POINT('Ctrl Pts',(-2.00000000049539,40.5583333336194,1.15470053866527));
#6453=CARTESIAN_POINT('Ctrl Pts',(-2.00000000049539,40.500000000286,0.));
#6454=CARTESIAN_POINT('Ctrl Pts',(-2.00000000049539,40.4416666669527,-1.15470053866527));
#6455=CARTESIAN_POINT('Ctrl Pts',(-1.0000000002477,40.3833333336193,-1.7320508079979));
#6456=CARTESIAN_POINT('Ctrl Pts',(-1.41410031865014E-16,40.325000000286,
-2.30940107733053));
#6457=CARTESIAN_POINT('Ctrl Pts',(1.0000000002477,40.2666666669527,-1.7320508079979));
#6458=CARTESIAN_POINT('Ctrl Pts',(2.00000000049539,40.2083333336194,-1.15470053866527));
#6459=CARTESIAN_POINT('Ctrl Pts',(2.00000000049539,40.150000000286,-2.44929359890139E-16));
#6460=CARTESIAN_POINT('Ctrl Pts',(2.00000000049539,40.0916666669527,1.15470053866527));
#6461=CARTESIAN_POINT('Ctrl Pts',(1.0000000002477,40.0333333336194,1.7320508079979));
#6462=CARTESIAN_POINT('Ctrl Pts',(4.24230095595043E-16,39.975000000286,
2.30940107733053));
#6463=CARTESIAN_POINT('Ctrl Pts',(-1.0000000002477,39.9166666669527,1.7320508079979));
#6464=CARTESIAN_POINT('Ctrl Pts',(-2.00000000049539,39.8583333336194,1.15470053866527));
#6465=CARTESIAN_POINT('Ctrl Pts',(-2.00000000049539,39.800000000286,0.));
#6466=CARTESIAN_POINT('Ctrl Pts',(-2.00000000049539,39.7416666669527,-1.15470053866527));
#6467=CARTESIAN_POINT('Ctrl Pts',(-1.0000000002477,39.6833333336194,-1.7320508079979));
#6468=CARTESIAN_POINT('Ctrl Pts',(-1.41410031865014E-16,39.625000000286,
-2.30940107733053));
#6469=CARTESIAN_POINT('Ctrl Pts',(1.0000000002477,39.5666666669527,-1.7320508079979));
#6470=CARTESIAN_POINT('Ctrl Pts',(2.00000000049539,39.5083333336194,-1.15470053866527));
#6471=CARTESIAN_POINT('Ctrl Pts',(2.00000000049539,39.450000000286,-2.44929359890139E-16));
#6472=CARTESIAN_POINT('Ctrl Pts',(2.00000000049539,39.3916666669527,1.15470053866527));
#6473=CARTESIAN_POINT('Ctrl Pts',(1.0000000002477,39.3333333336194,1.7320508079979));
#6474=CARTESIAN_POINT('Ctrl Pts',(4.24230095595043E-16,39.275000000286,
2.30940107733053));
#6475=CARTESIAN_POINT('Ctrl Pts',(-1.0000000002477,39.2166666669527,1.7320508079979));
#6476=CARTESIAN_POINT('Ctrl Pts',(-2.00000000049539,39.1583333336194,1.15470053866527));
#6477=CARTESIAN_POINT('Ctrl Pts',(-2.00000000049539,39.100000000286,0.));
#6478=CARTESIAN_POINT('Ctrl Pts',(-2.00000000049539,39.0416666669527,-1.15470053866527));
#6479=CARTESIAN_POINT('Ctrl Pts',(-1.0000000002477,38.9833333336194,-1.7320508079979));
#6480=CARTESIAN_POINT('Ctrl Pts',(-1.41410031865014E-16,38.925000000286,
-2.30940107733053));
#6481=CARTESIAN_POINT('Ctrl Pts',(1.0000000002477,38.8666666669527,-1.7320508079979));
#6482=CARTESIAN_POINT('Ctrl Pts',(2.00000000049539,38.8083333336194,-1.15470053866527));
#6483=CARTESIAN_POINT('Ctrl Pts',(2.00000000049539,38.750000000286,-2.44929359890139E-16));
#6484=CARTESIAN_POINT('Ctrl Pts',(2.00000000049539,38.6916666669527,1.15470053866527));
#6485=CARTESIAN_POINT('Ctrl Pts',(1.0000000002477,38.6333333336194,1.7320508079979));
#6486=CARTESIAN_POINT('Ctrl Pts',(4.24230095595043E-16,38.575000000286,
2.30940107733053));
#6487=CARTESIAN_POINT('Ctrl Pts',(-1.0000000002477,38.5166666669527,1.7320508079979));
#6488=CARTESIAN_POINT('Ctrl Pts',(-2.00000000049539,38.4583333336194,1.15470053866527));
#6489=CARTESIAN_POINT('Ctrl Pts',(-2.00000000049539,38.400000000286,0.));
#6490=CARTESIAN_POINT('Ctrl Pts',(-2.00000000049539,38.3416666669527,-1.15470053866527));
#6491=CARTESIAN_POINT('Ctrl Pts',(-1.0000000002477,38.2833333336194,-1.7320508079979));
#6492=CARTESIAN_POINT('Ctrl Pts',(-1.41410031865014E-16,38.225000000286,
-2.30940107733053));
#6493=CARTESIAN_POINT('Ctrl Pts',(1.0000000002477,38.1666666669527,-1.7320508079979));
#6494=CARTESIAN_POINT('Ctrl Pts',(2.00000000049539,38.1083333336194,-1.15470053866527));
#6495=CARTESIAN_POINT('Ctrl Pts',(2.00000000049539,38.050000000286,-2.44929359890139E-16));
#6496=CARTESIAN_POINT('Ctrl Pts',(2.00000000049539,37.9916666669527,1.15470053866527));
#6497=CARTESIAN_POINT('Ctrl Pts',(1.0000000002477,37.9333333336194,1.7320508079979));
#6498=CARTESIAN_POINT('Ctrl Pts',(4.24230095595043E-16,37.875000000286,
2.30940107733053));
#6499=CARTESIAN_POINT('Ctrl Pts',(-1.0000000002477,37.8166666669527,1.7320508079979));
#6500=CARTESIAN_POINT('Ctrl Pts',(-2.00000000049539,37.7583333336194,1.15470053866527));
#6501=CARTESIAN_POINT('Ctrl Pts',(-2.00000000049539,37.700000000286,0.));
#6502=CARTESIAN_POINT('Ctrl Pts',(-2.00000000049539,37.6416666669527,-1.15470053866527));
#6503=CARTESIAN_POINT('Ctrl Pts',(-1.0000000002477,37.5833333336194,-1.7320508079979));
#6504=CARTESIAN_POINT('Ctrl Pts',(-1.41410031865014E-16,37.525000000286,
-2.30940107733053));
#6505=CARTESIAN_POINT('Ctrl Pts',(1.0000000002477,37.4666666669527,-1.7320508079979));
#6506=CARTESIAN_POINT('Ctrl Pts',(2.00000000049539,37.4083333336194,-1.15470053866527));
#6507=CARTESIAN_POINT('Ctrl Pts',(2.00000000049539,37.350000000286,-2.44929359890139E-16));
#6508=CARTESIAN_POINT('Ctrl Pts',(2.00000000049539,37.2916666669527,1.15470053866527));
#6509=CARTESIAN_POINT('Ctrl Pts',(1.0000000002477,37.2333333336194,1.7320508079979));
#6510=CARTESIAN_POINT('Ctrl Pts',(4.24230095595043E-16,37.175000000286,
2.30940107733053));
#6511=CARTESIAN_POINT('Ctrl Pts',(-1.0000000002477,37.1166666669527,1.7320508079979));
#6512=CARTESIAN_POINT('Ctrl Pts',(-2.00000000049539,37.0583333336194,1.15470053866527));
#6513=CARTESIAN_POINT('Ctrl Pts',(-2.00000000049539,37.000000000286,0.));
#6514=CARTESIAN_POINT('Ctrl Pts',(-2.00000000049539,36.9416666669527,-1.15470053866527));
#6515=CARTESIAN_POINT('Ctrl Pts',(-1.0000000002477,36.8833333336194,-1.7320508079979));
#6516=CARTESIAN_POINT('Ctrl Pts',(-1.41410031865014E-16,36.825000000286,
-2.30940107733053));
#6517=CARTESIAN_POINT('Ctrl Pts',(1.0000000002477,36.7666666669527,-1.7320508079979));
#6518=CARTESIAN_POINT('Ctrl Pts',(2.00000000049539,36.7083333336194,-1.15470053866527));
#6519=CARTESIAN_POINT('Ctrl Pts',(2.00000000049539,36.650000000286,-2.44929359890139E-16));
#6520=CARTESIAN_POINT('Ctrl Pts',(2.00000000049539,36.5916666669527,1.15470053866527));
#6521=CARTESIAN_POINT('Ctrl Pts',(1.0000000002477,36.5333333336194,1.7320508079979));
#6522=CARTESIAN_POINT('Ctrl Pts',(4.24230095595043E-16,36.475000000286,
2.30940107733053));
#6523=CARTESIAN_POINT('Ctrl Pts',(-1.0000000002477,36.4166666669527,1.7320508079979));
#6524=CARTESIAN_POINT('Ctrl Pts',(-2.00000000049539,36.3583333336194,1.15470053866527));
#6525=CARTESIAN_POINT('Ctrl Pts',(-2.00000000049539,36.300000000286,0.));
#6526=CARTESIAN_POINT('Ctrl Pts',(-2.00000000049539,36.2416666669527,-1.15470053866527));
#6527=CARTESIAN_POINT('Ctrl Pts',(-1.0000000002477,36.1833333336194,-1.7320508079979));
#6528=CARTESIAN_POINT('Ctrl Pts',(-1.41410031865014E-16,36.125000000286,
-2.30940107733053));
#6529=CARTESIAN_POINT('Ctrl Pts',(1.0000000002477,36.0666666669527,-1.7320508079979));
#6530=CARTESIAN_POINT('Ctrl Pts',(2.00000000049539,36.0083333336194,-1.15470053866527));
#6531=CARTESIAN_POINT('Ctrl Pts',(2.00000000049539,35.950000000286,-2.44929359890139E-16));
#6532=CARTESIAN_POINT('Ctrl Pts',(2.00000000049539,35.8916666669527,1.15470053866527));
#6533=CARTESIAN_POINT('Ctrl Pts',(1.0000000002477,35.8333333336194,1.7320508079979));
#6534=CARTESIAN_POINT('Ctrl Pts',(4.24230095595043E-16,35.775000000286,
2.30940107733053));
#6535=CARTESIAN_POINT('Ctrl Pts',(-1.0000000002477,35.7166666669527,1.7320508079979));
#6536=CARTESIAN_POINT('Ctrl Pts',(-2.00000000049539,35.6583333336194,1.15470053866527));
#6537=CARTESIAN_POINT('Ctrl Pts',(-2.00000000049539,35.600000000286,0.));
#6538=CARTESIAN_POINT('Ctrl Pts',(-2.00000000049539,35.5416666669527,-1.15470053866527));
#6539=CARTESIAN_POINT('Ctrl Pts',(-1.0000000002477,35.4833333336194,-1.7320508079979));
#6540=CARTESIAN_POINT('Ctrl Pts',(-1.41410031865014E-16,35.425000000286,
-2.30940107733053));
#6541=CARTESIAN_POINT('Ctrl Pts',(1.0000000002477,35.3666666669527,-1.7320508079979));
#6542=CARTESIAN_POINT('Ctrl Pts',(2.00000000049539,35.3083333336194,-1.15470053866527));
#6543=CARTESIAN_POINT('Ctrl Pts',(2.00000000049539,35.250000000286,-2.44929359890139E-16));
#6544=CARTESIAN_POINT('Ctrl Pts',(2.00000000049539,35.1916666669527,1.15470053866527));
#6545=CARTESIAN_POINT('Ctrl Pts',(1.0000000002477,35.1333333336194,1.7320508079979));
#6546=CARTESIAN_POINT('Ctrl Pts',(4.24230095595043E-16,35.075000000286,
2.30940107733053));
#6547=CARTESIAN_POINT('Ctrl Pts',(-1.0000000002477,35.0166666669527,1.7320508079979));
#6548=CARTESIAN_POINT('Ctrl Pts',(-2.00000000049539,34.9583333336194,1.15470053866527));
#6549=CARTESIAN_POINT('Ctrl Pts',(-2.00000000049539,34.900000000286,0.));
#6550=CARTESIAN_POINT('Ctrl Pts',(-2.00000000049539,34.8416666669527,-1.15470053866527));
#6551=CARTESIAN_POINT('Ctrl Pts',(-1.0000000002477,34.7833333336194,-1.7320508079979));
#6552=CARTESIAN_POINT('Ctrl Pts',(-1.41410031865014E-16,34.725000000286,
-2.30940107733053));
#6553=CARTESIAN_POINT('Ctrl Pts',(1.0000000002477,34.6666666669527,-1.7320508079979));
#6554=CARTESIAN_POINT('Ctrl Pts',(2.00000000049539,34.6083333336194,-1.15470053866527));
#6555=CARTESIAN_POINT('Ctrl Pts',(2.00000000049539,34.550000000286,-2.44929359890139E-16));
#6556=CARTESIAN_POINT('Ctrl Pts',(2.00000000049539,34.4916666669527,1.15470053866527));
#6557=CARTESIAN_POINT('Ctrl Pts',(1.0000000002477,34.4333333336194,1.7320508079979));
#6558=CARTESIAN_POINT('Ctrl Pts',(4.24230095595043E-16,34.375000000286,
2.30940107733053));
#6559=CARTESIAN_POINT('Ctrl Pts',(-1.0000000002477,34.3166666669527,1.7320508079979));
#6560=CARTESIAN_POINT('Ctrl Pts',(-2.00000000049539,34.2583333336194,1.15470053866527));
#6561=CARTESIAN_POINT('Ctrl Pts',(-2.00000000049539,34.200000000286,0.));
#6562=CARTESIAN_POINT('Ctrl Pts',(-2.00000000049539,34.1416666669527,-1.15470053866527));
#6563=CARTESIAN_POINT('Ctrl Pts',(-1.0000000002477,34.0833333336194,-1.7320508079979));
#6564=CARTESIAN_POINT('Ctrl Pts',(-1.41410031865014E-16,34.025000000286,
-2.30940107733053));
#6565=CARTESIAN_POINT('Ctrl Pts',(1.0000000002477,33.9666666669527,-1.7320508079979));
#6566=CARTESIAN_POINT('Ctrl Pts',(2.00000000049539,33.9083333336194,-1.15470053866527));
#6567=CARTESIAN_POINT('Ctrl Pts',(2.00000000049539,33.850000000286,-2.44929359890139E-16));
#6568=CARTESIAN_POINT('Ctrl Pts',(2.00000000049539,33.7916666669527,1.15470053866527));
#6569=CARTESIAN_POINT('Ctrl Pts',(1.0000000002477,33.7333333336194,1.7320508079979));
#6570=CARTESIAN_POINT('Ctrl Pts',(4.24230095595043E-16,33.675000000286,
2.30940107733053));
#6571=CARTESIAN_POINT('Ctrl Pts',(-1.0000000002477,33.6166666669527,1.7320508079979));
#6572=CARTESIAN_POINT('Ctrl Pts',(-2.00000000049539,33.5583333336194,1.15470053866527));
#6573=CARTESIAN_POINT('Ctrl Pts',(-2.00000000049539,33.500000000286,0.));
#6574=CARTESIAN_POINT('Ctrl Pts',(-2.00000000049539,33.4416666669527,-1.15470053866527));
#6575=CARTESIAN_POINT('Ctrl Pts',(-1.0000000002477,33.3833333336194,-1.7320508079979));
#6576=CARTESIAN_POINT('Ctrl Pts',(-1.41410031865014E-16,33.325000000286,
-2.30940107733053));
#6577=CARTESIAN_POINT('Ctrl Pts',(1.0000000002477,33.2666666669527,-1.7320508079979));
#6578=CARTESIAN_POINT('Ctrl Pts',(2.00000000049539,33.2083333336194,-1.15470053866527));
#6579=CARTESIAN_POINT('Ctrl Pts',(2.00000000049539,33.150000000286,-2.44929359890139E-16));
#6580=CARTESIAN_POINT('Ctrl Pts',(2.00000000049539,33.0916666669527,1.15470053866527));
#6581=CARTESIAN_POINT('Ctrl Pts',(1.0000000002477,33.0333333336194,1.7320508079979));
#6582=CARTESIAN_POINT('Ctrl Pts',(4.24230095595043E-16,32.975000000286,
2.30940107733053));
#6583=CARTESIAN_POINT('Ctrl Pts',(-1.0000000002477,32.9166666669527,1.7320508079979));
#6584=CARTESIAN_POINT('Ctrl Pts',(-2.00000000049539,32.8583333336194,1.15470053866527));
#6585=CARTESIAN_POINT('Ctrl Pts',(-2.00000000049539,32.800000000286,0.));
#6586=CARTESIAN_POINT('Ctrl Pts',(-2.00000000049539,32.7416666669527,-1.15470053866527));
#6587=CARTESIAN_POINT('Ctrl Pts',(-1.0000000002477,32.6833333336194,-1.7320508079979));
#6588=CARTESIAN_POINT('Ctrl Pts',(-1.41410031865014E-16,32.625000000286,
-2.30940107733053));
#6589=CARTESIAN_POINT('Ctrl Pts',(1.0000000002477,32.5666666669527,-1.7320508079979));
#6590=CARTESIAN_POINT('Ctrl Pts',(2.00000000049539,32.5083333336194,-1.15470053866527));
#6591=CARTESIAN_POINT('Ctrl Pts',(2.00000000049539,32.450000000286,-2.44929359890139E-16));
#6592=CARTESIAN_POINT('Ctrl Pts',(2.00000000049539,32.3916666669527,1.15470053866527));
#6593=CARTESIAN_POINT('Ctrl Pts',(1.0000000002477,32.3333333336194,1.7320508079979));
#6594=CARTESIAN_POINT('Ctrl Pts',(4.24230095595043E-16,32.275000000286,
2.30940107733053));
#6595=CARTESIAN_POINT('Ctrl Pts',(-1.0000000002477,32.2166666669527,1.7320508079979));
#6596=CARTESIAN_POINT('Ctrl Pts',(-2.00000000049539,32.1583333336194,1.15470053866527));
#6597=CARTESIAN_POINT('Ctrl Pts',(-2.00000000049539,32.100000000286,0.));
#6598=CARTESIAN_POINT('Ctrl Pts',(-2.00000000049539,32.0416666669527,-1.15470053866527));
#6599=CARTESIAN_POINT('Ctrl Pts',(-1.0000000002477,31.9833333336194,-1.7320508079979));
#6600=CARTESIAN_POINT('Ctrl Pts',(-1.41410031865014E-16,31.925000000286,
-2.30940107733053));
#6601=CARTESIAN_POINT('Ctrl Pts',(1.0000000002477,31.8666666669527,-1.7320508079979));
#6602=CARTESIAN_POINT('Ctrl Pts',(2.00000000049539,31.8083333336194,-1.15470053866527));
#6603=CARTESIAN_POINT('Ctrl Pts',(2.00000000049539,31.750000000286,-2.44929359890139E-16));
#6604=CARTESIAN_POINT('Ctrl Pts',(2.00000000049539,31.6916666669527,1.15470053866527));
#6605=CARTESIAN_POINT('Ctrl Pts',(1.0000000002477,31.6333333336194,1.7320508079979));
#6606=CARTESIAN_POINT('Ctrl Pts',(4.24230095595043E-16,31.575000000286,
2.30940107733053));
#6607=CARTESIAN_POINT('Ctrl Pts',(-1.0000000002477,31.5166666669527,1.7320508079979));
#6608=CARTESIAN_POINT('Ctrl Pts',(-2.00000000049539,31.4583333336194,1.15470053866527));
#6609=CARTESIAN_POINT('Ctrl Pts',(-2.00000000049539,31.400000000286,0.));
#6610=CARTESIAN_POINT('Ctrl Pts',(-2.00000000049539,31.3416666669527,-1.15470053866527));
#6611=CARTESIAN_POINT('Ctrl Pts',(-1.0000000002477,31.2833333336194,-1.7320508079979));
#6612=CARTESIAN_POINT('Ctrl Pts',(-1.41410031865014E-16,31.225000000286,
-2.30940107733053));
#6613=CARTESIAN_POINT('Ctrl Pts',(1.0000000002477,31.1666666669527,-1.7320508079979));
#6614=CARTESIAN_POINT('Ctrl Pts',(2.00000000049539,31.1083333336194,-1.15470053866527));
#6615=CARTESIAN_POINT('Ctrl Pts',(2.00000000049539,31.050000000286,-2.44929359890139E-16));
#6616=CARTESIAN_POINT('Ctrl Pts',(2.00000000049539,30.9916666669527,1.15470053866527));
#6617=CARTESIAN_POINT('Ctrl Pts',(1.0000000002477,30.9333333336194,1.7320508079979));
#6618=CARTESIAN_POINT('Ctrl Pts',(4.24230095595043E-16,30.875000000286,
2.30940107733053));
#6619=CARTESIAN_POINT('Ctrl Pts',(-1.0000000002477,30.8166666669527,1.7320508079979));
#6620=CARTESIAN_POINT('Ctrl Pts',(-2.00000000049539,30.7583333336194,1.15470053866527));
#6621=CARTESIAN_POINT('Ctrl Pts',(-2.00000000049539,30.700000000286,0.));
#6622=CARTESIAN_POINT('Ctrl Pts',(-2.00000000049539,30.6416666669527,-1.15470053866527));
#6623=CARTESIAN_POINT('Ctrl Pts',(-1.0000000002477,30.5833333336194,-1.7320508079979));
#6624=CARTESIAN_POINT('Ctrl Pts',(-1.41410031865014E-16,30.525000000286,
-2.30940107733053));
#6625=CARTESIAN_POINT('Ctrl Pts',(1.0000000002477,30.4666666669527,-1.7320508079979));
#6626=CARTESIAN_POINT('Ctrl Pts',(2.00000000049539,30.4083333336193,-1.15470053866527));
#6627=CARTESIAN_POINT('Ctrl Pts',(2.00000000049539,30.350000000286,-2.44929359890139E-16));
#6628=CARTESIAN_POINT('Ctrl Pts',(2.00000000049539,30.2916666669527,1.15470053866527));
#6629=CARTESIAN_POINT('Ctrl Pts',(1.0000000002477,30.2333333336194,1.7320508079979));
#6630=CARTESIAN_POINT('Ctrl Pts',(4.24230095595043E-16,30.175000000286,
2.30940107733053));
#6631=CARTESIAN_POINT('Ctrl Pts',(-1.0000000002477,30.1166666669527,1.7320508079979));
#6632=CARTESIAN_POINT('Ctrl Pts',(-2.00000000049539,30.0583333336194,1.15470053866527));
#6633=CARTESIAN_POINT('Ctrl Pts',(-2.00000000049539,30.000000000286,0.));
#6634=CARTESIAN_POINT('Ctrl Pts',(-2.00000000049539,29.9416666669527,-1.15470053866527));
#6635=CARTESIAN_POINT('Ctrl Pts',(-1.0000000002477,29.8833333336194,-1.7320508079979));
#6636=CARTESIAN_POINT('Ctrl Pts',(-1.41410031865014E-16,29.825000000286,
-2.30940107733053));
#6637=CARTESIAN_POINT('Ctrl Pts',(1.0000000002477,29.7666666669527,-1.7320508079979));
#6638=CARTESIAN_POINT('Ctrl Pts',(2.00000000049539,29.7083333336194,-1.15470053866527));
#6639=CARTESIAN_POINT('Ctrl Pts',(2.00000000049539,29.650000000286,-2.44929359890139E-16));
#6640=CARTESIAN_POINT('Ctrl Pts',(2.00000000049539,29.5916666669527,1.15470053866527));
#6641=CARTESIAN_POINT('Ctrl Pts',(1.0000000002477,29.5333333336194,1.7320508079979));
#6642=CARTESIAN_POINT('Ctrl Pts',(4.24230095595043E-16,29.475000000286,
2.30940107733053));
#6643=CARTESIAN_POINT('Ctrl Pts',(-1.0000000002477,29.4166666669527,1.7320508079979));
#6644=CARTESIAN_POINT('Ctrl Pts',(-2.00000000049539,29.3583333336194,1.15470053866527));
#6645=CARTESIAN_POINT('Ctrl Pts',(-2.00000000049539,29.300000000286,0.));
#6646=CARTESIAN_POINT('Ctrl Pts',(-2.00000000049539,29.2416666669527,-1.15470053866527));
#6647=CARTESIAN_POINT('Ctrl Pts',(-1.0000000002477,29.1833333336194,-1.7320508079979));
#6648=CARTESIAN_POINT('Ctrl Pts',(-1.41410031865014E-16,29.125000000286,
-2.30940107733053));
#6649=CARTESIAN_POINT('Ctrl Pts',(1.0000000002477,29.0666666669527,-1.7320508079979));
#6650=CARTESIAN_POINT('Ctrl Pts',(2.00000000049539,29.0083333336194,-1.15470053866527));
#6651=CARTESIAN_POINT('Ctrl Pts',(2.00000000049539,28.950000000286,-2.44929359890139E-16));
#6652=CARTESIAN_POINT('Ctrl Pts',(2.00000000049539,28.8916666669527,1.15470053866527));
#6653=CARTESIAN_POINT('Ctrl Pts',(1.0000000002477,28.8333333336194,1.7320508079979));
#6654=CARTESIAN_POINT('Ctrl Pts',(4.24230095595043E-16,28.775000000286,
2.30940107733053));
#6655=CARTESIAN_POINT('Ctrl Pts',(-1.0000000002477,28.7166666669527,1.7320508079979));
#6656=CARTESIAN_POINT('Ctrl Pts',(-2.00000000049539,28.6583333336194,1.15470053866527));
#6657=CARTESIAN_POINT('Ctrl Pts',(-2.00000000049539,28.600000000286,0.));
#6658=CARTESIAN_POINT('Ctrl Pts',(-2.00000000049539,28.5416666669527,-1.15470053866527));
#6659=CARTESIAN_POINT('Ctrl Pts',(-1.0000000002477,28.4833333336194,-1.7320508079979));
#6660=CARTESIAN_POINT('Ctrl Pts',(-1.41410031865014E-16,28.425000000286,
-2.30940107733053));
#6661=CARTESIAN_POINT('Ctrl Pts',(1.0000000002477,28.3666666669527,-1.7320508079979));
#6662=CARTESIAN_POINT('Ctrl Pts',(2.00000000049539,28.3083333336194,-1.15470053866527));
#6663=CARTESIAN_POINT('Ctrl Pts',(2.00000000049539,28.250000000286,-2.44929359890139E-16));
#6664=CARTESIAN_POINT('Ctrl Pts',(2.00000000049539,28.1916666669527,1.15470053866527));
#6665=CARTESIAN_POINT('Ctrl Pts',(1.0000000002477,28.1333333336194,1.7320508079979));
#6666=CARTESIAN_POINT('Ctrl Pts',(4.24230095595043E-16,28.075000000286,
2.30940107733053));
#6667=CARTESIAN_POINT('Ctrl Pts',(-1.0000000002477,28.0166666669527,1.7320508079979));
#6668=CARTESIAN_POINT('Ctrl Pts',(-2.00000000049539,27.9583333336194,1.15470053866527));
#6669=CARTESIAN_POINT('Ctrl Pts',(-2.00000000049539,27.900000000286,0.));
#6670=CARTESIAN_POINT('Ctrl Pts',(-2.00000000049539,27.8416666669527,-1.15470053866527));
#6671=CARTESIAN_POINT('Ctrl Pts',(-1.0000000002477,27.7833333336194,-1.7320508079979));
#6672=CARTESIAN_POINT('Ctrl Pts',(-1.41410031865014E-16,27.725000000286,
-2.30940107733053));
#6673=CARTESIAN_POINT('Ctrl Pts',(1.0000000002477,27.6666666669527,-1.7320508079979));
#6674=CARTESIAN_POINT('Ctrl Pts',(2.00000000049539,27.6083333336194,-1.15470053866527));
#6675=CARTESIAN_POINT('Ctrl Pts',(2.00000000049539,27.550000000286,-2.44929359890139E-16));
#6676=CARTESIAN_POINT('Ctrl Pts',(2.00000000049539,27.4916666669527,1.15470053866527));
#6677=CARTESIAN_POINT('Ctrl Pts',(1.0000000002477,27.4333333336194,1.7320508079979));
#6678=CARTESIAN_POINT('Ctrl Pts',(4.24230095595043E-16,27.375000000286,
2.30940107733053));
#6679=CARTESIAN_POINT('Ctrl Pts',(-1.0000000002477,27.3166666669527,1.7320508079979));
#6680=CARTESIAN_POINT('Ctrl Pts',(-2.00000000049539,27.2583333336194,1.15470053866527));
#6681=CARTESIAN_POINT('Ctrl Pts',(-2.00000000049539,27.200000000286,0.));
#6682=CARTESIAN_POINT('Ctrl Pts',(-2.00000000049539,27.1416666669527,-1.15470053866527));
#6683=CARTESIAN_POINT('Ctrl Pts',(-1.0000000002477,27.0833333336194,-1.7320508079979));
#6684=CARTESIAN_POINT('Ctrl Pts',(-1.41410031865014E-16,27.025000000286,
-2.30940107733053));
#6685=CARTESIAN_POINT('Ctrl Pts',(1.0000000002477,26.9666666669527,-1.7320508079979));
#6686=CARTESIAN_POINT('Ctrl Pts',(2.00000000049539,26.9083333336194,-1.15470053866527));
#6687=CARTESIAN_POINT('Ctrl Pts',(2.00000000049539,26.850000000286,-2.44929359890139E-16));
#6688=CARTESIAN_POINT('Ctrl Pts',(2.00000000049539,26.7916666669527,1.15470053866527));
#6689=CARTESIAN_POINT('Ctrl Pts',(1.0000000002477,26.7333333336194,1.7320508079979));
#6690=CARTESIAN_POINT('Ctrl Pts',(4.24230095595043E-16,26.675000000286,
2.30940107733053));
#6691=CARTESIAN_POINT('Ctrl Pts',(-1.0000000002477,26.6166666669527,1.7320508079979));
#6692=CARTESIAN_POINT('Ctrl Pts',(-2.00000000049539,26.5583333336194,1.15470053866527));
#6693=CARTESIAN_POINT('Ctrl Pts',(-2.00000000049539,26.500000000286,0.));
#6694=CARTESIAN_POINT('Ctrl Pts',(-2.00000000049539,26.4416666669527,-1.15470053866527));
#6695=CARTESIAN_POINT('Ctrl Pts',(-1.0000000002477,26.3833333336194,-1.7320508079979));
#6696=CARTESIAN_POINT('Ctrl Pts',(-1.41410031865014E-16,26.325000000286,
-2.30940107733053));
#6697=CARTESIAN_POINT('Ctrl Pts',(1.0000000002477,26.2666666669527,-1.7320508079979));
#6698=CARTESIAN_POINT('Ctrl Pts',(2.00000000049539,26.2083333336194,-1.15470053866527));
#6699=CARTESIAN_POINT('Ctrl Pts',(2.00000000049539,26.150000000286,-2.44929359890139E-16));
#6700=CARTESIAN_POINT('Ctrl Pts',(2.00000000049539,26.0916666669527,1.15470053866527));
#6701=CARTESIAN_POINT('Ctrl Pts',(1.0000000002477,26.0333333336194,1.7320508079979));
#6702=CARTESIAN_POINT('Ctrl Pts',(4.24230095595043E-16,25.975000000286,
2.30940107733053));
#6703=CARTESIAN_POINT('Ctrl Pts',(-1.0000000002477,25.9166666669527,1.7320508079979));
#6704=CARTESIAN_POINT('Ctrl Pts',(-2.00000000049539,25.8583333336194,1.15470053866527));
#6705=CARTESIAN_POINT('Ctrl Pts',(-2.00000000049539,25.800000000286,0.));
#6706=CARTESIAN_POINT('Ctrl Pts',(-2.00000000049539,25.7416666669527,-1.15470053866527));
#6707=CARTESIAN_POINT('Ctrl Pts',(-1.0000000002477,25.6833333336194,-1.7320508079979));
#6708=CARTESIAN_POINT('Ctrl Pts',(-1.41410031865014E-16,25.625000000286,
-2.30940107733053));
#6709=CARTESIAN_POINT('Ctrl Pts',(1.0000000002477,25.5666666669527,-1.7320508079979));
#6710=CARTESIAN_POINT('Ctrl Pts',(2.00000000049539,25.5083333336194,-1.15470053866527));
#6711=CARTESIAN_POINT('Ctrl Pts',(2.00000000049539,25.450000000286,-2.44929359890139E-16));
#6712=CARTESIAN_POINT('Ctrl Pts',(2.00000000049539,25.3916666669527,1.15470053866527));
#6713=CARTESIAN_POINT('Ctrl Pts',(1.0000000002477,25.3333333336194,1.7320508079979));
#6714=CARTESIAN_POINT('Ctrl Pts',(4.24230095595043E-16,25.275000000286,
2.30940107733053));
#6715=CARTESIAN_POINT('Ctrl Pts',(-1.0000000002477,25.2166666669527,1.7320508079979));
#6716=CARTESIAN_POINT('Ctrl Pts',(-2.00000000049539,25.1583333336194,1.15470053866527));
#6717=CARTESIAN_POINT('Ctrl Pts',(-2.00000000049539,25.100000000286,0.));
#6718=CARTESIAN_POINT('Ctrl Pts',(-2.00000000049539,25.0416666669527,-1.15470053866527));
#6719=CARTESIAN_POINT('Ctrl Pts',(-1.0000000002477,24.9833333336194,-1.7320508079979));
#6720=CARTESIAN_POINT('Ctrl Pts',(-1.41410031865014E-16,24.925000000286,
-2.30940107733053));
#6721=CARTESIAN_POINT('Ctrl Pts',(1.0000000002477,24.8666666669527,-1.7320508079979));
#6722=CARTESIAN_POINT('Ctrl Pts',(2.00000000049539,24.8083333336194,-1.15470053866527));
#6723=CARTESIAN_POINT('Ctrl Pts',(2.00000000049539,24.750000000286,-2.44929359890139E-16));
#6724=CARTESIAN_POINT('Ctrl Pts',(2.00000000049539,24.6916666669527,1.15470053866527));
#6725=CARTESIAN_POINT('Ctrl Pts',(1.0000000002477,24.6333333336194,1.7320508079979));
#6726=CARTESIAN_POINT('Ctrl Pts',(4.24230095595043E-16,24.575000000286,
2.30940107733053));
#6727=CARTESIAN_POINT('Ctrl Pts',(-1.0000000002477,24.5166666669527,1.7320508079979));
#6728=CARTESIAN_POINT('Ctrl Pts',(-2.00000000049539,24.4583333336194,1.15470053866527));
#6729=CARTESIAN_POINT('Ctrl Pts',(-2.00000000049539,24.400000000286,0.));
#6730=CARTESIAN_POINT('Ctrl Pts',(-2.00000000049539,24.3416666669527,-1.15470053866527));
#6731=CARTESIAN_POINT('Ctrl Pts',(-1.0000000002477,24.2833333336194,-1.7320508079979));
#6732=CARTESIAN_POINT('Ctrl Pts',(-1.41410031865014E-16,24.225000000286,
-2.30940107733053));
#6733=CARTESIAN_POINT('Ctrl Pts',(1.0000000002477,24.1666666669527,-1.7320508079979));
#6734=CARTESIAN_POINT('Ctrl Pts',(2.00000000049539,24.1083333336194,-1.15470053866527));
#6735=CARTESIAN_POINT('Ctrl Pts',(2.00000000049539,24.050000000286,-2.44929359890139E-16));
#6736=CARTESIAN_POINT('Ctrl Pts',(2.00000000049539,23.9916666669527,1.15470053866527));
#6737=CARTESIAN_POINT('Ctrl Pts',(1.0000000002477,23.9333333336194,1.7320508079979));
#6738=CARTESIAN_POINT('Ctrl Pts',(4.24230095595043E-16,23.875000000286,
2.30940107733053));
#6739=CARTESIAN_POINT('Ctrl Pts',(-1.0000000002477,23.8166666669527,1.7320508079979));
#6740=CARTESIAN_POINT('Ctrl Pts',(-2.00000000049539,23.7583333336194,1.15470053866527));
#6741=CARTESIAN_POINT('Ctrl Pts',(-2.00000000049539,23.700000000286,0.));
#6742=CARTESIAN_POINT('Ctrl Pts',(-2.00000000049539,23.6416666669527,-1.15470053866527));
#6743=CARTESIAN_POINT('Ctrl Pts',(-1.0000000002477,23.5833333336194,-1.7320508079979));
#6744=CARTESIAN_POINT('Ctrl Pts',(-1.41410031865014E-16,23.525000000286,
-2.30940107733053));
#6745=CARTESIAN_POINT('Ctrl Pts',(1.0000000002477,23.4666666669527,-1.7320508079979));
#6746=CARTESIAN_POINT('Ctrl Pts',(2.00000000049539,23.4083333336194,-1.15470053866527));
#6747=CARTESIAN_POINT('Ctrl Pts',(2.00000000049539,23.350000000286,-2.44929359890139E-16));
#6748=CARTESIAN_POINT('Ctrl Pts',(2.00000000049539,23.2916666669527,1.15470053866527));
#6749=CARTESIAN_POINT('Ctrl Pts',(1.0000000002477,23.2333333336194,1.7320508079979));
#6750=CARTESIAN_POINT('Ctrl Pts',(4.24230095595043E-16,23.175000000286,
2.30940107733053));
#6751=CARTESIAN_POINT('Ctrl Pts',(-1.0000000002477,23.1166666669527,1.7320508079979));
#6752=CARTESIAN_POINT('Ctrl Pts',(-2.00000000049539,23.0583333336194,1.15470053866527));
#6753=CARTESIAN_POINT('Ctrl Pts',(-2.00000000049539,23.000000000286,0.));
#6754=CARTESIAN_POINT('Ctrl Pts',(-2.00000000049539,22.9416666669527,-1.15470053866527));
#6755=CARTESIAN_POINT('Ctrl Pts',(-1.0000000002477,22.8833333336194,-1.7320508079979));
#6756=CARTESIAN_POINT('Ctrl Pts',(-1.41410031865014E-16,22.825000000286,
-2.30940107733053));
#6757=CARTESIAN_POINT('Ctrl Pts',(1.0000000002477,22.7666666669527,-1.7320508079979));
#6758=CARTESIAN_POINT('Ctrl Pts',(2.00000000049539,22.7083333336194,-1.15470053866527));
#6759=CARTESIAN_POINT('Ctrl Pts',(2.00000000049539,22.650000000286,-2.44929359890139E-16));
#6760=CARTESIAN_POINT('Ctrl Pts',(2.00000000049539,22.5916666669527,1.15470053866527));
#6761=CARTESIAN_POINT('Ctrl Pts',(1.0000000002477,22.5333333336194,1.7320508079979));
#6762=CARTESIAN_POINT('Ctrl Pts',(4.24230095595043E-16,22.475000000286,
2.30940107733053));
#6763=CARTESIAN_POINT('Ctrl Pts',(-1.0000000002477,22.4166666669527,1.7320508079979));
#6764=CARTESIAN_POINT('Ctrl Pts',(-2.00000000049539,22.3583333336194,1.15470053866527));
#6765=CARTESIAN_POINT('Ctrl Pts',(-2.00000000049539,22.300000000286,0.));
#6766=CARTESIAN_POINT('Ctrl Pts',(-2.00000000049539,22.2416666669527,-1.15470053866527));
#6767=CARTESIAN_POINT('Ctrl Pts',(-1.0000000002477,22.1833333336194,-1.7320508079979));
#6768=CARTESIAN_POINT('Ctrl Pts',(-1.41410031865014E-16,22.125000000286,
-2.30940107733053));
#6769=CARTESIAN_POINT('Ctrl Pts',(1.0000000002477,22.0666666669527,-1.7320508079979));
#6770=CARTESIAN_POINT('Ctrl Pts',(2.00000000049539,22.0083333336194,-1.15470053866527));
#6771=CARTESIAN_POINT('Ctrl Pts',(2.00000000049539,21.950000000286,-2.44929359890139E-16));
#6772=CARTESIAN_POINT('Ctrl Pts',(2.00000000049539,21.8916666669527,1.15470053866527));
#6773=CARTESIAN_POINT('Ctrl Pts',(1.0000000002477,21.8333333336194,1.7320508079979));
#6774=CARTESIAN_POINT('Ctrl Pts',(4.24230095595043E-16,21.775000000286,
2.30940107733053));
#6775=CARTESIAN_POINT('Ctrl Pts',(-1.0000000002477,21.7166666669527,1.7320508079979));
#6776=CARTESIAN_POINT('Ctrl Pts',(-2.00000000049539,21.6583333336193,1.15470053866527));
#6777=CARTESIAN_POINT('Ctrl Pts',(-2.00000000049539,21.600000000286,0.));
#6778=CARTESIAN_POINT('Ctrl Pts',(-2.00000000049539,21.5416666669527,-1.15470053866527));
#6779=CARTESIAN_POINT('Ctrl Pts',(-1.0000000002477,21.4833333336194,-1.7320508079979));
#6780=CARTESIAN_POINT('Ctrl Pts',(-1.41410031865014E-16,21.425000000286,
-2.30940107733053));
#6781=CARTESIAN_POINT('Ctrl Pts',(1.0000000002477,21.3666666669527,-1.7320508079979));
#6782=CARTESIAN_POINT('Ctrl Pts',(2.00000000049539,21.3083333336193,-1.15470053866527));
#6783=CARTESIAN_POINT('Ctrl Pts',(2.00000000049539,21.250000000286,-2.44929359890139E-16));
#6784=CARTESIAN_POINT('Ctrl Pts',(2.00000000049539,21.1916666669527,1.15470053866527));
#6785=CARTESIAN_POINT('Ctrl Pts',(1.0000000002477,21.1333333336194,1.7320508079979));
#6786=CARTESIAN_POINT('Ctrl Pts',(4.24230095595043E-16,21.075000000286,
2.30940107733053));
#6787=CARTESIAN_POINT('Ctrl Pts',(-1.0000000002477,21.0166666669527,1.7320508079979));
#6788=CARTESIAN_POINT('Ctrl Pts',(-2.00000000049539,20.9583333336194,1.15470053866527));
#6789=CARTESIAN_POINT('Ctrl Pts',(-2.00000000049539,20.900000000286,0.));
#6790=CARTESIAN_POINT('Ctrl Pts',(-2.00000000049539,20.8416666669527,-1.15470053866527));
#6791=CARTESIAN_POINT('Ctrl Pts',(-1.0000000002477,20.7833333336194,-1.7320508079979));
#6792=CARTESIAN_POINT('Ctrl Pts',(-1.41410031865014E-16,20.725000000286,
-2.30940107733053));
#6793=CARTESIAN_POINT('Ctrl Pts',(1.0000000002477,20.6666666669527,-1.7320508079979));
#6794=CARTESIAN_POINT('Ctrl Pts',(2.00000000049539,20.6083333336194,-1.15470053866527));
#6795=CARTESIAN_POINT('Ctrl Pts',(2.00000000049539,20.550000000286,-2.44929359890139E-16));
#6796=CARTESIAN_POINT('Ctrl Pts',(2.00000000049539,20.4916666669527,1.15470053866527));
#6797=CARTESIAN_POINT('Ctrl Pts',(1.0000000002477,20.4333333336194,1.7320508079979));
#6798=CARTESIAN_POINT('Ctrl Pts',(4.24230095595043E-16,20.375000000286,
2.30940107733053));
#6799=CARTESIAN_POINT('Ctrl Pts',(-1.0000000002477,20.3166666669527,1.7320508079979));
#6800=CARTESIAN_POINT('Ctrl Pts',(-2.00000000049539,20.2583333336194,1.15470053866527));
#6801=CARTESIAN_POINT('Ctrl Pts',(-2.00000000049539,20.200000000286,0.));
#6802=CARTESIAN_POINT('Ctrl Pts',(-2.00000000049539,20.1416666669527,-1.15470053866527));
#6803=CARTESIAN_POINT('Ctrl Pts',(-1.0000000002477,20.0833333336194,-1.7320508079979));
#6804=CARTESIAN_POINT('Ctrl Pts',(-1.41410031865014E-16,20.025000000286,
-2.30940107733053));
#6805=CARTESIAN_POINT('Ctrl Pts',(1.0000000002477,19.9666666669527,-1.7320508079979));
#6806=CARTESIAN_POINT('Ctrl Pts',(2.00000000049539,19.9083333336194,-1.15470053866527));
#6807=CARTESIAN_POINT('Ctrl Pts',(2.00000000049539,19.850000000286,-2.44929359890139E-16));
#6808=CARTESIAN_POINT('Ctrl Pts',(2.00000000049539,19.7916666669527,1.15470053866527));
#6809=CARTESIAN_POINT('Ctrl Pts',(1.0000000002477,19.7333333336194,1.7320508079979));
#6810=CARTESIAN_POINT('Ctrl Pts',(4.24230095595043E-16,19.675000000286,
2.30940107733053));
#6811=CARTESIAN_POINT('Ctrl Pts',(-1.0000000002477,19.6166666669527,1.7320508079979));
#6812=CARTESIAN_POINT('Ctrl Pts',(-2.00000000049539,19.5583333336194,1.15470053866527));
#6813=CARTESIAN_POINT('Ctrl Pts',(-2.00000000049539,19.500000000286,0.));
#6814=CARTESIAN_POINT('Ctrl Pts',(-2.00000000049539,19.4416666669527,-1.15470053866527));
#6815=CARTESIAN_POINT('Ctrl Pts',(-1.0000000002477,19.3833333336194,-1.7320508079979));
#6816=CARTESIAN_POINT('Ctrl Pts',(-1.41410031865014E-16,19.325000000286,
-2.30940107733053));
#6817=CARTESIAN_POINT('Ctrl Pts',(1.0000000002477,19.2666666669527,-1.7320508079979));
#6818=CARTESIAN_POINT('Ctrl Pts',(2.00000000049539,19.2083333336194,-1.15470053866527));
#6819=CARTESIAN_POINT('Ctrl Pts',(2.00000000049539,19.150000000286,-2.44929359890139E-16));
#6820=CARTESIAN_POINT('Ctrl Pts',(2.00000000049539,19.0916666669527,1.15470053866527));
#6821=CARTESIAN_POINT('Ctrl Pts',(1.0000000002477,19.0333333336194,1.7320508079979));
#6822=CARTESIAN_POINT('Ctrl Pts',(4.24230095595043E-16,18.975000000286,
2.30940107733053));
#6823=CARTESIAN_POINT('Ctrl Pts',(-1.0000000002477,18.9166666669527,1.7320508079979));
#6824=CARTESIAN_POINT('Ctrl Pts',(-2.00000000049539,18.8583333336194,1.15470053866527));
#6825=CARTESIAN_POINT('Ctrl Pts',(-2.00000000049539,18.800000000286,0.));
#6826=CARTESIAN_POINT('Ctrl Pts',(-2.00000000049539,18.7416666669527,-1.15470053866527));
#6827=CARTESIAN_POINT('Ctrl Pts',(-1.0000000002477,18.6833333336194,-1.7320508079979));
#6828=CARTESIAN_POINT('Ctrl Pts',(-1.41410031865014E-16,18.625000000286,
-2.30940107733053));
#6829=CARTESIAN_POINT('Ctrl Pts',(1.0000000002477,18.5666666669527,-1.7320508079979));
#6830=CARTESIAN_POINT('Ctrl Pts',(2.00000000049539,18.5083333336194,-1.15470053866527));
#6831=CARTESIAN_POINT('Ctrl Pts',(2.00000000049539,18.450000000286,-2.44929359890139E-16));
#6832=CARTESIAN_POINT('Ctrl Pts',(2.00000000049539,18.3916666669527,1.15470053866527));
#6833=CARTESIAN_POINT('Ctrl Pts',(1.0000000002477,18.3333333336194,1.7320508079979));
#6834=CARTESIAN_POINT('Ctrl Pts',(4.24230095595043E-16,18.275000000286,
2.30940107733053));
#6835=CARTESIAN_POINT('Ctrl Pts',(-1.0000000002477,18.2166666669527,1.7320508079979));
#6836=CARTESIAN_POINT('Ctrl Pts',(-2.00000000049539,18.1583333336194,1.15470053866527));
#6837=CARTESIAN_POINT('Ctrl Pts',(-2.00000000049539,18.100000000286,0.));
#6838=CARTESIAN_POINT('Ctrl Pts',(-2.00000000049539,18.0416666669527,-1.15470053866527));
#6839=CARTESIAN_POINT('Ctrl Pts',(-1.0000000002477,17.9833333336194,-1.7320508079979));
#6840=CARTESIAN_POINT('Ctrl Pts',(-1.41410031865014E-16,17.925000000286,
-2.30940107733053));
#6841=CARTESIAN_POINT('Ctrl Pts',(1.0000000002477,17.8666666669527,-1.7320508079979));
#6842=CARTESIAN_POINT('Ctrl Pts',(2.00000000049539,17.8083333336194,-1.15470053866527));
#6843=CARTESIAN_POINT('Ctrl Pts',(2.00000000049539,17.750000000286,-2.44929359890139E-16));
#6844=CARTESIAN_POINT('Ctrl Pts',(2.00000000049539,17.6916666669527,1.15470053866527));
#6845=CARTESIAN_POINT('Ctrl Pts',(1.0000000002477,17.6333333336194,1.7320508079979));
#6846=CARTESIAN_POINT('Ctrl Pts',(4.24230095595043E-16,17.575000000286,
2.30940107733053));
#6847=CARTESIAN_POINT('Ctrl Pts',(-1.0000000002477,17.5166666669527,1.7320508079979));
#6848=CARTESIAN_POINT('Ctrl Pts',(-2.00000000049539,17.4583333336194,1.15470053866527));
#6849=CARTESIAN_POINT('Ctrl Pts',(-2.00000000049539,17.400000000286,0.));
#6850=CARTESIAN_POINT('Ctrl Pts',(-2.00000000049539,17.3416666669527,-1.15470053866527));
#6851=CARTESIAN_POINT('Ctrl Pts',(-1.0000000002477,17.2833333336194,-1.7320508079979));
#6852=CARTESIAN_POINT('Ctrl Pts',(-1.41410031865014E-16,17.225000000286,
-2.30940107733053));
#6853=CARTESIAN_POINT('Ctrl Pts',(1.0000000002477,17.1666666669527,-1.7320508079979));
#6854=CARTESIAN_POINT('Ctrl Pts',(2.00000000049539,17.1083333336194,-1.15470053866527));
#6855=CARTESIAN_POINT('Ctrl Pts',(2.00000000049539,17.050000000286,-2.44929359890139E-16));
#6856=CARTESIAN_POINT('Ctrl Pts',(2.00000000049539,16.9916666669527,1.15470053866527));
#6857=CARTESIAN_POINT('Ctrl Pts',(1.0000000002477,16.9333333336194,1.7320508079979));
#6858=CARTESIAN_POINT('Ctrl Pts',(4.24230095595043E-16,16.875000000286,
2.30940107733053));
#6859=CARTESIAN_POINT('Ctrl Pts',(-1.0000000002477,16.8166666669527,1.7320508079979));
#6860=CARTESIAN_POINT('Ctrl Pts',(-2.00000000049539,16.7583333336194,1.15470053866527));
#6861=CARTESIAN_POINT('Ctrl Pts',(-2.00000000049539,16.700000000286,0.));
#6862=CARTESIAN_POINT('Ctrl Pts',(-2.00000000049539,16.6416666669527,-1.15470053866527));
#6863=CARTESIAN_POINT('Ctrl Pts',(-1.0000000002477,16.5833333336194,-1.7320508079979));
#6864=CARTESIAN_POINT('Ctrl Pts',(-1.41410031865014E-16,16.525000000286,
-2.30940107733053));
#6865=CARTESIAN_POINT('Ctrl Pts',(1.0000000002477,16.4666666669527,-1.7320508079979));
#6866=CARTESIAN_POINT('Ctrl Pts',(2.00000000049539,16.4083333336194,-1.15470053866527));
#6867=CARTESIAN_POINT('Ctrl Pts',(2.00000000049539,16.350000000286,-2.44929359890139E-16));
#6868=CARTESIAN_POINT('Ctrl Pts',(2.00000000049539,16.2916666669527,1.15470053866527));
#6869=CARTESIAN_POINT('Ctrl Pts',(1.0000000002477,16.2333333336194,1.7320508079979));
#6870=CARTESIAN_POINT('Ctrl Pts',(4.24230095595043E-16,16.175000000286,
2.30940107733053));
#6871=CARTESIAN_POINT('Ctrl Pts',(-1.0000000002477,16.1166666669527,1.7320508079979));
#6872=CARTESIAN_POINT('Ctrl Pts',(-2.00000000049539,16.0583333336194,1.15470053866527));
#6873=CARTESIAN_POINT('Ctrl Pts',(-2.00000000049539,16.000000000286,0.));
#6874=CARTESIAN_POINT('Ctrl Pts',(-2.00000000049539,15.9416666669527,-1.15470053866527));
#6875=CARTESIAN_POINT('Ctrl Pts',(-1.0000000002477,15.8833333336194,-1.7320508079979));
#6876=CARTESIAN_POINT('Ctrl Pts',(-1.41410031865014E-16,15.825000000286,
-2.30940107733053));
#6877=CARTESIAN_POINT('Ctrl Pts',(1.0000000002477,15.7666666669527,-1.7320508079979));
#6878=CARTESIAN_POINT('Ctrl Pts',(2.00000000049539,15.7083333336194,-1.15470053866527));
#6879=CARTESIAN_POINT('Ctrl Pts',(2.00000000049539,15.650000000286,-2.44929359890139E-16));
#6880=CARTESIAN_POINT('Ctrl Pts',(2.00000000049539,15.5916666669527,1.15470053866527));
#6881=CARTESIAN_POINT('Ctrl Pts',(1.0000000002477,15.5333333336194,1.7320508079979));
#6882=CARTESIAN_POINT('Ctrl Pts',(4.24230095595043E-16,15.475000000286,
2.30940107733053));
#6883=CARTESIAN_POINT('Ctrl Pts',(-1.0000000002477,15.4166666669527,1.7320508079979));
#6884=CARTESIAN_POINT('Ctrl Pts',(-2.00000000049539,15.3583333336194,1.15470053866527));
#6885=CARTESIAN_POINT('Ctrl Pts',(-2.00000000049539,15.300000000286,0.));
#6886=CARTESIAN_POINT('Ctrl Pts',(-2.00000000049539,15.2416666669527,-1.15470053866527));
#6887=CARTESIAN_POINT('Ctrl Pts',(-1.0000000002477,15.1833333336194,-1.7320508079979));
#6888=CARTESIAN_POINT('Ctrl Pts',(-1.41410031865014E-16,15.125000000286,
-2.30940107733053));
#6889=CARTESIAN_POINT('Ctrl Pts',(1.0000000002477,15.0666666669527,-1.7320508079979));
#6890=CARTESIAN_POINT('Ctrl Pts',(2.00000000049539,15.0083333336194,-1.15470053866527));
#6891=CARTESIAN_POINT('Ctrl Pts',(2.00000000049539,14.950000000286,-2.44929359890139E-16));
#6892=CARTESIAN_POINT('Ctrl Pts',(2.00000000049539,14.8916666669527,1.15470053866527));
#6893=CARTESIAN_POINT('Ctrl Pts',(1.0000000002477,14.8333333336194,1.7320508079979));
#6894=CARTESIAN_POINT('Ctrl Pts',(4.24230095595043E-16,14.775000000286,
2.30940107733053));
#6895=CARTESIAN_POINT('Ctrl Pts',(-1.0000000002477,14.7166666669527,1.7320508079979));
#6896=CARTESIAN_POINT('Ctrl Pts',(-2.00000000049539,14.6583333336194,1.15470053866527));
#6897=CARTESIAN_POINT('Ctrl Pts',(-2.00000000049539,14.600000000286,0.));
#6898=CARTESIAN_POINT('Ctrl Pts',(-2.00000000049539,14.5416666669527,-1.15470053866527));
#6899=CARTESIAN_POINT('Ctrl Pts',(-1.0000000002477,14.4833333336194,-1.7320508079979));
#6900=CARTESIAN_POINT('Ctrl Pts',(-1.41410031865014E-16,14.425000000286,
-2.30940107733053));
#6901=CARTESIAN_POINT('Ctrl Pts',(1.0000000002477,14.3666666669527,-1.7320508079979));
#6902=CARTESIAN_POINT('Ctrl Pts',(2.00000000049539,14.3083333336194,-1.15470053866527));
#6903=CARTESIAN_POINT('Ctrl Pts',(2.00000000049539,14.250000000286,-2.44929359890139E-16));
#6904=CARTESIAN_POINT('Ctrl Pts',(2.00000000049539,14.1916666669527,1.15470053866527));
#6905=CARTESIAN_POINT('Ctrl Pts',(1.0000000002477,14.1333333336194,1.7320508079979));
#6906=CARTESIAN_POINT('Ctrl Pts',(4.24230095595043E-16,14.075000000286,
2.30940107733053));
#6907=CARTESIAN_POINT('Ctrl Pts',(-1.0000000002477,14.0166666669527,1.7320508079979));
#6908=CARTESIAN_POINT('Ctrl Pts',(-2.00000000049539,13.9583333336194,1.15470053866527));
#6909=CARTESIAN_POINT('Ctrl Pts',(-2.00000000049539,13.900000000286,0.));
#6910=CARTESIAN_POINT('Ctrl Pts',(-2.00000000049539,13.8416666669527,-1.15470053866527));
#6911=CARTESIAN_POINT('Ctrl Pts',(-1.0000000002477,13.7833333336194,-1.7320508079979));
#6912=CARTESIAN_POINT('Ctrl Pts',(-1.41410031865014E-16,13.725000000286,
-2.30940107733053));
#6913=CARTESIAN_POINT('Ctrl Pts',(1.0000000002477,13.6666666669527,-1.7320508079979));
#6914=CARTESIAN_POINT('Ctrl Pts',(2.00000000049539,13.6083333336194,-1.15470053866527));
#6915=CARTESIAN_POINT('Ctrl Pts',(2.00000000049539,13.550000000286,-2.44929359890139E-16));
#6916=CARTESIAN_POINT('Ctrl Pts',(2.00000000049539,13.4916666669527,1.15470053866527));
#6917=CARTESIAN_POINT('Ctrl Pts',(1.0000000002477,13.4333333336194,1.7320508079979));
#6918=CARTESIAN_POINT('Ctrl Pts',(4.24230095595043E-16,13.375000000286,
2.30940107733053));
#6919=CARTESIAN_POINT('Ctrl Pts',(-1.0000000002477,13.3166666669527,1.7320508079979));
#6920=CARTESIAN_POINT('Ctrl Pts',(-2.00000000049539,13.2583333336194,1.15470053866527));
#6921=CARTESIAN_POINT('Ctrl Pts',(-2.00000000049539,13.200000000286,0.));
#6922=CARTESIAN_POINT('Ctrl Pts',(-2.00000000049539,13.1416666669527,-1.15470053866527));
#6923=CARTESIAN_POINT('Ctrl Pts',(-1.0000000002477,13.0833333336194,-1.7320508079979));
#6924=CARTESIAN_POINT('Ctrl Pts',(-1.41410031865014E-16,13.025000000286,
-2.30940107733053));
#6925=CARTESIAN_POINT('Ctrl Pts',(1.0000000002477,12.9666666669527,-1.7320508079979));
#6926=CARTESIAN_POINT('Ctrl Pts',(2.00000000049539,12.9083333336194,-1.15470053866527));
#6927=CARTESIAN_POINT('Ctrl Pts',(2.00000000049539,12.850000000286,-2.44929359890139E-16));
#6928=CARTESIAN_POINT('Ctrl Pts',(2.00000000049539,12.7916666669527,1.15470053866527));
#6929=CARTESIAN_POINT('Ctrl Pts',(1.0000000002477,12.7333333336194,1.7320508079979));
#6930=CARTESIAN_POINT('Ctrl Pts',(4.24230095595043E-16,12.675000000286,
2.30940107733053));
#6931=CARTESIAN_POINT('Ctrl Pts',(-1.0000000002477,12.6166666669527,1.7320508079979));
#6932=CARTESIAN_POINT('Ctrl Pts',(-2.00000000049539,12.5583333336194,1.15470053866527));
#6933=CARTESIAN_POINT('Ctrl Pts',(-2.00000000049539,12.500000000286,0.));
#6934=CARTESIAN_POINT('Ctrl Pts',(-2.00000000049539,12.4416666669527,-1.15470053866527));
#6935=CARTESIAN_POINT('Ctrl Pts',(-1.0000000002477,12.3833333336194,-1.7320508079979));
#6936=CARTESIAN_POINT('Ctrl Pts',(-1.41410031865014E-16,12.325000000286,
-2.30940107733053));
#6937=CARTESIAN_POINT('Ctrl Pts',(1.0000000002477,12.2666666669527,-1.7320508079979));
#6938=CARTESIAN_POINT('Ctrl Pts',(2.00000000049539,12.2083333336194,-1.15470053866527));
#6939=CARTESIAN_POINT('Ctrl Pts',(2.00000000049539,12.150000000286,-2.44929359890139E-16));
#6940=CARTESIAN_POINT('Ctrl Pts',(2.00000000049539,12.0916666669527,1.15470053866527));
#6941=CARTESIAN_POINT('Ctrl Pts',(1.0000000002477,12.0333333336194,1.7320508079979));
#6942=CARTESIAN_POINT('Ctrl Pts',(4.24230095595043E-16,11.975000000286,
2.30940107733053));
#6943=CARTESIAN_POINT('Ctrl Pts',(-1.0000000002477,11.9166666669527,1.7320508079979));
#6944=CARTESIAN_POINT('Ctrl Pts',(-2.00000000049539,11.8583333336194,1.15470053866527));
#6945=CARTESIAN_POINT('Ctrl Pts',(-2.00000000049539,11.800000000286,0.));
#6946=CARTESIAN_POINT('Ctrl Pts',(-2.00000000049539,11.7416666669527,-1.15470053866527));
#6947=CARTESIAN_POINT('Ctrl Pts',(-1.0000000002477,11.6833333336194,-1.7320508079979));
#6948=CARTESIAN_POINT('Ctrl Pts',(-1.41410031865014E-16,11.625000000286,
-2.30940107733053));
#6949=CARTESIAN_POINT('Ctrl Pts',(1.0000000002477,11.5666666669527,-1.7320508079979));
#6950=CARTESIAN_POINT('Ctrl Pts',(2.00000000049539,11.5083333336194,-1.15470053866527));
#6951=CARTESIAN_POINT('Ctrl Pts',(2.00000000049539,11.450000000286,-2.44929359890139E-16));
#6952=CARTESIAN_POINT('Ctrl Pts',(2.00000000049539,11.3916666669527,1.15470053866527));
#6953=CARTESIAN_POINT('Ctrl Pts',(1.0000000002477,11.3333333336194,1.7320508079979));
#6954=CARTESIAN_POINT('Ctrl Pts',(4.24230095595043E-16,11.275000000286,
2.30940107733053));
#6955=CARTESIAN_POINT('Ctrl Pts',(-1.0000000002477,11.2166666669527,1.7320508079979));
#6956=CARTESIAN_POINT('Ctrl Pts',(-2.00000000049539,11.1583333336194,1.15470053866527));
#6957=CARTESIAN_POINT('Ctrl Pts',(-2.00000000049539,11.100000000286,0.));
#6958=CARTESIAN_POINT('Ctrl Pts',(-2.00000000049539,11.0416666669527,-1.15470053866527));
#6959=CARTESIAN_POINT('Ctrl Pts',(-1.0000000002477,10.9833333336194,-1.7320508079979));
#6960=CARTESIAN_POINT('Ctrl Pts',(-1.41410031865014E-16,10.925000000286,
-2.30940107733053));
#6961=CARTESIAN_POINT('Ctrl Pts',(1.0000000002477,10.8666666669527,-1.7320508079979));
#6962=CARTESIAN_POINT('Ctrl Pts',(2.00000000049539,10.8083333336194,-1.15470053866527));
#6963=CARTESIAN_POINT('Ctrl Pts',(2.00000000049539,10.750000000286,-2.44929359890139E-16));
#6964=CARTESIAN_POINT('Ctrl Pts',(2.00000000049539,10.6916666669527,1.15470053866527));
#6965=CARTESIAN_POINT('Ctrl Pts',(1.0000000002477,10.6333333336194,1.7320508079979));
#6966=CARTESIAN_POINT('Ctrl Pts',(4.24230095595043E-16,10.575000000286,
2.30940107733053));
#6967=CARTESIAN_POINT('Ctrl Pts',(-1.0000000002477,10.5166666669527,1.7320508079979));
#6968=CARTESIAN_POINT('Ctrl Pts',(-2.00000000049539,10.4583333336194,1.15470053866527));
#6969=CARTESIAN_POINT('Ctrl Pts',(-2.00000000049539,10.400000000286,0.));
#6970=CARTESIAN_POINT('Ctrl Pts',(-2.00000000049539,10.3416666669527,-1.15470053866527));
#6971=CARTESIAN_POINT('Ctrl Pts',(-1.0000000002477,10.2833333336194,-1.7320508079979));
#6972=CARTESIAN_POINT('Ctrl Pts',(-1.41410031865014E-16,10.225000000286,
-2.30940107733053));
#6973=CARTESIAN_POINT('Ctrl Pts',(1.0000000002477,10.1666666669527,-1.7320508079979));
#6974=CARTESIAN_POINT('Ctrl Pts',(2.00000000049539,10.1083333336194,-1.15470053866527));
#6975=CARTESIAN_POINT('Ctrl Pts',(2.00000000049539,10.050000000286,-2.44929359890139E-16));
#6976=CARTESIAN_POINT('Ctrl Pts',(2.00000000049539,9.99166666695269,1.15470053866527));
#6977=CARTESIAN_POINT('Ctrl Pts',(1.0000000002477,9.93333333361936,1.7320508079979));
#6978=CARTESIAN_POINT('Ctrl Pts',(4.24230095595043E-16,9.87500000028603,
2.30940107733053));
#6979=CARTESIAN_POINT('Ctrl Pts',(-1.0000000002477,9.81666666695269,1.7320508079979));
#6980=CARTESIAN_POINT('Ctrl Pts',(-2.00000000049539,9.75833333361936,1.15470053866527));
#6981=CARTESIAN_POINT('Ctrl Pts',(-2.00000000049539,9.70000000028602,0.));
#6982=CARTESIAN_POINT('Ctrl Pts',(-2.00000000049539,9.64166666695269,-1.15470053866527));
#6983=CARTESIAN_POINT('Ctrl Pts',(-1.0000000002477,9.58333333361935,-1.7320508079979));
#6984=CARTESIAN_POINT('Ctrl Pts',(-1.41410031865014E-16,9.52500000028602,
-2.30940107733053));
#6985=CARTESIAN_POINT('Ctrl Pts',(1.0000000002477,9.4666666669527,-1.7320508079979));
#6986=CARTESIAN_POINT('Ctrl Pts',(2.00000000049539,9.40833333361935,-1.15470053866527));
#6987=CARTESIAN_POINT('Ctrl Pts',(2.00000000049539,9.35000000028603,-2.44929359890139E-16));
#6988=CARTESIAN_POINT('Ctrl Pts',(2.00000000049539,9.29166666695269,1.15470053866527));
#6989=CARTESIAN_POINT('Ctrl Pts',(1.0000000002477,9.23333333361936,1.7320508079979));
#6990=CARTESIAN_POINT('Ctrl Pts',(4.24230095595043E-16,9.17500000028602,
2.30940107733053));
#6991=CARTESIAN_POINT('Ctrl Pts',(-1.0000000002477,9.11666666695269,1.7320508079979));
#6992=CARTESIAN_POINT('Ctrl Pts',(-2.00000000049539,9.05833333361936,1.15470053866527));
#6993=CARTESIAN_POINT('Ctrl Pts',(-2.00000000049539,9.00000000028602,0.));
#6994=CARTESIAN_POINT('Ctrl Pts',(-2.00000000049539,8.9416666669527,-1.15470053866527));
#6995=CARTESIAN_POINT('Ctrl Pts',(-1.0000000002477,8.88333333361936,-1.7320508079979));
#6996=CARTESIAN_POINT('Ctrl Pts',(-1.41410031865014E-16,8.82500000028603,
-2.30940107733053));
#6997=CARTESIAN_POINT('Ctrl Pts',(1.0000000002477,8.76666666695269,-1.7320508079979));
#6998=CARTESIAN_POINT('Ctrl Pts',(2.00000000049539,8.70833333361936,-1.15470053866527));
#6999=CARTESIAN_POINT('Ctrl Pts',(2.00000000049539,8.65000000028602,-2.44929359890139E-16));
#7000=CARTESIAN_POINT('Ctrl Pts',(2.00000000049539,8.59166666695269,1.15470053866527));
#7001=CARTESIAN_POINT('Ctrl Pts',(1.0000000002477,8.53333333361935,1.7320508079979));
#7002=CARTESIAN_POINT('Ctrl Pts',(4.24230095595043E-16,8.47500000028603,
2.30940107733053));
#7003=CARTESIAN_POINT('Ctrl Pts',(-1.0000000002477,8.41666666695269,1.7320508079979));
#7004=CARTESIAN_POINT('Ctrl Pts',(-2.00000000049539,8.35833333361936,1.15470053866527));
#7005=CARTESIAN_POINT('Ctrl Pts',(-2.00000000049539,8.30000000028603,0.));
#7006=CARTESIAN_POINT('Ctrl Pts',(-2.00000000049539,8.24166666695269,-1.15470053866527));
#7007=CARTESIAN_POINT('Ctrl Pts',(-1.0000000002477,8.18333333361936,-1.7320508079979));
#7008=CARTESIAN_POINT('Ctrl Pts',(-1.41410031865014E-16,8.12500000028602,
-2.30940107733053));
#7009=CARTESIAN_POINT('Ctrl Pts',(1.0000000002477,8.0666666669527,-1.7320508079979));
#7010=CARTESIAN_POINT('Ctrl Pts',(2.00000000049539,8.00833333361936,-1.15470053866527));
#7011=CARTESIAN_POINT('Ctrl Pts',(2.00000000049539,7.95000000028603,-2.44929359890139E-16));
#7012=CARTESIAN_POINT('Ctrl Pts',(2.00000000049539,7.89166666695269,1.15470053866527));
#7013=CARTESIAN_POINT('Ctrl Pts',(1.0000000002477,7.83333333361936,1.7320508079979));
#7014=CARTESIAN_POINT('Ctrl Pts',(4.24230095595043E-16,7.77500000028602,
2.30940107733053));
#7015=CARTESIAN_POINT('Ctrl Pts',(-1.0000000002477,7.71666666695269,1.7320508079979));
#7016=CARTESIAN_POINT('Ctrl Pts',(-2.00000000049539,7.65833333361935,1.15470053866527));
#7017=CARTESIAN_POINT('Ctrl Pts',(-2.00000000049539,7.60000000028603,0.));
#7018=CARTESIAN_POINT('Ctrl Pts',(-2.00000000049539,7.5416666669527,-1.15470053866527));
#7019=CARTESIAN_POINT('Ctrl Pts',(-1.0000000002477,7.48333333361936,-1.7320508079979));
#7020=CARTESIAN_POINT('Ctrl Pts',(-1.41410031865014E-16,7.42500000028603,
-2.30940107733053));
#7021=CARTESIAN_POINT('Ctrl Pts',(1.0000000002477,7.36666666695269,-1.7320508079979));
#7022=CARTESIAN_POINT('Ctrl Pts',(2.00000000049539,7.30833333361936,-1.15470053866527));
#7023=CARTESIAN_POINT('Ctrl Pts',(2.00000000049539,7.25000000028602,-2.44929359890139E-16));
#7024=CARTESIAN_POINT('Ctrl Pts',(2.00000000049539,7.1916666669527,1.15470053866527));
#7025=CARTESIAN_POINT('Ctrl Pts',(1.0000000002477,7.13333333361935,1.7320508079979));
#7026=CARTESIAN_POINT('Ctrl Pts',(4.24230095595043E-16,7.07500000028603,
2.30940107733053));
#7027=CARTESIAN_POINT('Ctrl Pts',(-1.0000000002477,7.01666666695269,1.7320508079979));
#7028=CARTESIAN_POINT('Ctrl Pts',(-2.00000000049539,6.95833333361936,1.15470053866527));
#7029=CARTESIAN_POINT('Ctrl Pts',(-2.00000000049539,6.90000000028602,0.));
#7030=CARTESIAN_POINT('Ctrl Pts',(-2.00000000049539,6.84166666695269,-1.15470053866527));
#7031=CARTESIAN_POINT('Ctrl Pts',(-1.0000000002477,6.78333333361935,-1.7320508079979));
#7032=CARTESIAN_POINT('Ctrl Pts',(-1.41410031865014E-16,6.72500000028603,
-2.30940107733053));
#7033=CARTESIAN_POINT('Ctrl Pts',(1.0000000002477,6.6666666669527,-1.7320508079979));
#7034=CARTESIAN_POINT('Ctrl Pts',(2.00000000049539,6.60833333361936,-1.15470053866527));
#7035=CARTESIAN_POINT('Ctrl Pts',(2.00000000049539,6.55000000028603,-2.44929359890139E-16));
#7036=CARTESIAN_POINT('Ctrl Pts',(2.00000000049539,6.49166666695269,1.15470053866527));
#7037=CARTESIAN_POINT('Ctrl Pts',(1.0000000002477,6.43333333361936,1.7320508079979));
#7038=CARTESIAN_POINT('Ctrl Pts',(4.24230095595043E-16,6.37500000028602,
2.30940107733053));
#7039=CARTESIAN_POINT('Ctrl Pts',(-1.0000000002477,6.31666666695269,1.7320508079979));
#7040=CARTESIAN_POINT('Ctrl Pts',(-2.00000000049539,6.25833333361935,1.15470053866527));
#7041=CARTESIAN_POINT('Ctrl Pts',(-2.00000000049539,6.20000000028603,0.));
#7042=CARTESIAN_POINT('Ctrl Pts',(-2.00000000049539,6.14166666695269,-1.15470053866527));
#7043=CARTESIAN_POINT('Ctrl Pts',(-1.0000000002477,6.08333333361936,-1.7320508079979));
#7044=CARTESIAN_POINT('Ctrl Pts',(-1.41410031865014E-16,6.02500000028602,
-2.30940107733053));
#7045=CARTESIAN_POINT('Ctrl Pts',(1.0000000002477,5.96666666695269,-1.7320508079979));
#7046=CARTESIAN_POINT('Ctrl Pts',(2.00000000049539,5.90833333361937,-1.15470053866527));
#7047=CARTESIAN_POINT('Ctrl Pts',(2.00000000049539,5.85000000028602,-2.44929359890139E-16));
#7048=CARTESIAN_POINT('Ctrl Pts',(2.00000000049539,5.7916666669527,1.15470053866527));
#7049=CARTESIAN_POINT('Ctrl Pts',(1.0000000002477,5.73333333361935,1.7320508079979));
#7050=CARTESIAN_POINT('Ctrl Pts',(4.24230095595043E-16,5.67500000028603,
2.30940107733053));
#7051=CARTESIAN_POINT('Ctrl Pts',(-1.0000000002477,5.61666666695269,1.7320508079979));
#7052=CARTESIAN_POINT('Ctrl Pts',(-2.00000000049539,5.55833333361936,1.15470053866527));
#7053=CARTESIAN_POINT('Ctrl Pts',(-2.00000000049539,5.50000000028602,0.));
#7054=CARTESIAN_POINT('Ctrl Pts',(-2.00000000049539,5.44166666695269,-1.15470053866527));
#7055=CARTESIAN_POINT('Ctrl Pts',(-1.0000000002477,5.38333333361935,-1.7320508079979));
#7056=CARTESIAN_POINT('Ctrl Pts',(-1.41410031865014E-16,5.32500000028603,
-2.30940107733053));
#7057=CARTESIAN_POINT('Ctrl Pts',(1.0000000002477,5.26666666695268,-1.7320508079979));
#7058=CARTESIAN_POINT('Ctrl Pts',(2.00000000049539,5.20833333361936,-1.15470053866527));
#7059=CARTESIAN_POINT('Ctrl Pts',(2.00000000049539,5.15000000028603,-2.44929359890139E-16));
#7060=CARTESIAN_POINT('Ctrl Pts',(2.00000000049539,5.09166666695269,1.15470053866527));
#7061=CARTESIAN_POINT('Ctrl Pts',(1.0000000002477,5.03333333361936,1.7320508079979));
#7062=CARTESIAN_POINT('Ctrl Pts',(4.24230095595043E-16,4.97500000028602,
2.30940107733053));
#7063=CARTESIAN_POINT('Ctrl Pts',(-1.0000000002477,4.9166666669527,1.7320508079979));
#7064=CARTESIAN_POINT('Ctrl Pts',(-2.00000000049539,4.85833333361936,1.15470053866527));
#7065=CARTESIAN_POINT('Ctrl Pts',(-2.00000000049539,4.80000000028603,0.));
#7066=CARTESIAN_POINT('Ctrl Pts',(-2.00000000049539,4.74166666695269,-1.15470053866527));
#7067=CARTESIAN_POINT('Ctrl Pts',(-1.0000000002477,4.68333333361936,-1.7320508079979));
#7068=CARTESIAN_POINT('Ctrl Pts',(-1.41410031865014E-16,4.62500000028602,
-2.30940107733053));
#7069=CARTESIAN_POINT('Ctrl Pts',(1.0000000002477,4.56666666695269,-1.7320508079979));
#7070=CARTESIAN_POINT('Ctrl Pts',(2.00000000049539,4.50833333361935,-1.15470053866527));
#7071=CARTESIAN_POINT('Ctrl Pts',(2.00000000049539,4.45000000028603,-2.44929359890139E-16));
#7072=CARTESIAN_POINT('Ctrl Pts',(2.00000000049539,4.3916666669527,1.15470053866527));
#7073=CARTESIAN_POINT('Ctrl Pts',(1.0000000002477,4.33333333361936,1.7320508079979));
#7074=CARTESIAN_POINT('Ctrl Pts',(4.24230095595043E-16,4.27500000028603,
2.30940107733053));
#7075=CARTESIAN_POINT('Ctrl Pts',(-1.0000000002477,4.21666666695269,1.7320508079979));
#7076=CARTESIAN_POINT('Ctrl Pts',(-2.00000000049539,4.15833333361936,1.15470053866527));
#7077=CARTESIAN_POINT('Ctrl Pts',(-2.00000000049539,4.10000000028602,0.));
#7078=CARTESIAN_POINT('Ctrl Pts',(-2.00000000049539,4.0416666669527,-1.15470053866527));
#7079=CARTESIAN_POINT('Ctrl Pts',(-1.0000000002477,3.98333333361935,-1.7320508079979));
#7080=CARTESIAN_POINT('Ctrl Pts',(-1.41410031865014E-16,3.92500000028603,
-2.30940107733053));
#7081=CARTESIAN_POINT('Ctrl Pts',(1.0000000002477,3.86666666695269,-1.7320508079979));
#7082=CARTESIAN_POINT('Ctrl Pts',(2.00000000049539,3.80833333361936,-1.15470053866527));
#7083=CARTESIAN_POINT('Ctrl Pts',(2.00000000049539,3.75000000028602,-2.44929359890139E-16));
#7084=CARTESIAN_POINT('Ctrl Pts',(2.00000000049539,3.69166666695269,1.15470053866527));
#7085=CARTESIAN_POINT('Ctrl Pts',(1.0000000002477,3.63333333361935,1.7320508079979));
#7086=CARTESIAN_POINT('Ctrl Pts',(4.24230095595043E-16,3.57500000028602,
2.30940107733053));
#7087=CARTESIAN_POINT('Ctrl Pts',(-1.0000000002477,3.5166666669527,1.7320508079979));
#7088=CARTESIAN_POINT('Ctrl Pts',(-2.00000000049539,3.45833333361936,1.15470053866527));
#7089=CARTESIAN_POINT('Ctrl Pts',(-2.00000000049539,3.40000000028603,0.));
#7090=CARTESIAN_POINT('Ctrl Pts',(-2.00000000049539,3.34166666695269,-1.15470053866527));
#7091=CARTESIAN_POINT('Ctrl Pts',(-1.0000000002477,3.28333333361936,-1.7320508079979));
#7092=CARTESIAN_POINT('Ctrl Pts',(-1.41410031865014E-16,3.22500000028602,
-2.30940107733053));
#7093=CARTESIAN_POINT('Ctrl Pts',(1.0000000002477,3.16666666695269,-1.7320508079979));
#7094=CARTESIAN_POINT('Ctrl Pts',(2.00000000049539,3.10833333361935,-1.15470053866527));
#7095=CARTESIAN_POINT('Ctrl Pts',(2.00000000049539,3.05000000028603,-2.44929359890139E-16));
#7096=CARTESIAN_POINT('Ctrl Pts',(2.00000000049539,2.99166666695269,1.15470053866527));
#7097=CARTESIAN_POINT('Ctrl Pts',(1.0000000002477,2.93333333361936,1.7320508079979));
#7098=CARTESIAN_POINT('Ctrl Pts',(4.24230095595043E-16,2.87500000028602,
2.30940107733053));
#7099=CARTESIAN_POINT('Ctrl Pts',(-1.0000000002477,2.81666666695269,1.7320508079979));
#7100=CARTESIAN_POINT('Ctrl Pts',(-2.00000000049539,2.75833333361936,1.15470053866527));
#7101=CARTESIAN_POINT('Ctrl Pts',(-2.00000000049539,2.70000000028602,0.));
#7102=CARTESIAN_POINT('Ctrl Pts',(-2.00000000049539,2.6416666669527,-1.15470053866527));
#7103=CARTESIAN_POINT('Ctrl Pts',(-1.0000000002477,2.58333333361936,-1.7320508079979));
#7104=CARTESIAN_POINT('Ctrl Pts',(-1.41410031865014E-16,2.52500000028603,
-2.30940107733053));
#7105=CARTESIAN_POINT('Ctrl Pts',(1.0000000002477,2.46666666695269,-1.7320508079979));
#7106=CARTESIAN_POINT('Ctrl Pts',(2.00000000049539,2.40833333361936,-1.15470053866527));
#7107=CARTESIAN_POINT('Ctrl Pts',(2.00000000049539,2.35000000028602,-2.44929359890139E-16));
#7108=CARTESIAN_POINT('Ctrl Pts',(2.00000000049539,2.29166666695269,1.15470053866527));
#7109=CARTESIAN_POINT('Ctrl Pts',(1.0000000002477,2.23333333361935,1.7320508079979));
#7110=CARTESIAN_POINT('Ctrl Pts',(4.24230095595043E-16,2.17500000028603,
2.30940107733053));
#7111=CARTESIAN_POINT('Ctrl Pts',(-1.0000000002477,2.11666666695269,1.7320508079979));
#7112=CARTESIAN_POINT('Ctrl Pts',(-2.00000000049539,2.05833333361936,1.15470053866527));
#7113=CARTESIAN_POINT('Ctrl Pts',(-2.00000000049539,2.00000000028603,0.));
#7114=CARTESIAN_POINT('Ctrl Pts',(-2.00000000049539,1.94166666695269,-1.15470053866527));
#7115=CARTESIAN_POINT('Ctrl Pts',(-1.0000000002477,1.88333333361936,-1.7320508079979));
#7116=CARTESIAN_POINT('Ctrl Pts',(-1.41410031865014E-16,1.82500000028602,
-2.30940107733053));
#7117=CARTESIAN_POINT('Ctrl Pts',(1.0000000002477,1.7666666669527,-1.7320508079979));
#7118=CARTESIAN_POINT('Ctrl Pts',(2.00000000049539,1.70833333361935,-1.15470053866527));
#7119=CARTESIAN_POINT('Ctrl Pts',(2.00000000049539,1.65000000028603,-2.44929359890139E-16));
#7120=CARTESIAN_POINT('Ctrl Pts',(2.00000000049539,1.59166666695269,1.15470053866527));
#7121=CARTESIAN_POINT('Ctrl Pts',(1.0000000002477,1.53333333361936,1.7320508079979));
#7122=CARTESIAN_POINT('Ctrl Pts',(4.24230095595043E-16,1.47500000028602,
2.30940107733053));
#7123=CARTESIAN_POINT('Ctrl Pts',(-1.0000000002477,1.41666666695269,1.7320508079979));
#7124=CARTESIAN_POINT('Ctrl Pts',(-2.00000000049539,1.35833333361935,1.15470053866527));
#7125=CARTESIAN_POINT('Ctrl Pts',(-2.00000000049539,1.30000000028603,0.));
#7126=CARTESIAN_POINT('Ctrl Pts',(-2.00000000049539,1.2416666669527,-1.15470053866527));
#7127=CARTESIAN_POINT('Ctrl Pts',(-1.0000000002477,1.18333333361936,-1.7320508079979));
#7128=CARTESIAN_POINT('Ctrl Pts',(-1.41410031865014E-16,1.12500000028603,
-2.30940107733053));
#7129=CARTESIAN_POINT('Ctrl Pts',(1.0000000002477,1.06666666695269,-1.7320508079979));
#7130=CARTESIAN_POINT('Ctrl Pts',(2.00000000049539,1.00833333361936,-1.15470053866527));
#7131=CARTESIAN_POINT('Ctrl Pts',(2.00000000049539,0.950000000286022,-2.44929359890139E-16));
#7132=CARTESIAN_POINT('Ctrl Pts',(2.00000000049539,0.891666666952695,1.15470053866527));
#7133=CARTESIAN_POINT('Ctrl Pts',(1.0000000002477,0.833333333619354,1.7320508079979));
#7134=CARTESIAN_POINT('Ctrl Pts',(4.24230095595043E-16,0.775000000286027,
2.30940107733053));
#7135=CARTESIAN_POINT('Ctrl Pts',(-1.0000000002477,0.716666666952686,1.7320508079979));
#7136=CARTESIAN_POINT('Ctrl Pts',(-2.00000000049539,0.65833333361936,1.15470053866527));
#7137=CARTESIAN_POINT('Ctrl Pts',(-2.00000000049539,0.600000000286019,0.));
#7138=CARTESIAN_POINT('Ctrl Pts',(-2.00000000049539,0.541666666952692,-1.15470053866527));
#7139=CARTESIAN_POINT('Ctrl Pts',(-1.0000000002477,0.483333333619351,-1.7320508079979));
#7140=CARTESIAN_POINT('Ctrl Pts',(-1.41410031865014E-16,0.425000000286024,
-2.30940107733053));
#7141=CARTESIAN_POINT('Ctrl Pts',(1.0000000002477,0.366666666952697,-1.7320508079979));
#7142=CARTESIAN_POINT('Ctrl Pts',(2.00000000049539,0.308333333619356,-1.15470053866527));
#7143=CARTESIAN_POINT('Ctrl Pts',(2.00000000049539,0.250000000286029,-2.44929359890139E-16));
#7144=CARTESIAN_POINT('Ctrl Pts',(2.00000000049539,0.191666666952689,1.15470053866527));
#7145=CARTESIAN_POINT('Ctrl Pts',(1.0000000002477,0.133333333619362,1.7320508079979));
#7146=CARTESIAN_POINT('Ctrl Pts',(4.24230095595043E-16,0.075000000286021,
2.30940107733053));
#7147=CARTESIAN_POINT('Ctrl Pts',(-1.0000000002477,0.0166666669526941,1.7320508079979));
#7148=CARTESIAN_POINT('Ctrl Pts',(-2.00000000049539,-0.0416666663806467,
1.15470053866527));
#7149=CARTESIAN_POINT('Ctrl Pts',(-2.00000000049539,-0.0999999997139736,
0.));
#7150=CARTESIAN_POINT('Ctrl Pts',(-2.00000000049539,-0.158333333047314,
-1.15470053866527));
#7151=CARTESIAN_POINT('Ctrl Pts',(-1.0000000002477,-0.216666666380641,-1.7320508079979));
#7152=CARTESIAN_POINT('Ctrl Pts',(-1.41410031865014E-16,-0.274999999713982,
-2.30940107733053));
#7153=CARTESIAN_POINT('Ctrl Pts',(1.0000000002477,-0.333333333047309,-1.7320508079979));
#7154=CARTESIAN_POINT('Ctrl Pts',(2.00000000049539,-0.391666666380636,-1.15470053866527));
#7155=CARTESIAN_POINT('Ctrl Pts',(2.00000000049539,-0.449999999713977,-2.44929359890139E-16));
#7156=CARTESIAN_POINT('Ctrl Pts',(2.00000000049539,-0.508333333047304,1.15470053866527));
#7157=CARTESIAN_POINT('Ctrl Pts',(1.0000000002477,-0.566666666380644,1.7320508079979));
#7158=CARTESIAN_POINT('Ctrl Pts',(4.24230095595043E-16,-0.624999999713971,
2.30940107733053));
#7159=CARTESIAN_POINT('Ctrl Pts',(-1.0000000002477,-0.683333333047312,1.7320508079979));
#7160=CARTESIAN_POINT('Ctrl Pts',(-2.00000000049539,-0.741666666380639,
1.15470053866527));
#7161=CARTESIAN_POINT('Ctrl Pts',(-2.00000000049539,-0.79999999971398,0.));
#7162=CARTESIAN_POINT('Ctrl Pts',(-2.00000000049539,-0.858333333047307,
-1.15470053866527));
#7163=CARTESIAN_POINT('Ctrl Pts',(-1.0000000002477,-0.916666666380648,-1.7320508079979));
#7164=CARTESIAN_POINT('Ctrl Pts',(-1.41410031865014E-16,-0.974999999713974,
-2.30940107733053));
#7165=CARTESIAN_POINT('Ctrl Pts',(1.0000000002477,-1.03333333304732,-1.7320508079979));
#7166=CARTESIAN_POINT('Ctrl Pts',(2.00000000049539,-1.09166666638064,-1.15470053866527));
#7167=CARTESIAN_POINT('Ctrl Pts',(2.00000000049539,-1.14999999971397,-2.44929359890139E-16));
#7168=CARTESIAN_POINT('Ctrl Pts',(2.00000000049539,-1.20833333304731,1.15470053866527));
#7169=CARTESIAN_POINT('Ctrl Pts',(1.0000000002477,-1.26666666638064,1.7320508079979));
#7170=CARTESIAN_POINT('Ctrl Pts',(4.24230095595043E-16,-1.32499999971398,
2.30940107733053));
#7171=CARTESIAN_POINT('Ctrl Pts',(-1.0000000002477,-1.3833333330473,1.7320508079979));
#7172=CARTESIAN_POINT('Ctrl Pts',(-2.00000000049539,-1.44166666638065,1.15470053866527));
#7173=CARTESIAN_POINT('Ctrl Pts',(-2.00000000049539,-1.49999999971397,0.));
#7174=CARTESIAN_POINT('Ctrl Pts',(-2.00000000049539,-1.55833333304731,-1.15470053866527));
#7175=CARTESIAN_POINT('Ctrl Pts',(-1.0000000002477,-1.61666666638064,-1.7320508079979));
#7176=CARTESIAN_POINT('Ctrl Pts',(-1.41410031865014E-16,-1.67499999971398,
-2.30940107733053));
#7177=CARTESIAN_POINT('Ctrl Pts',(1.0000000002477,-1.73333333304731,-1.7320508079979));
#7178=CARTESIAN_POINT('Ctrl Pts',(2.00000000049539,-1.79166666638065,-1.15470053866527));
#7179=CARTESIAN_POINT('Ctrl Pts',(2.00000000049539,-1.84999999971398,-2.44929359890139E-16));
#7180=CARTESIAN_POINT('Ctrl Pts',(2.00000000049539,-1.9083333330473,1.15470053866527));
#7181=CARTESIAN_POINT('Ctrl Pts',(1.0000000002477,-1.96666666638064,1.7320508079979));
#7182=CARTESIAN_POINT('Ctrl Pts',(0.738898696525379,-1.98189757576067,1.88279771598774));
#7183=CARTESIAN_POINT('Ctrl Pts',(0.444961184151523,-1.9990439306449,1.94987423865747));
#7184=CARTESIAN_POINT('Ctrl Pts',(-1.52006374725761,9.52000000000001,0.563397231550268));
#7185=CARTESIAN_POINT('Ctrl Pts',(-1.58927882503764,9.52000000000001,0.429537689746389));
#7186=CARTESIAN_POINT('Ctrl Pts',(-1.63814900638563,9.52000000000001,0.288940715437786));
#7187=CARTESIAN_POINT('Ctrl Pts',(-1.69591065797373,9.52000000000001,-0.00549261577426306));
#7188=CARTESIAN_POINT('Ctrl Pts',(-1.70375959008733,9.52000000000001,-0.15553028221414));
#7189=CARTESIAN_POINT('Ctrl Pts',(-1.68351521825398,9.52000000000001,-0.453449224894565));
#7190=CARTESIAN_POINT('Ctrl Pts',(-1.65426345691986,9.52,-0.602019915388218));
#7191=CARTESIAN_POINT('Ctrl Pts',(-1.56087360396711,9.52,-0.884017448979234));
#7192=CARTESIAN_POINT('Ctrl Pts',(-1.49537671531736,9.52000000000001,-1.02113231381166));
#7193=CARTESIAN_POINT('Ctrl Pts',(-1.3343529445858,9.52000000000001,-1.27139381246717));
#7194=CARTESIAN_POINT('Ctrl Pts',(-1.23864034261375,9.52000000000001,-1.3859272903417));
#7195=CARTESIAN_POINT('Ctrl Pts',(-1.01839953499697,9.52000000000001,-1.59036808297552));
#7196=CARTESIAN_POINT('Ctrl Pts',(-0.897345930978197,9.52000000000001,-1.67656690067514));
#7197=CARTESIAN_POINT('Ctrl Pts',(-0.636953702877006,9.52000000000001,-1.82216955557148));
#7198=CARTESIAN_POINT('Ctrl Pts',(-0.497563221603356,9.52000000000001,-1.88052046250904));
#7199=CARTESIAN_POINT('Ctrl Pts',(-0.212605147610961,9.52000000000001,-1.96369393371656));
#7200=CARTESIAN_POINT('Ctrl Pts',(-0.0644024157051228,9.52000000000001,
-1.98948599115583));
#7201=CARTESIAN_POINT('Ctrl Pts',(0.0859174328513603,9.52000000000001,-1.99815344810835));
#7202=CARTESIAN_POINT('Ctrl Pts',(1.6211138875,0.731250000955919,-1.9852919333802E-16));
#7203=CARTESIAN_POINT('Ctrl Pts',(1.6211138875,0.672916667622592,0.935950539335165));
#7204=CARTESIAN_POINT('Ctrl Pts',(0.810556943750001,0.614583334289251,1.40392580900275));
#7205=CARTESIAN_POINT('Ctrl Pts',(3.43862649647115E-16,0.556250000955924,
1.87190107867033));
#7206=CARTESIAN_POINT('Ctrl Pts',(-0.810556943749999,0.497916667622583,
1.40392580900275));
#7207=CARTESIAN_POINT('Ctrl Pts',(-1.6211138875,0.439583334289256,0.935950539335167));
#7208=CARTESIAN_POINT('Ctrl Pts',(-1.6211138875,0.381250000955916,0.));
#7209=CARTESIAN_POINT('Ctrl Pts',(-1.6211138875,0.322916667622589,-0.935950539335166));
#7210=CARTESIAN_POINT('Ctrl Pts',(-0.81055694375,0.264583334289248,-1.40392580900275));
#7211=CARTESIAN_POINT('Ctrl Pts',(-1.14620883215705E-16,0.206250000955921,
-1.87190107867033));
#7212=CARTESIAN_POINT('Ctrl Pts',(0.81055694375,0.147916667622594,-1.40392580900275));
#7213=CARTESIAN_POINT('Ctrl Pts',(1.37954992065153,0.106967962856252,-1.07541756062164));
#7214=CARTESIAN_POINT('Ctrl Pts',(1.55927926836488,0.0611138874999995,-0.443461835441161));
#7215=CARTESIAN_POINT('Origin',(-2.77555756156289E-16,71.6937500009559,
-2.08166817117217E-16));
#7216=CARTESIAN_POINT('Ctrl Pts',(1.6211138875,0.556250000955924,-1.9852919333802E-16));
#7217=CARTESIAN_POINT('Ctrl Pts',(1.6211138875,0.497916667622597,0.935950539335165));
#7218=CARTESIAN_POINT('Ctrl Pts',(0.810556943750001,0.439583334289256,1.40392580900275));
#7219=CARTESIAN_POINT('Ctrl Pts',(3.43862649647115E-16,0.381250000955929,
1.87190107867033));
#7220=CARTESIAN_POINT('Ctrl Pts',(-0.810556943749999,0.322916667622589,
1.40392580900275));
#7221=CARTESIAN_POINT('Ctrl Pts',(-1.6211138875,0.264583334289262,0.935950539335167));
#7222=CARTESIAN_POINT('Ctrl Pts',(-1.6211138875,0.206250000955921,0.));
#7223=CARTESIAN_POINT('Ctrl Pts',(-1.6211138875,0.147916667622594,-0.935950539335166));
#7224=CARTESIAN_POINT('Ctrl Pts',(-0.81055694375,0.0895833342892532,-1.40392580900275));
#7225=CARTESIAN_POINT('Ctrl Pts',(-0.623625223172666,0.0761304233604275,
-1.51185088819815));
#7226=CARTESIAN_POINT('Ctrl Pts',(-0.414966524668622,0.0611138874999821,
-1.56710338511853));
#7227=CARTESIAN_POINT('Ctrl Pts',(-2.00612458230317,71.3839639726704,0.));
#7228=CARTESIAN_POINT('Ctrl Pts',(-2.00612458230317,71.3256306393371,-1.15823656762066));
#7229=CARTESIAN_POINT('Ctrl Pts',(-1.00306229115158,71.2672973060038,-1.73735485143099));
#7230=CARTESIAN_POINT('Ctrl Pts',(-1.41843070519206E-16,71.2089639726704,
-2.31647313524132));
#7231=CARTESIAN_POINT('Ctrl Pts',(1.00306229115158,71.1506306393371,-1.73735485143099));
#7232=CARTESIAN_POINT('Ctrl Pts',(2.00612458230317,71.0922973060038,-1.15823656762066));
#7233=CARTESIAN_POINT('Ctrl Pts',(2.00612458230317,71.0339639726704,-2.45679404840839E-16));
#7234=CARTESIAN_POINT('Ctrl Pts',(2.00612458230317,70.9756306393371,1.15823656762066));
#7235=CARTESIAN_POINT('Ctrl Pts',(1.00306229115158,70.9172973060038,1.73735485143099));
#7236=CARTESIAN_POINT('Ctrl Pts',(4.25529211557617E-16,70.8589639726704,
2.31647313524132));
#7237=CARTESIAN_POINT('Ctrl Pts',(-1.00306229115158,70.8006306393371,1.73735485143099));
#7238=CARTESIAN_POINT('Ctrl Pts',(-2.00612458230316,70.7422973060038,1.15823656762066));
#7239=CARTESIAN_POINT('Ctrl Pts',(-2.00612458230317,70.6839639726704,0.));
#7240=CARTESIAN_POINT('Ctrl Pts',(-2.00612458230317,70.6256306393371,-1.15823656762066));
#7241=CARTESIAN_POINT('Ctrl Pts',(-1.00306229115158,70.5672973060038,-1.73735485143099));
#7242=CARTESIAN_POINT('Ctrl Pts',(-1.41843070519206E-16,70.5089639726704,
-2.31647313524132));
#7243=CARTESIAN_POINT('Ctrl Pts',(1.00306229115158,70.4506306393371,-1.73735485143099));
#7244=CARTESIAN_POINT('Ctrl Pts',(2.00612458230317,70.3922973060038,-1.15823656762066));
#7245=CARTESIAN_POINT('Ctrl Pts',(2.00612458230317,70.3339639726704,-2.45679404840839E-16));
#7246=CARTESIAN_POINT('Ctrl Pts',(2.00612458230317,70.2756306393371,1.15823656762066));
#7247=CARTESIAN_POINT('Ctrl Pts',(1.00306229115158,70.2172973060038,1.73735485143099));
#7248=CARTESIAN_POINT('Ctrl Pts',(4.25529211557617E-16,70.1589639726704,
2.31647313524132));
#7249=CARTESIAN_POINT('Ctrl Pts',(-1.00306229115158,70.1006306393371,1.73735485143099));
#7250=CARTESIAN_POINT('Ctrl Pts',(-2.00612458230316,70.0422973060037,1.15823656762066));
#7251=CARTESIAN_POINT('Ctrl Pts',(-2.00612458230317,69.9839639726704,0.));
#7252=CARTESIAN_POINT('Ctrl Pts',(-2.00612458230317,69.9256306393371,-1.15823656762066));
#7253=CARTESIAN_POINT('Ctrl Pts',(-1.00306229115158,69.8672973060038,-1.73735485143099));
#7254=CARTESIAN_POINT('Ctrl Pts',(-1.41843070519206E-16,69.8089639726704,
-2.31647313524132));
#7255=CARTESIAN_POINT('Ctrl Pts',(1.00306229115158,69.7506306393371,-1.73735485143099));
#7256=CARTESIAN_POINT('Ctrl Pts',(2.00612458230317,69.6922973060038,-1.15823656762066));
#7257=CARTESIAN_POINT('Ctrl Pts',(2.00612458230317,69.6339639726704,-2.45679404840839E-16));
#7258=CARTESIAN_POINT('Ctrl Pts',(2.00612458230317,69.5756306393371,1.15823656762066));
#7259=CARTESIAN_POINT('Ctrl Pts',(1.00306229115158,69.5172973060038,1.73735485143099));
#7260=CARTESIAN_POINT('Ctrl Pts',(4.25529211557617E-16,69.4589639726704,
2.31647313524132));
#7261=CARTESIAN_POINT('Ctrl Pts',(-1.00306229115158,69.4006306393371,1.73735485143099));
#7262=CARTESIAN_POINT('Ctrl Pts',(-2.00612458230316,69.3422973060038,1.15823656762066));
#7263=CARTESIAN_POINT('Ctrl Pts',(-2.00612458230317,69.2839639726704,0.));
#7264=CARTESIAN_POINT('Ctrl Pts',(-2.00612458230317,69.2256306393371,-1.15823656762066));
#7265=CARTESIAN_POINT('Ctrl Pts',(-1.00306229115158,69.1672973060038,-1.73735485143099));
#7266=CARTESIAN_POINT('Ctrl Pts',(-1.41843070519206E-16,69.1089639726704,
-2.31647313524132));
#7267=CARTESIAN_POINT('Ctrl Pts',(1.00306229115158,69.0506306393371,-1.73735485143099));
#7268=CARTESIAN_POINT('Ctrl Pts',(2.00612458230317,68.9922973060038,-1.15823656762066));
#7269=CARTESIAN_POINT('Ctrl Pts',(2.00612458230317,68.9339639726704,-2.45679404840839E-16));
#7270=CARTESIAN_POINT('Ctrl Pts',(2.00612458230317,68.8756306393371,1.15823656762066));
#7271=CARTESIAN_POINT('Ctrl Pts',(1.00306229115158,68.8172973060038,1.73735485143099));
#7272=CARTESIAN_POINT('Ctrl Pts',(4.25529211557617E-16,68.7589639726704,
2.31647313524132));
#7273=CARTESIAN_POINT('Ctrl Pts',(-1.00306229115158,68.7006306393371,1.73735485143099));
#7274=CARTESIAN_POINT('Ctrl Pts',(-2.00612458230316,68.6422973060037,1.15823656762066));
#7275=CARTESIAN_POINT('Ctrl Pts',(-2.00612458230317,68.5839639726704,0.));
#7276=CARTESIAN_POINT('Ctrl Pts',(-2.00612458230317,68.5256306393371,-1.15823656762066));
#7277=CARTESIAN_POINT('Ctrl Pts',(-1.00306229115158,68.4672973060038,-1.73735485143099));
#7278=CARTESIAN_POINT('Ctrl Pts',(-1.41843070519206E-16,68.4089639726704,
-2.31647313524132));
#7279=CARTESIAN_POINT('Ctrl Pts',(1.00306229115158,68.3506306393371,-1.73735485143099));
#7280=CARTESIAN_POINT('Ctrl Pts',(2.00612458230317,68.2922973060038,-1.15823656762066));
#7281=CARTESIAN_POINT('Ctrl Pts',(2.00612458230317,68.2339639726704,-2.45679404840839E-16));
#7282=CARTESIAN_POINT('Ctrl Pts',(2.00612458230317,68.1756306393371,1.15823656762066));
#7283=CARTESIAN_POINT('Ctrl Pts',(1.00306229115158,68.1172973060038,1.73735485143099));
#7284=CARTESIAN_POINT('Ctrl Pts',(4.25529211557617E-16,68.0589639726704,
2.31647313524132));
#7285=CARTESIAN_POINT('Ctrl Pts',(-1.00306229115158,68.0006306393371,1.73735485143099));
#7286=CARTESIAN_POINT('Ctrl Pts',(-2.00612458230316,67.9422973060038,1.15823656762066));
#7287=CARTESIAN_POINT('Ctrl Pts',(-2.00612458230317,67.8839639726704,0.));
#7288=CARTESIAN_POINT('Ctrl Pts',(-2.00612458230317,67.8256306393371,-1.15823656762066));
#7289=CARTESIAN_POINT('Ctrl Pts',(-1.00306229115158,67.7672973060038,-1.73735485143099));
#7290=CARTESIAN_POINT('Ctrl Pts',(-1.41843070519206E-16,67.7089639726704,
-2.31647313524132));
#7291=CARTESIAN_POINT('Ctrl Pts',(1.00306229115158,67.6506306393371,-1.73735485143099));
#7292=CARTESIAN_POINT('Ctrl Pts',(2.00612458230317,67.5922973060038,-1.15823656762066));
#7293=CARTESIAN_POINT('Ctrl Pts',(2.00612458230317,67.5339639726704,-2.45679404840839E-16));
#7294=CARTESIAN_POINT('Ctrl Pts',(2.00612458230317,67.4756306393371,1.15823656762066));
#7295=CARTESIAN_POINT('Ctrl Pts',(1.00306229115158,67.4172973060038,1.73735485143099));
#7296=CARTESIAN_POINT('Ctrl Pts',(4.25529211557617E-16,67.3589639726704,
2.31647313524132));
#7297=CARTESIAN_POINT('Ctrl Pts',(-1.00306229115158,67.3006306393371,1.73735485143099));
#7298=CARTESIAN_POINT('Ctrl Pts',(-2.00612458230316,67.2422973060038,1.15823656762066));
#7299=CARTESIAN_POINT('Ctrl Pts',(-2.00612458230317,67.1839639726704,0.));
#7300=CARTESIAN_POINT('Ctrl Pts',(-2.00612458230317,67.1256306393371,-1.15823656762066));
#7301=CARTESIAN_POINT('Ctrl Pts',(-1.00306229115158,67.0672973060038,-1.73735485143099));
#7302=CARTESIAN_POINT('Ctrl Pts',(-1.41843070519206E-16,67.0089639726704,
-2.31647313524132));
#7303=CARTESIAN_POINT('Ctrl Pts',(1.00306229115158,66.9506306393371,-1.73735485143099));
#7304=CARTESIAN_POINT('Ctrl Pts',(2.00612458230317,66.8922973060038,-1.15823656762066));
#7305=CARTESIAN_POINT('Ctrl Pts',(2.00612458230317,66.8339639726704,-2.45679404840839E-16));
#7306=CARTESIAN_POINT('Ctrl Pts',(2.00612458230317,66.7756306393371,1.15823656762066));
#7307=CARTESIAN_POINT('Ctrl Pts',(1.00306229115158,66.7172973060038,1.73735485143099));
#7308=CARTESIAN_POINT('Ctrl Pts',(4.25529211557617E-16,66.6589639726704,
2.31647313524132));
#7309=CARTESIAN_POINT('Ctrl Pts',(-1.00306229115158,66.6006306393371,1.73735485143099));
#7310=CARTESIAN_POINT('Ctrl Pts',(-2.00612458230316,66.5422973060038,1.15823656762066));
#7311=CARTESIAN_POINT('Ctrl Pts',(-2.00612458230317,66.4839639726704,0.));
#7312=CARTESIAN_POINT('Ctrl Pts',(-2.00612458230317,66.4256306393371,-1.15823656762066));
#7313=CARTESIAN_POINT('Ctrl Pts',(-1.00306229115158,66.3672973060038,-1.73735485143099));
#7314=CARTESIAN_POINT('Ctrl Pts',(-1.41843070519206E-16,66.3089639726704,
-2.31647313524132));
#7315=CARTESIAN_POINT('Ctrl Pts',(1.00306229115158,66.2506306393371,-1.73735485143099));
#7316=CARTESIAN_POINT('Ctrl Pts',(2.00612458230317,66.1922973060038,-1.15823656762066));
#7317=CARTESIAN_POINT('Ctrl Pts',(2.00612458230317,66.1339639726704,-2.45679404840839E-16));
#7318=CARTESIAN_POINT('Ctrl Pts',(2.00612458230317,66.0756306393371,1.15823656762066));
#7319=CARTESIAN_POINT('Ctrl Pts',(1.00306229115158,66.0172973060038,1.73735485143099));
#7320=CARTESIAN_POINT('Ctrl Pts',(4.25529211557617E-16,65.9589639726704,
2.31647313524132));
#7321=CARTESIAN_POINT('Ctrl Pts',(-1.00306229115158,65.9006306393371,1.73735485143099));
#7322=CARTESIAN_POINT('Ctrl Pts',(-2.00612458230316,65.8422973060038,1.15823656762066));
#7323=CARTESIAN_POINT('Ctrl Pts',(-2.00612458230317,65.7839639726704,0.));
#7324=CARTESIAN_POINT('Ctrl Pts',(-2.00612458230317,65.7256306393371,-1.15823656762066));
#7325=CARTESIAN_POINT('Ctrl Pts',(-1.00306229115158,65.6672973060038,-1.73735485143099));
#7326=CARTESIAN_POINT('Ctrl Pts',(-1.41843070519206E-16,65.6089639726704,
-2.31647313524132));
#7327=CARTESIAN_POINT('Ctrl Pts',(1.00306229115158,65.5506306393371,-1.73735485143099));
#7328=CARTESIAN_POINT('Ctrl Pts',(2.00612458230317,65.4922973060037,-1.15823656762066));
#7329=CARTESIAN_POINT('Ctrl Pts',(2.00612458230317,65.4339639726704,-2.45679404840839E-16));
#7330=CARTESIAN_POINT('Ctrl Pts',(2.00612458230317,65.3756306393371,1.15823656762066));
#7331=CARTESIAN_POINT('Ctrl Pts',(1.00306229115158,65.3172973060038,1.73735485143099));
#7332=CARTESIAN_POINT('Ctrl Pts',(4.25529211557617E-16,65.2589639726704,
2.31647313524132));
#7333=CARTESIAN_POINT('Ctrl Pts',(-1.00306229115158,65.2006306393371,1.73735485143099));
#7334=CARTESIAN_POINT('Ctrl Pts',(-2.00612458230316,65.1422973060038,1.15823656762066));
#7335=CARTESIAN_POINT('Ctrl Pts',(-2.00612458230317,65.0839639726704,0.));
#7336=CARTESIAN_POINT('Ctrl Pts',(-2.00612458230317,65.0256306393371,-1.15823656762066));
#7337=CARTESIAN_POINT('Ctrl Pts',(-1.00306229115158,64.9672973060038,-1.73735485143099));
#7338=CARTESIAN_POINT('Ctrl Pts',(-1.41843070519206E-16,64.9089639726704,
-2.31647313524132));
#7339=CARTESIAN_POINT('Ctrl Pts',(1.00306229115158,64.8506306393371,-1.73735485143099));
#7340=CARTESIAN_POINT('Ctrl Pts',(2.00612458230317,64.7922973060038,-1.15823656762066));
#7341=CARTESIAN_POINT('Ctrl Pts',(2.00612458230317,64.7339639726704,-2.45679404840839E-16));
#7342=CARTESIAN_POINT('Ctrl Pts',(2.00612458230317,64.6756306393371,1.15823656762066));
#7343=CARTESIAN_POINT('Ctrl Pts',(1.00306229115158,64.6172973060038,1.73735485143099));
#7344=CARTESIAN_POINT('Ctrl Pts',(4.25529211557617E-16,64.5589639726704,
2.31647313524132));
#7345=CARTESIAN_POINT('Ctrl Pts',(-1.00306229115158,64.5006306393371,1.73735485143099));
#7346=CARTESIAN_POINT('Ctrl Pts',(-2.00612458230316,64.4422973060038,1.15823656762066));
#7347=CARTESIAN_POINT('Ctrl Pts',(-2.00612458230317,64.3839639726704,0.));
#7348=CARTESIAN_POINT('Ctrl Pts',(-2.00612458230317,64.3256306393371,-1.15823656762066));
#7349=CARTESIAN_POINT('Ctrl Pts',(-1.00306229115158,64.2672973060038,-1.73735485143099));
#7350=CARTESIAN_POINT('Ctrl Pts',(-1.41843070519206E-16,64.2089639726704,
-2.31647313524132));
#7351=CARTESIAN_POINT('Ctrl Pts',(1.00306229115158,64.1506306393371,-1.73735485143099));
#7352=CARTESIAN_POINT('Ctrl Pts',(2.00612458230317,64.0922973060038,-1.15823656762066));
#7353=CARTESIAN_POINT('Ctrl Pts',(2.00612458230317,64.0339639726704,-2.45679404840839E-16));
#7354=CARTESIAN_POINT('Ctrl Pts',(2.00612458230317,63.9756306393371,1.15823656762066));
#7355=CARTESIAN_POINT('Ctrl Pts',(1.00306229115158,63.9172973060038,1.73735485143099));
#7356=CARTESIAN_POINT('Ctrl Pts',(4.25529211557617E-16,63.8589639726704,
2.31647313524132));
#7357=CARTESIAN_POINT('Ctrl Pts',(-1.00306229115158,63.8006306393371,1.73735485143099));
#7358=CARTESIAN_POINT('Ctrl Pts',(-2.00612458230316,63.7422973060038,1.15823656762066));
#7359=CARTESIAN_POINT('Ctrl Pts',(-2.00612458230317,63.6839639726704,0.));
#7360=CARTESIAN_POINT('Ctrl Pts',(-2.00612458230317,63.6256306393371,-1.15823656762066));
#7361=CARTESIAN_POINT('Ctrl Pts',(-1.00306229115158,63.5672973060038,-1.73735485143099));
#7362=CARTESIAN_POINT('Ctrl Pts',(-1.41843070519206E-16,63.5089639726704,
-2.31647313524132));
#7363=CARTESIAN_POINT('Ctrl Pts',(1.00306229115158,63.4506306393371,-1.73735485143099));
#7364=CARTESIAN_POINT('Ctrl Pts',(2.00612458230317,63.3922973060038,-1.15823656762066));
#7365=CARTESIAN_POINT('Ctrl Pts',(2.00612458230317,63.3339639726704,-2.45679404840839E-16));
#7366=CARTESIAN_POINT('Ctrl Pts',(2.00612458230317,63.2756306393371,1.15823656762066));
#7367=CARTESIAN_POINT('Ctrl Pts',(1.00306229115158,63.2172973060038,1.73735485143099));
#7368=CARTESIAN_POINT('Ctrl Pts',(4.25529211557617E-16,63.1589639726704,
2.31647313524132));
#7369=CARTESIAN_POINT('Ctrl Pts',(-1.00306229115158,63.1006306393371,1.73735485143099));
#7370=CARTESIAN_POINT('Ctrl Pts',(-2.00612458230316,63.0422973060038,1.15823656762066));
#7371=CARTESIAN_POINT('Ctrl Pts',(-2.00612458230317,62.9839639726704,0.));
#7372=CARTESIAN_POINT('Ctrl Pts',(-2.00612458230317,62.9256306393371,-1.15823656762066));
#7373=CARTESIAN_POINT('Ctrl Pts',(-1.00306229115158,62.8672973060038,-1.73735485143099));
#7374=CARTESIAN_POINT('Ctrl Pts',(-1.41843070519206E-16,62.8089639726704,
-2.31647313524132));
#7375=CARTESIAN_POINT('Ctrl Pts',(1.00306229115158,62.7506306393371,-1.73735485143099));
#7376=CARTESIAN_POINT('Ctrl Pts',(2.00612458230317,62.6922973060038,-1.15823656762066));
#7377=CARTESIAN_POINT('Ctrl Pts',(2.00612458230317,62.6339639726704,-2.45679404840839E-16));
#7378=CARTESIAN_POINT('Ctrl Pts',(2.00612458230317,62.5756306393371,1.15823656762066));
#7379=CARTESIAN_POINT('Ctrl Pts',(1.00306229115158,62.5172973060038,1.73735485143099));
#7380=CARTESIAN_POINT('Ctrl Pts',(4.25529211557617E-16,62.4589639726704,
2.31647313524132));
#7381=CARTESIAN_POINT('Ctrl Pts',(-1.00306229115158,62.4006306393371,1.73735485143099));
#7382=CARTESIAN_POINT('Ctrl Pts',(-2.00612458230316,62.3422973060038,1.15823656762066));
#7383=CARTESIAN_POINT('Ctrl Pts',(-2.00612458230317,62.2839639726704,0.));
#7384=CARTESIAN_POINT('Ctrl Pts',(-2.00612458230317,62.2256306393371,-1.15823656762066));
#7385=CARTESIAN_POINT('Ctrl Pts',(-1.00306229115158,62.1672973060038,-1.73735485143099));
#7386=CARTESIAN_POINT('Ctrl Pts',(-1.41843070519206E-16,62.1089639726704,
-2.31647313524132));
#7387=CARTESIAN_POINT('Ctrl Pts',(1.00306229115158,62.0506306393371,-1.73735485143099));
#7388=CARTESIAN_POINT('Ctrl Pts',(2.00612458230317,61.9922973060038,-1.15823656762066));
#7389=CARTESIAN_POINT('Ctrl Pts',(2.00612458230317,61.9339639726704,-2.45679404840839E-16));
#7390=CARTESIAN_POINT('Ctrl Pts',(2.00612458230317,61.8756306393371,1.15823656762066));
#7391=CARTESIAN_POINT('Ctrl Pts',(1.00306229115158,61.8172973060038,1.73735485143099));
#7392=CARTESIAN_POINT('Ctrl Pts',(4.25529211557617E-16,61.7589639726704,
2.31647313524132));
#7393=CARTESIAN_POINT('Ctrl Pts',(-1.00306229115158,61.7006306393371,1.73735485143099));
#7394=CARTESIAN_POINT('Ctrl Pts',(-2.00612458230316,61.6422973060038,1.15823656762066));
#7395=CARTESIAN_POINT('Ctrl Pts',(-2.00612458230317,61.5839639726704,0.));
#7396=CARTESIAN_POINT('Ctrl Pts',(-2.00612458230317,61.5256306393371,-1.15823656762066));
#7397=CARTESIAN_POINT('Ctrl Pts',(-1.00306229115158,61.4672973060038,-1.73735485143099));
#7398=CARTESIAN_POINT('Ctrl Pts',(-1.41843070519206E-16,61.4089639726704,
-2.31647313524132));
#7399=CARTESIAN_POINT('Ctrl Pts',(1.00306229115158,61.3506306393371,-1.73735485143099));
#7400=CARTESIAN_POINT('Ctrl Pts',(2.00612458230317,61.2922973060038,-1.15823656762066));
#7401=CARTESIAN_POINT('Ctrl Pts',(2.00612458230317,61.2339639726704,-2.45679404840839E-16));
#7402=CARTESIAN_POINT('Ctrl Pts',(2.00612458230317,61.1756306393371,1.15823656762066));
#7403=CARTESIAN_POINT('Ctrl Pts',(1.00306229115158,61.1172973060038,1.73735485143099));
#7404=CARTESIAN_POINT('Ctrl Pts',(4.25529211557617E-16,61.0589639726704,
2.31647313524132));
#7405=CARTESIAN_POINT('Ctrl Pts',(-1.00306229115158,61.0006306393371,1.73735485143099));
#7406=CARTESIAN_POINT('Ctrl Pts',(-2.00612458230316,60.9422973060038,1.15823656762066));
#7407=CARTESIAN_POINT('Ctrl Pts',(-2.00612458230317,60.8839639726704,0.));
#7408=CARTESIAN_POINT('Ctrl Pts',(-2.00612458230317,60.8256306393371,-1.15823656762066));
#7409=CARTESIAN_POINT('Ctrl Pts',(-1.00306229115158,60.7672973060038,-1.73735485143099));
#7410=CARTESIAN_POINT('Ctrl Pts',(-1.41843070519206E-16,60.7089639726704,
-2.31647313524132));
#7411=CARTESIAN_POINT('Ctrl Pts',(1.00306229115158,60.6506306393371,-1.73735485143099));
#7412=CARTESIAN_POINT('Ctrl Pts',(2.00612458230317,60.5922973060038,-1.15823656762066));
#7413=CARTESIAN_POINT('Ctrl Pts',(2.00612458230317,60.5339639726704,-2.45679404840839E-16));
#7414=CARTESIAN_POINT('Ctrl Pts',(2.00612458230317,60.4756306393371,1.15823656762066));
#7415=CARTESIAN_POINT('Ctrl Pts',(1.00306229115158,60.4172973060038,1.73735485143099));
#7416=CARTESIAN_POINT('Ctrl Pts',(4.25529211557617E-16,60.3589639726704,
2.31647313524132));
#7417=CARTESIAN_POINT('Ctrl Pts',(-1.00306229115158,60.3006306393371,1.73735485143099));
#7418=CARTESIAN_POINT('Ctrl Pts',(-2.00612458230316,60.2422973060038,1.15823656762066));
#7419=CARTESIAN_POINT('Ctrl Pts',(-2.00612458230317,60.1839639726704,0.));
#7420=CARTESIAN_POINT('Ctrl Pts',(-2.00612458230317,60.1256306393371,-1.15823656762066));
#7421=CARTESIAN_POINT('Ctrl Pts',(-1.00306229115158,60.0672973060038,-1.73735485143099));
#7422=CARTESIAN_POINT('Ctrl Pts',(-1.41843070519206E-16,60.0089639726704,
-2.31647313524132));
#7423=CARTESIAN_POINT('Ctrl Pts',(1.00306229115158,59.9506306393371,-1.73735485143099));
#7424=CARTESIAN_POINT('Ctrl Pts',(2.00612458230317,59.8922973060038,-1.15823656762066));
#7425=CARTESIAN_POINT('Ctrl Pts',(2.00612458230317,59.8339639726704,-2.45679404840839E-16));
#7426=CARTESIAN_POINT('Ctrl Pts',(2.00612458230317,59.7756306393371,1.15823656762066));
#7427=CARTESIAN_POINT('Ctrl Pts',(1.00306229115158,59.7172973060038,1.73735485143099));
#7428=CARTESIAN_POINT('Ctrl Pts',(4.25529211557617E-16,59.6589639726704,
2.31647313524132));
#7429=CARTESIAN_POINT('Ctrl Pts',(-1.00306229115158,59.6006306393371,1.73735485143099));
#7430=CARTESIAN_POINT('Ctrl Pts',(-2.00612458230316,59.5422973060038,1.15823656762066));
#7431=CARTESIAN_POINT('Ctrl Pts',(-2.00612458230317,59.4839639726704,0.));
#7432=CARTESIAN_POINT('Ctrl Pts',(-2.00612458230317,59.4256306393371,-1.15823656762066));
#7433=CARTESIAN_POINT('Ctrl Pts',(-1.00306229115158,59.3672973060038,-1.73735485143099));
#7434=CARTESIAN_POINT('Ctrl Pts',(-1.41843070519206E-16,59.3089639726704,
-2.31647313524132));
#7435=CARTESIAN_POINT('Ctrl Pts',(1.00306229115158,59.2506306393371,-1.73735485143099));
#7436=CARTESIAN_POINT('Ctrl Pts',(2.00612458230317,59.1922973060038,-1.15823656762066));
#7437=CARTESIAN_POINT('Ctrl Pts',(2.00612458230317,59.1339639726704,-2.45679404840839E-16));
#7438=CARTESIAN_POINT('Ctrl Pts',(2.00612458230317,59.0756306393371,1.15823656762066));
#7439=CARTESIAN_POINT('Ctrl Pts',(1.00306229115158,59.0172973060038,1.73735485143099));
#7440=CARTESIAN_POINT('Ctrl Pts',(4.25529211557617E-16,58.9589639726704,
2.31647313524132));
#7441=CARTESIAN_POINT('Ctrl Pts',(-1.00306229115158,58.9006306393371,1.73735485143099));
#7442=CARTESIAN_POINT('Ctrl Pts',(-2.00612458230316,58.8422973060038,1.15823656762066));
#7443=CARTESIAN_POINT('Ctrl Pts',(-2.00612458230317,58.7839639726704,0.));
#7444=CARTESIAN_POINT('Ctrl Pts',(-2.00612458230317,58.7256306393371,-1.15823656762066));
#7445=CARTESIAN_POINT('Ctrl Pts',(-1.00306229115158,58.6672973060038,-1.73735485143099));
#7446=CARTESIAN_POINT('Ctrl Pts',(-1.41843070519206E-16,58.6089639726704,
-2.31647313524132));
#7447=CARTESIAN_POINT('Ctrl Pts',(1.00306229115158,58.5506306393371,-1.73735485143099));
#7448=CARTESIAN_POINT('Ctrl Pts',(2.00612458230317,58.4922973060038,-1.15823656762066));
#7449=CARTESIAN_POINT('Ctrl Pts',(2.00612458230317,58.4339639726704,-2.45679404840839E-16));
#7450=CARTESIAN_POINT('Ctrl Pts',(2.00612458230317,58.3756306393371,1.15823656762066));
#7451=CARTESIAN_POINT('Ctrl Pts',(1.00306229115158,58.3172973060038,1.73735485143099));
#7452=CARTESIAN_POINT('Ctrl Pts',(4.25529211557617E-16,58.2589639726704,
2.31647313524132));
#7453=CARTESIAN_POINT('Ctrl Pts',(-1.00306229115158,58.2006306393371,1.73735485143099));
#7454=CARTESIAN_POINT('Ctrl Pts',(-2.00612458230316,58.1422973060038,1.15823656762066));
#7455=CARTESIAN_POINT('Ctrl Pts',(-2.00612458230317,58.0839639726704,0.));
#7456=CARTESIAN_POINT('Ctrl Pts',(-2.00612458230317,58.0256306393371,-1.15823656762066));
#7457=CARTESIAN_POINT('Ctrl Pts',(-1.00306229115158,57.9672973060038,-1.73735485143099));
#7458=CARTESIAN_POINT('Ctrl Pts',(-1.41843070519206E-16,57.9089639726704,
-2.31647313524132));
#7459=CARTESIAN_POINT('Ctrl Pts',(1.00306229115158,57.8506306393371,-1.73735485143099));
#7460=CARTESIAN_POINT('Ctrl Pts',(2.00612458230317,57.7922973060038,-1.15823656762066));
#7461=CARTESIAN_POINT('Ctrl Pts',(2.00612458230317,57.7339639726704,-2.45679404840839E-16));
#7462=CARTESIAN_POINT('Ctrl Pts',(2.00612458230317,57.6756306393371,1.15823656762066));
#7463=CARTESIAN_POINT('Ctrl Pts',(1.00306229115158,57.6172973060038,1.73735485143099));
#7464=CARTESIAN_POINT('Ctrl Pts',(4.25529211557617E-16,57.5589639726704,
2.31647313524132));
#7465=CARTESIAN_POINT('Ctrl Pts',(-1.00306229115158,57.5006306393371,1.73735485143099));
#7466=CARTESIAN_POINT('Ctrl Pts',(-2.00612458230316,57.4422973060038,1.15823656762066));
#7467=CARTESIAN_POINT('Ctrl Pts',(-2.00612458230317,57.3839639726704,0.));
#7468=CARTESIAN_POINT('Ctrl Pts',(-2.00612458230317,57.3256306393371,-1.15823656762066));
#7469=CARTESIAN_POINT('Ctrl Pts',(-1.00306229115158,57.2672973060038,-1.73735485143099));
#7470=CARTESIAN_POINT('Ctrl Pts',(-1.41843070519206E-16,57.2089639726704,
-2.31647313524132));
#7471=CARTESIAN_POINT('Ctrl Pts',(1.00306229115158,57.1506306393371,-1.73735485143099));
#7472=CARTESIAN_POINT('Ctrl Pts',(2.00612458230317,57.0922973060038,-1.15823656762066));
#7473=CARTESIAN_POINT('Ctrl Pts',(2.00612458230317,57.0339639726704,-2.45679404840839E-16));
#7474=CARTESIAN_POINT('Ctrl Pts',(2.00612458230317,56.9756306393371,1.15823656762066));
#7475=CARTESIAN_POINT('Ctrl Pts',(1.00306229115158,56.9172973060038,1.73735485143099));
#7476=CARTESIAN_POINT('Ctrl Pts',(4.25529211557617E-16,56.8589639726704,
2.31647313524132));
#7477=CARTESIAN_POINT('Ctrl Pts',(-1.00306229115158,56.8006306393371,1.73735485143099));
#7478=CARTESIAN_POINT('Ctrl Pts',(-2.00612458230316,56.7422973060038,1.15823656762066));
#7479=CARTESIAN_POINT('Ctrl Pts',(-2.00612458230317,56.6839639726704,0.));
#7480=CARTESIAN_POINT('Ctrl Pts',(-2.00612458230317,56.6256306393371,-1.15823656762066));
#7481=CARTESIAN_POINT('Ctrl Pts',(-1.00306229115158,56.5672973060038,-1.73735485143099));
#7482=CARTESIAN_POINT('Ctrl Pts',(-1.41843070519206E-16,56.5089639726704,
-2.31647313524132));
#7483=CARTESIAN_POINT('Ctrl Pts',(1.00306229115158,56.4506306393371,-1.73735485143099));
#7484=CARTESIAN_POINT('Ctrl Pts',(2.00612458230317,56.3922973060038,-1.15823656762066));
#7485=CARTESIAN_POINT('Ctrl Pts',(2.00612458230317,56.3339639726704,-2.45679404840839E-16));
#7486=CARTESIAN_POINT('Ctrl Pts',(2.00612458230317,56.2756306393371,1.15823656762066));
#7487=CARTESIAN_POINT('Ctrl Pts',(1.00306229115158,56.2172973060038,1.73735485143099));
#7488=CARTESIAN_POINT('Ctrl Pts',(4.25529211557617E-16,56.1589639726704,
2.31647313524132));
#7489=CARTESIAN_POINT('Ctrl Pts',(-1.00306229115158,56.1006306393371,1.73735485143099));
#7490=CARTESIAN_POINT('Ctrl Pts',(-2.00612458230316,56.0422973060038,1.15823656762066));
#7491=CARTESIAN_POINT('Ctrl Pts',(-2.00612458230317,55.9839639726704,0.));
#7492=CARTESIAN_POINT('Ctrl Pts',(-2.00612458230317,55.9256306393371,-1.15823656762066));
#7493=CARTESIAN_POINT('Ctrl Pts',(-1.00306229115158,55.8672973060038,-1.73735485143099));
#7494=CARTESIAN_POINT('Ctrl Pts',(-1.41843070519206E-16,55.8089639726704,
-2.31647313524132));
#7495=CARTESIAN_POINT('Ctrl Pts',(1.00306229115158,55.7506306393371,-1.73735485143099));
#7496=CARTESIAN_POINT('Ctrl Pts',(2.00612458230317,55.6922973060038,-1.15823656762066));
#7497=CARTESIAN_POINT('Ctrl Pts',(2.00612458230317,55.6339639726704,-2.45679404840839E-16));
#7498=CARTESIAN_POINT('Ctrl Pts',(2.00612458230317,55.5756306393371,1.15823656762066));
#7499=CARTESIAN_POINT('Ctrl Pts',(1.00306229115158,55.5172973060038,1.73735485143099));
#7500=CARTESIAN_POINT('Ctrl Pts',(4.25529211557617E-16,55.4589639726704,
2.31647313524132));
#7501=CARTESIAN_POINT('Ctrl Pts',(-1.00306229115158,55.4006306393371,1.73735485143099));
#7502=CARTESIAN_POINT('Ctrl Pts',(-2.00612458230316,55.3422973060038,1.15823656762066));
#7503=CARTESIAN_POINT('Ctrl Pts',(-2.00612458230317,55.2839639726704,0.));
#7504=CARTESIAN_POINT('Ctrl Pts',(-2.00612458230317,55.2256306393371,-1.15823656762066));
#7505=CARTESIAN_POINT('Ctrl Pts',(-1.00306229115158,55.1672973060038,-1.73735485143099));
#7506=CARTESIAN_POINT('Ctrl Pts',(-1.41843070519206E-16,55.1089639726704,
-2.31647313524132));
#7507=CARTESIAN_POINT('Ctrl Pts',(1.00306229115158,55.0506306393371,-1.73735485143099));
#7508=CARTESIAN_POINT('Ctrl Pts',(2.00612458230317,54.9922973060038,-1.15823656762066));
#7509=CARTESIAN_POINT('Ctrl Pts',(2.00612458230317,54.9339639726704,-2.45679404840839E-16));
#7510=CARTESIAN_POINT('Ctrl Pts',(2.00612458230317,54.8756306393371,1.15823656762066));
#7511=CARTESIAN_POINT('Ctrl Pts',(1.00306229115158,54.8172973060038,1.73735485143099));
#7512=CARTESIAN_POINT('Ctrl Pts',(4.25529211557617E-16,54.7589639726704,
2.31647313524132));
#7513=CARTESIAN_POINT('Ctrl Pts',(-1.00306229115158,54.7006306393371,1.73735485143099));
#7514=CARTESIAN_POINT('Ctrl Pts',(-2.00612458230316,54.6422973060038,1.15823656762066));
#7515=CARTESIAN_POINT('Ctrl Pts',(-2.00612458230317,54.5839639726704,0.));
#7516=CARTESIAN_POINT('Ctrl Pts',(-2.00612458230317,54.5256306393371,-1.15823656762066));
#7517=CARTESIAN_POINT('Ctrl Pts',(-1.00306229115158,54.4672973060038,-1.73735485143099));
#7518=CARTESIAN_POINT('Ctrl Pts',(-1.41843070519206E-16,54.4089639726704,
-2.31647313524132));
#7519=CARTESIAN_POINT('Ctrl Pts',(1.00306229115158,54.3506306393371,-1.73735485143099));
#7520=CARTESIAN_POINT('Ctrl Pts',(2.00612458230317,54.2922973060038,-1.15823656762066));
#7521=CARTESIAN_POINT('Ctrl Pts',(2.00612458230317,54.2339639726704,-2.45679404840839E-16));
#7522=CARTESIAN_POINT('Ctrl Pts',(2.00612458230317,54.1756306393371,1.15823656762066));
#7523=CARTESIAN_POINT('Ctrl Pts',(1.00306229115158,54.1172973060038,1.73735485143099));
#7524=CARTESIAN_POINT('Ctrl Pts',(4.25529211557617E-16,54.0589639726704,
2.31647313524132));
#7525=CARTESIAN_POINT('Ctrl Pts',(-1.00306229115158,54.0006306393371,1.73735485143099));
#7526=CARTESIAN_POINT('Ctrl Pts',(-2.00612458230316,53.9422973060038,1.15823656762066));
#7527=CARTESIAN_POINT('Ctrl Pts',(-2.00612458230317,53.8839639726704,0.));
#7528=CARTESIAN_POINT('Ctrl Pts',(-2.00612458230317,53.8256306393371,-1.15823656762066));
#7529=CARTESIAN_POINT('Ctrl Pts',(-1.00306229115158,53.7672973060038,-1.73735485143099));
#7530=CARTESIAN_POINT('Ctrl Pts',(-1.41843070519206E-16,53.7089639726704,
-2.31647313524132));
#7531=CARTESIAN_POINT('Ctrl Pts',(1.00306229115158,53.6506306393371,-1.73735485143099));
#7532=CARTESIAN_POINT('Ctrl Pts',(2.00612458230317,53.5922973060038,-1.15823656762066));
#7533=CARTESIAN_POINT('Ctrl Pts',(2.00612458230317,53.5339639726704,-2.45679404840839E-16));
#7534=CARTESIAN_POINT('Ctrl Pts',(2.00612458230317,53.4756306393371,1.15823656762066));
#7535=CARTESIAN_POINT('Ctrl Pts',(1.00306229115158,53.4172973060038,1.73735485143099));
#7536=CARTESIAN_POINT('Ctrl Pts',(4.25529211557617E-16,53.3589639726704,
2.31647313524132));
#7537=CARTESIAN_POINT('Ctrl Pts',(-1.00306229115158,53.3006306393371,1.73735485143099));
#7538=CARTESIAN_POINT('Ctrl Pts',(-2.00612458230316,53.2422973060038,1.15823656762066));
#7539=CARTESIAN_POINT('Ctrl Pts',(-2.00612458230317,53.1839639726704,0.));
#7540=CARTESIAN_POINT('Ctrl Pts',(-2.00612458230317,53.1256306393371,-1.15823656762066));
#7541=CARTESIAN_POINT('Ctrl Pts',(-1.00306229115158,53.0672973060038,-1.73735485143099));
#7542=CARTESIAN_POINT('Ctrl Pts',(-1.41843070519206E-16,53.0089639726704,
-2.31647313524132));
#7543=CARTESIAN_POINT('Ctrl Pts',(1.00306229115158,52.9506306393371,-1.73735485143099));
#7544=CARTESIAN_POINT('Ctrl Pts',(2.00612458230317,52.8922973060038,-1.15823656762066));
#7545=CARTESIAN_POINT('Ctrl Pts',(2.00612458230317,52.8339639726704,-2.45679404840839E-16));
#7546=CARTESIAN_POINT('Ctrl Pts',(2.00612458230317,52.7756306393371,1.15823656762066));
#7547=CARTESIAN_POINT('Ctrl Pts',(1.00306229115158,52.7172973060038,1.73735485143099));
#7548=CARTESIAN_POINT('Ctrl Pts',(4.25529211557617E-16,52.6589639726704,
2.31647313524132));
#7549=CARTESIAN_POINT('Ctrl Pts',(-1.00306229115158,52.6006306393371,1.73735485143099));
#7550=CARTESIAN_POINT('Ctrl Pts',(-2.00612458230316,52.5422973060038,1.15823656762066));
#7551=CARTESIAN_POINT('Ctrl Pts',(-2.00612458230317,52.4839639726704,0.));
#7552=CARTESIAN_POINT('Ctrl Pts',(-2.00612458230317,52.4256306393371,-1.15823656762066));
#7553=CARTESIAN_POINT('Ctrl Pts',(-1.00306229115158,52.3672973060038,-1.73735485143099));
#7554=CARTESIAN_POINT('Ctrl Pts',(-1.41843070519206E-16,52.3089639726704,
-2.31647313524132));
#7555=CARTESIAN_POINT('Ctrl Pts',(1.00306229115158,52.2506306393371,-1.73735485143099));
#7556=CARTESIAN_POINT('Ctrl Pts',(2.00612458230317,52.1922973060038,-1.15823656762066));
#7557=CARTESIAN_POINT('Ctrl Pts',(2.00612458230317,52.1339639726704,-2.45679404840839E-16));
#7558=CARTESIAN_POINT('Ctrl Pts',(2.00612458230317,52.0756306393371,1.15823656762066));
#7559=CARTESIAN_POINT('Ctrl Pts',(1.00306229115158,52.0172973060038,1.73735485143099));
#7560=CARTESIAN_POINT('Ctrl Pts',(4.25529211557617E-16,51.9589639726704,
2.31647313524132));
#7561=CARTESIAN_POINT('Ctrl Pts',(-1.00306229115158,51.9006306393371,1.73735485143099));
#7562=CARTESIAN_POINT('Ctrl Pts',(-2.00612458230316,51.8422973060038,1.15823656762066));
#7563=CARTESIAN_POINT('Ctrl Pts',(-2.00612458230317,51.7839639726704,0.));
#7564=CARTESIAN_POINT('Ctrl Pts',(-2.00612458230317,51.7256306393371,-1.15823656762066));
#7565=CARTESIAN_POINT('Ctrl Pts',(-1.00306229115158,51.6672973060038,-1.73735485143099));
#7566=CARTESIAN_POINT('Ctrl Pts',(-1.41843070519206E-16,51.6089639726704,
-2.31647313524132));
#7567=CARTESIAN_POINT('Ctrl Pts',(1.00306229115158,51.5506306393371,-1.73735485143099));
#7568=CARTESIAN_POINT('Ctrl Pts',(2.00612458230317,51.4922973060038,-1.15823656762066));
#7569=CARTESIAN_POINT('Ctrl Pts',(2.00612458230317,51.4339639726704,-2.45679404840839E-16));
#7570=CARTESIAN_POINT('Ctrl Pts',(2.00612458230317,51.3756306393371,1.15823656762066));
#7571=CARTESIAN_POINT('Ctrl Pts',(1.00306229115158,51.3172973060038,1.73735485143099));
#7572=CARTESIAN_POINT('Ctrl Pts',(4.25529211557617E-16,51.2589639726704,
2.31647313524132));
#7573=CARTESIAN_POINT('Ctrl Pts',(-1.00306229115158,51.2006306393371,1.73735485143099));
#7574=CARTESIAN_POINT('Ctrl Pts',(-2.00612458230316,51.1422973060038,1.15823656762066));
#7575=CARTESIAN_POINT('Ctrl Pts',(-2.00612458230317,51.0839639726704,0.));
#7576=CARTESIAN_POINT('Ctrl Pts',(-2.00612458230317,51.0256306393371,-1.15823656762066));
#7577=CARTESIAN_POINT('Ctrl Pts',(-1.00306229115158,50.9672973060038,-1.73735485143099));
#7578=CARTESIAN_POINT('Ctrl Pts',(-1.41843070519206E-16,50.9089639726704,
-2.31647313524132));
#7579=CARTESIAN_POINT('Ctrl Pts',(1.00306229115158,50.8506306393371,-1.73735485143099));
#7580=CARTESIAN_POINT('Ctrl Pts',(2.00612458230317,50.7922973060038,-1.15823656762066));
#7581=CARTESIAN_POINT('Ctrl Pts',(2.00612458230317,50.7339639726704,-2.45679404840839E-16));
#7582=CARTESIAN_POINT('Ctrl Pts',(2.00612458230317,50.6756306393371,1.15823656762066));
#7583=CARTESIAN_POINT('Ctrl Pts',(1.00306229115158,50.6172973060038,1.73735485143099));
#7584=CARTESIAN_POINT('Ctrl Pts',(4.25529211557617E-16,50.5589639726704,
2.31647313524132));
#7585=CARTESIAN_POINT('Ctrl Pts',(-1.00306229115158,50.5006306393371,1.73735485143099));
#7586=CARTESIAN_POINT('Ctrl Pts',(-2.00612458230316,50.4422973060038,1.15823656762066));
#7587=CARTESIAN_POINT('Ctrl Pts',(-2.00612458230317,50.3839639726704,0.));
#7588=CARTESIAN_POINT('Ctrl Pts',(-2.00612458230317,50.3256306393371,-1.15823656762066));
#7589=CARTESIAN_POINT('Ctrl Pts',(-1.00306229115158,50.2672973060038,-1.73735485143099));
#7590=CARTESIAN_POINT('Ctrl Pts',(-1.41843070519206E-16,50.2089639726704,
-2.31647313524132));
#7591=CARTESIAN_POINT('Ctrl Pts',(1.00306229115158,50.1506306393371,-1.73735485143099));
#7592=CARTESIAN_POINT('Ctrl Pts',(2.00612458230317,50.0922973060038,-1.15823656762066));
#7593=CARTESIAN_POINT('Ctrl Pts',(2.00612458230317,50.0339639726704,-2.45679404840839E-16));
#7594=CARTESIAN_POINT('Ctrl Pts',(2.00612458230317,49.9756306393371,1.15823656762066));
#7595=CARTESIAN_POINT('Ctrl Pts',(1.00306229115158,49.9172973060038,1.73735485143099));
#7596=CARTESIAN_POINT('Ctrl Pts',(4.25529211557617E-16,49.8589639726704,
2.31647313524132));
#7597=CARTESIAN_POINT('Ctrl Pts',(-1.00306229115158,49.8006306393371,1.73735485143099));
#7598=CARTESIAN_POINT('Ctrl Pts',(-2.00612458230316,49.7422973060038,1.15823656762066));
#7599=CARTESIAN_POINT('Ctrl Pts',(-2.00612458230317,49.6839639726704,0.));
#7600=CARTESIAN_POINT('Ctrl Pts',(-2.00612458230317,49.6256306393371,-1.15823656762066));
#7601=CARTESIAN_POINT('Ctrl Pts',(-1.00306229115158,49.5672973060038,-1.73735485143099));
#7602=CARTESIAN_POINT('Ctrl Pts',(-1.41843070519206E-16,49.5089639726704,
-2.31647313524132));
#7603=CARTESIAN_POINT('Ctrl Pts',(1.00306229115158,49.4506306393371,-1.73735485143099));
#7604=CARTESIAN_POINT('Ctrl Pts',(2.00612458230317,49.3922973060038,-1.15823656762066));
#7605=CARTESIAN_POINT('Ctrl Pts',(2.00612458230317,49.3339639726704,-2.45679404840839E-16));
#7606=CARTESIAN_POINT('Ctrl Pts',(2.00612458230317,49.2756306393371,1.15823656762066));
#7607=CARTESIAN_POINT('Ctrl Pts',(1.00306229115158,49.2172973060038,1.73735485143099));
#7608=CARTESIAN_POINT('Ctrl Pts',(4.25529211557617E-16,49.1589639726704,
2.31647313524132));
#7609=CARTESIAN_POINT('Ctrl Pts',(-1.00306229115158,49.1006306393371,1.73735485143099));
#7610=CARTESIAN_POINT('Ctrl Pts',(-2.00612458230316,49.0422973060038,1.15823656762066));
#7611=CARTESIAN_POINT('Ctrl Pts',(-2.00612458230317,48.9839639726704,0.));
#7612=CARTESIAN_POINT('Ctrl Pts',(-2.00612458230317,48.9256306393371,-1.15823656762066));
#7613=CARTESIAN_POINT('Ctrl Pts',(-1.00306229115158,48.8672973060038,-1.73735485143099));
#7614=CARTESIAN_POINT('Ctrl Pts',(-1.41843070519206E-16,48.8089639726704,
-2.31647313524132));
#7615=CARTESIAN_POINT('Ctrl Pts',(1.00306229115158,48.7506306393371,-1.73735485143099));
#7616=CARTESIAN_POINT('Ctrl Pts',(2.00612458230317,48.6922973060038,-1.15823656762066));
#7617=CARTESIAN_POINT('Ctrl Pts',(2.00612458230317,48.6339639726704,-2.45679404840839E-16));
#7618=CARTESIAN_POINT('Ctrl Pts',(2.00612458230317,48.5756306393371,1.15823656762066));
#7619=CARTESIAN_POINT('Ctrl Pts',(1.00306229115158,48.5172973060038,1.73735485143099));
#7620=CARTESIAN_POINT('Ctrl Pts',(4.25529211557617E-16,48.4589639726704,
2.31647313524132));
#7621=CARTESIAN_POINT('Ctrl Pts',(-1.00306229115158,48.4006306393371,1.73735485143099));
#7622=CARTESIAN_POINT('Ctrl Pts',(-2.00612458230316,48.3422973060038,1.15823656762066));
#7623=CARTESIAN_POINT('Ctrl Pts',(-2.00612458230317,48.2839639726704,0.));
#7624=CARTESIAN_POINT('Ctrl Pts',(-2.00612458230317,48.2256306393371,-1.15823656762066));
#7625=CARTESIAN_POINT('Ctrl Pts',(-1.00306229115158,48.1672973060038,-1.73735485143099));
#7626=CARTESIAN_POINT('Ctrl Pts',(-1.41843070519206E-16,48.1089639726704,
-2.31647313524132));
#7627=CARTESIAN_POINT('Ctrl Pts',(1.00306229115158,48.0506306393371,-1.73735485143099));
#7628=CARTESIAN_POINT('Ctrl Pts',(2.00612458230317,47.9922973060037,-1.15823656762066));
#7629=CARTESIAN_POINT('Ctrl Pts',(2.00612458230317,47.9339639726704,-2.45679404840839E-16));
#7630=CARTESIAN_POINT('Ctrl Pts',(2.00612458230317,47.8756306393371,1.15823656762066));
#7631=CARTESIAN_POINT('Ctrl Pts',(1.00306229115158,47.8172973060038,1.73735485143099));
#7632=CARTESIAN_POINT('Ctrl Pts',(4.25529211557617E-16,47.7589639726704,
2.31647313524132));
#7633=CARTESIAN_POINT('Ctrl Pts',(-1.00306229115158,47.7006306393371,1.73735485143099));
#7634=CARTESIAN_POINT('Ctrl Pts',(-2.00612458230316,47.6422973060038,1.15823656762066));
#7635=CARTESIAN_POINT('Ctrl Pts',(-2.00612458230317,47.5839639726704,0.));
#7636=CARTESIAN_POINT('Ctrl Pts',(-2.00612458230317,47.5256306393371,-1.15823656762066));
#7637=CARTESIAN_POINT('Ctrl Pts',(-1.00306229115158,47.4672973060038,-1.73735485143099));
#7638=CARTESIAN_POINT('Ctrl Pts',(-1.41843070519206E-16,47.4089639726704,
-2.31647313524132));
#7639=CARTESIAN_POINT('Ctrl Pts',(1.00306229115158,47.3506306393371,-1.73735485143099));
#7640=CARTESIAN_POINT('Ctrl Pts',(2.00612458230317,47.2922973060038,-1.15823656762066));
#7641=CARTESIAN_POINT('Ctrl Pts',(2.00612458230317,47.2339639726704,-2.45679404840839E-16));
#7642=CARTESIAN_POINT('Ctrl Pts',(2.00612458230317,47.1756306393371,1.15823656762066));
#7643=CARTESIAN_POINT('Ctrl Pts',(1.00306229115158,47.1172973060038,1.73735485143099));
#7644=CARTESIAN_POINT('Ctrl Pts',(4.25529211557617E-16,47.0589639726704,
2.31647313524132));
#7645=CARTESIAN_POINT('Ctrl Pts',(-1.00306229115158,47.0006306393371,1.73735485143099));
#7646=CARTESIAN_POINT('Ctrl Pts',(-2.00612458230316,46.9422973060038,1.15823656762066));
#7647=CARTESIAN_POINT('Ctrl Pts',(-2.00612458230317,46.8839639726704,0.));
#7648=CARTESIAN_POINT('Ctrl Pts',(-2.00612458230317,46.8256306393371,-1.15823656762066));
#7649=CARTESIAN_POINT('Ctrl Pts',(-1.00306229115158,46.7672973060038,-1.73735485143099));
#7650=CARTESIAN_POINT('Ctrl Pts',(-1.41843070519206E-16,46.7089639726704,
-2.31647313524132));
#7651=CARTESIAN_POINT('Ctrl Pts',(1.00306229115158,46.6506306393371,-1.73735485143099));
#7652=CARTESIAN_POINT('Ctrl Pts',(2.00612458230317,46.5922973060038,-1.15823656762066));
#7653=CARTESIAN_POINT('Ctrl Pts',(2.00612458230317,46.5339639726704,-2.45679404840839E-16));
#7654=CARTESIAN_POINT('Ctrl Pts',(2.00612458230317,46.4756306393371,1.15823656762066));
#7655=CARTESIAN_POINT('Ctrl Pts',(1.00306229115158,46.4172973060038,1.73735485143099));
#7656=CARTESIAN_POINT('Ctrl Pts',(4.25529211557617E-16,46.3589639726704,
2.31647313524132));
#7657=CARTESIAN_POINT('Ctrl Pts',(-1.00306229115158,46.3006306393371,1.73735485143099));
#7658=CARTESIAN_POINT('Ctrl Pts',(-2.00612458230316,46.2422973060038,1.15823656762066));
#7659=CARTESIAN_POINT('Ctrl Pts',(-2.00612458230317,46.1839639726704,0.));
#7660=CARTESIAN_POINT('Ctrl Pts',(-2.00612458230317,46.1256306393371,-1.15823656762066));
#7661=CARTESIAN_POINT('Ctrl Pts',(-1.00306229115158,46.0672973060038,-1.73735485143099));
#7662=CARTESIAN_POINT('Ctrl Pts',(-1.41843070519206E-16,46.0089639726704,
-2.31647313524132));
#7663=CARTESIAN_POINT('Ctrl Pts',(1.00306229115158,45.9506306393371,-1.73735485143099));
#7664=CARTESIAN_POINT('Ctrl Pts',(2.00612458230317,45.8922973060038,-1.15823656762066));
#7665=CARTESIAN_POINT('Ctrl Pts',(2.00612458230317,45.8339639726704,-2.45679404840839E-16));
#7666=CARTESIAN_POINT('Ctrl Pts',(2.00612458230317,45.7756306393371,1.15823656762066));
#7667=CARTESIAN_POINT('Ctrl Pts',(1.00306229115158,45.7172973060038,1.73735485143099));
#7668=CARTESIAN_POINT('Ctrl Pts',(4.25529211557617E-16,45.6589639726704,
2.31647313524132));
#7669=CARTESIAN_POINT('Ctrl Pts',(-1.00306229115158,45.6006306393371,1.73735485143099));
#7670=CARTESIAN_POINT('Ctrl Pts',(-2.00612458230316,45.5422973060038,1.15823656762066));
#7671=CARTESIAN_POINT('Ctrl Pts',(-2.00612458230317,45.4839639726704,0.));
#7672=CARTESIAN_POINT('Ctrl Pts',(-2.00612458230317,45.4256306393371,-1.15823656762066));
#7673=CARTESIAN_POINT('Ctrl Pts',(-1.00306229115158,45.3672973060038,-1.73735485143099));
#7674=CARTESIAN_POINT('Ctrl Pts',(-1.41843070519206E-16,45.3089639726704,
-2.31647313524132));
#7675=CARTESIAN_POINT('Ctrl Pts',(1.00306229115158,45.2506306393371,-1.73735485143099));
#7676=CARTESIAN_POINT('Ctrl Pts',(2.00612458230317,45.1922973060038,-1.15823656762066));
#7677=CARTESIAN_POINT('Ctrl Pts',(2.00612458230317,45.1339639726704,-2.45679404840839E-16));
#7678=CARTESIAN_POINT('Ctrl Pts',(2.00612458230317,45.0756306393371,1.15823656762066));
#7679=CARTESIAN_POINT('Ctrl Pts',(1.00306229115158,45.0172973060038,1.73735485143099));
#7680=CARTESIAN_POINT('Ctrl Pts',(4.25529211557617E-16,44.9589639726704,
2.31647313524132));
#7681=CARTESIAN_POINT('Ctrl Pts',(-1.00306229115158,44.9006306393371,1.73735485143099));
#7682=CARTESIAN_POINT('Ctrl Pts',(-2.00612458230316,44.8422973060038,1.15823656762066));
#7683=CARTESIAN_POINT('Ctrl Pts',(-2.00612458230317,44.7839639726704,0.));
#7684=CARTESIAN_POINT('Ctrl Pts',(-2.00612458230317,44.7256306393371,-1.15823656762066));
#7685=CARTESIAN_POINT('Ctrl Pts',(-1.00306229115158,44.6672973060038,-1.73735485143099));
#7686=CARTESIAN_POINT('Ctrl Pts',(-1.41843070519206E-16,44.6089639726704,
-2.31647313524132));
#7687=CARTESIAN_POINT('Ctrl Pts',(1.00306229115158,44.5506306393371,-1.73735485143099));
#7688=CARTESIAN_POINT('Ctrl Pts',(2.00612458230317,44.4922973060038,-1.15823656762066));
#7689=CARTESIAN_POINT('Ctrl Pts',(2.00612458230317,44.4339639726704,-2.45679404840839E-16));
#7690=CARTESIAN_POINT('Ctrl Pts',(2.00612458230317,44.3756306393371,1.15823656762066));
#7691=CARTESIAN_POINT('Ctrl Pts',(1.00306229115158,44.3172973060038,1.73735485143099));
#7692=CARTESIAN_POINT('Ctrl Pts',(4.25529211557617E-16,44.2589639726704,
2.31647313524132));
#7693=CARTESIAN_POINT('Ctrl Pts',(-1.00306229115158,44.2006306393371,1.73735485143099));
#7694=CARTESIAN_POINT('Ctrl Pts',(-2.00612458230316,44.1422973060038,1.15823656762066));
#7695=CARTESIAN_POINT('Ctrl Pts',(-2.00612458230317,44.0839639726704,0.));
#7696=CARTESIAN_POINT('Ctrl Pts',(-2.00612458230317,44.0256306393371,-1.15823656762066));
#7697=CARTESIAN_POINT('Ctrl Pts',(-1.00306229115158,43.9672973060038,-1.73735485143099));
#7698=CARTESIAN_POINT('Ctrl Pts',(-1.41843070519206E-16,43.9089639726704,
-2.31647313524132));
#7699=CARTESIAN_POINT('Ctrl Pts',(1.00306229115158,43.8506306393371,-1.73735485143099));
#7700=CARTESIAN_POINT('Ctrl Pts',(2.00612458230317,43.7922973060038,-1.15823656762066));
#7701=CARTESIAN_POINT('Ctrl Pts',(2.00612458230317,43.7339639726704,-2.45679404840839E-16));
#7702=CARTESIAN_POINT('Ctrl Pts',(2.00612458230317,43.6756306393371,1.15823656762066));
#7703=CARTESIAN_POINT('Ctrl Pts',(1.00306229115158,43.6172973060038,1.73735485143099));
#7704=CARTESIAN_POINT('Ctrl Pts',(4.25529211557617E-16,43.5589639726704,
2.31647313524132));
#7705=CARTESIAN_POINT('Ctrl Pts',(-1.00306229115158,43.5006306393371,1.73735485143099));
#7706=CARTESIAN_POINT('Ctrl Pts',(-2.00612458230316,43.4422973060038,1.15823656762066));
#7707=CARTESIAN_POINT('Ctrl Pts',(-2.00612458230317,43.3839639726704,0.));
#7708=CARTESIAN_POINT('Ctrl Pts',(-2.00612458230317,43.3256306393371,-1.15823656762066));
#7709=CARTESIAN_POINT('Ctrl Pts',(-1.00306229115158,43.2672973060038,-1.73735485143099));
#7710=CARTESIAN_POINT('Ctrl Pts',(-1.41843070519206E-16,43.2089639726704,
-2.31647313524132));
#7711=CARTESIAN_POINT('Ctrl Pts',(1.00306229115158,43.1506306393371,-1.73735485143099));
#7712=CARTESIAN_POINT('Ctrl Pts',(2.00612458230317,43.0922973060038,-1.15823656762066));
#7713=CARTESIAN_POINT('Ctrl Pts',(2.00612458230317,43.0339639726704,-2.45679404840839E-16));
#7714=CARTESIAN_POINT('Ctrl Pts',(2.00612458230317,42.9756306393371,1.15823656762066));
#7715=CARTESIAN_POINT('Ctrl Pts',(1.00306229115158,42.9172973060038,1.73735485143099));
#7716=CARTESIAN_POINT('Ctrl Pts',(4.25529211557617E-16,42.8589639726704,
2.31647313524132));
#7717=CARTESIAN_POINT('Ctrl Pts',(-1.00306229115158,42.8006306393371,1.73735485143099));
#7718=CARTESIAN_POINT('Ctrl Pts',(-2.00612458230316,42.7422973060038,1.15823656762066));
#7719=CARTESIAN_POINT('Ctrl Pts',(-2.00612458230317,42.6839639726704,0.));
#7720=CARTESIAN_POINT('Ctrl Pts',(-2.00612458230317,42.6256306393371,-1.15823656762066));
#7721=CARTESIAN_POINT('Ctrl Pts',(-1.00306229115158,42.5672973060038,-1.73735485143099));
#7722=CARTESIAN_POINT('Ctrl Pts',(-1.41843070519206E-16,42.5089639726704,
-2.31647313524132));
#7723=CARTESIAN_POINT('Ctrl Pts',(1.00306229115158,42.4506306393371,-1.73735485143099));
#7724=CARTESIAN_POINT('Ctrl Pts',(2.00612458230317,42.3922973060038,-1.15823656762066));
#7725=CARTESIAN_POINT('Ctrl Pts',(2.00612458230317,42.3339639726704,-2.45679404840839E-16));
#7726=CARTESIAN_POINT('Ctrl Pts',(2.00612458230317,42.2756306393371,1.15823656762066));
#7727=CARTESIAN_POINT('Ctrl Pts',(1.00306229115158,42.2172973060038,1.73735485143099));
#7728=CARTESIAN_POINT('Ctrl Pts',(4.25529211557617E-16,42.1589639726704,
2.31647313524132));
#7729=CARTESIAN_POINT('Ctrl Pts',(-1.00306229115158,42.1006306393371,1.73735485143099));
#7730=CARTESIAN_POINT('Ctrl Pts',(-2.00612458230316,42.0422973060038,1.15823656762066));
#7731=CARTESIAN_POINT('Ctrl Pts',(-2.00612458230317,41.9839639726704,0.));
#7732=CARTESIAN_POINT('Ctrl Pts',(-2.00612458230317,41.9256306393371,-1.15823656762066));
#7733=CARTESIAN_POINT('Ctrl Pts',(-1.00306229115158,41.8672973060038,-1.73735485143099));
#7734=CARTESIAN_POINT('Ctrl Pts',(-1.41843070519206E-16,41.8089639726704,
-2.31647313524132));
#7735=CARTESIAN_POINT('Ctrl Pts',(1.00306229115158,41.7506306393371,-1.73735485143099));
#7736=CARTESIAN_POINT('Ctrl Pts',(2.00612458230317,41.6922973060038,-1.15823656762066));
#7737=CARTESIAN_POINT('Ctrl Pts',(2.00612458230317,41.6339639726704,-2.45679404840839E-16));
#7738=CARTESIAN_POINT('Ctrl Pts',(2.00612458230317,41.5756306393371,1.15823656762066));
#7739=CARTESIAN_POINT('Ctrl Pts',(1.00306229115158,41.5172973060038,1.73735485143099));
#7740=CARTESIAN_POINT('Ctrl Pts',(4.25529211557617E-16,41.4589639726704,
2.31647313524132));
#7741=CARTESIAN_POINT('Ctrl Pts',(-1.00306229115158,41.4006306393371,1.73735485143099));
#7742=CARTESIAN_POINT('Ctrl Pts',(-2.00612458230316,41.3422973060038,1.15823656762066));
#7743=CARTESIAN_POINT('Ctrl Pts',(-2.00612458230317,41.2839639726704,0.));
#7744=CARTESIAN_POINT('Ctrl Pts',(-2.00612458230317,41.2256306393371,-1.15823656762066));
#7745=CARTESIAN_POINT('Ctrl Pts',(-1.00306229115158,41.1672973060038,-1.73735485143099));
#7746=CARTESIAN_POINT('Ctrl Pts',(-1.41843070519206E-16,41.1089639726704,
-2.31647313524132));
#7747=CARTESIAN_POINT('Ctrl Pts',(1.00306229115158,41.0506306393371,-1.73735485143099));
#7748=CARTESIAN_POINT('Ctrl Pts',(2.00612458230317,40.9922973060038,-1.15823656762066));
#7749=CARTESIAN_POINT('Ctrl Pts',(2.00612458230317,40.9339639726704,-2.45679404840839E-16));
#7750=CARTESIAN_POINT('Ctrl Pts',(2.00612458230317,40.8756306393371,1.15823656762066));
#7751=CARTESIAN_POINT('Ctrl Pts',(1.00306229115158,40.8172973060038,1.73735485143099));
#7752=CARTESIAN_POINT('Ctrl Pts',(4.25529211557617E-16,40.7589639726704,
2.31647313524132));
#7753=CARTESIAN_POINT('Ctrl Pts',(-1.00306229115158,40.7006306393371,1.73735485143099));
#7754=CARTESIAN_POINT('Ctrl Pts',(-2.00612458230316,40.6422973060038,1.15823656762066));
#7755=CARTESIAN_POINT('Ctrl Pts',(-2.00612458230317,40.5839639726704,0.));
#7756=CARTESIAN_POINT('Ctrl Pts',(-2.00612458230317,40.5256306393371,-1.15823656762066));
#7757=CARTESIAN_POINT('Ctrl Pts',(-1.00306229115158,40.4672973060038,-1.73735485143099));
#7758=CARTESIAN_POINT('Ctrl Pts',(-1.41843070519206E-16,40.4089639726704,
-2.31647313524132));
#7759=CARTESIAN_POINT('Ctrl Pts',(1.00306229115158,40.3506306393371,-1.73735485143099));
#7760=CARTESIAN_POINT('Ctrl Pts',(2.00612458230317,40.2922973060038,-1.15823656762066));
#7761=CARTESIAN_POINT('Ctrl Pts',(2.00612458230317,40.2339639726704,-2.45679404840839E-16));
#7762=CARTESIAN_POINT('Ctrl Pts',(2.00612458230317,40.1756306393371,1.15823656762066));
#7763=CARTESIAN_POINT('Ctrl Pts',(1.00306229115158,40.1172973060038,1.73735485143099));
#7764=CARTESIAN_POINT('Ctrl Pts',(4.25529211557617E-16,40.0589639726704,
2.31647313524132));
#7765=CARTESIAN_POINT('Ctrl Pts',(-1.00306229115158,40.0006306393371,1.73735485143099));
#7766=CARTESIAN_POINT('Ctrl Pts',(-2.00612458230316,39.9422973060038,1.15823656762066));
#7767=CARTESIAN_POINT('Ctrl Pts',(-2.00612458230317,39.8839639726704,0.));
#7768=CARTESIAN_POINT('Ctrl Pts',(-2.00612458230317,39.8256306393371,-1.15823656762066));
#7769=CARTESIAN_POINT('Ctrl Pts',(-1.00306229115158,39.7672973060038,-1.73735485143099));
#7770=CARTESIAN_POINT('Ctrl Pts',(-1.41843070519206E-16,39.7089639726704,
-2.31647313524132));
#7771=CARTESIAN_POINT('Ctrl Pts',(1.00306229115158,39.6506306393371,-1.73735485143099));
#7772=CARTESIAN_POINT('Ctrl Pts',(2.00612458230317,39.5922973060038,-1.15823656762066));
#7773=CARTESIAN_POINT('Ctrl Pts',(2.00612458230317,39.5339639726704,-2.45679404840839E-16));
#7774=CARTESIAN_POINT('Ctrl Pts',(2.00612458230317,39.4756306393371,1.15823656762066));
#7775=CARTESIAN_POINT('Ctrl Pts',(1.00306229115158,39.4172973060038,1.73735485143099));
#7776=CARTESIAN_POINT('Ctrl Pts',(4.25529211557617E-16,39.3589639726704,
2.31647313524132));
#7777=CARTESIAN_POINT('Ctrl Pts',(-1.00306229115158,39.3006306393371,1.73735485143099));
#7778=CARTESIAN_POINT('Ctrl Pts',(-2.00612458230316,39.2422973060038,1.15823656762066));
#7779=CARTESIAN_POINT('Ctrl Pts',(-2.00612458230317,39.1839639726704,0.));
#7780=CARTESIAN_POINT('Ctrl Pts',(-2.00612458230317,39.1256306393371,-1.15823656762066));
#7781=CARTESIAN_POINT('Ctrl Pts',(-1.00306229115158,39.0672973060038,-1.73735485143099));
#7782=CARTESIAN_POINT('Ctrl Pts',(-1.41843070519206E-16,39.0089639726704,
-2.31647313524132));
#7783=CARTESIAN_POINT('Ctrl Pts',(1.00306229115158,38.9506306393371,-1.73735485143099));
#7784=CARTESIAN_POINT('Ctrl Pts',(2.00612458230317,38.8922973060038,-1.15823656762066));
#7785=CARTESIAN_POINT('Ctrl Pts',(2.00612458230317,38.8339639726704,-2.45679404840839E-16));
#7786=CARTESIAN_POINT('Ctrl Pts',(2.00612458230317,38.7756306393371,1.15823656762066));
#7787=CARTESIAN_POINT('Ctrl Pts',(1.00306229115158,38.7172973060038,1.73735485143099));
#7788=CARTESIAN_POINT('Ctrl Pts',(4.25529211557617E-16,38.6589639726704,
2.31647313524132));
#7789=CARTESIAN_POINT('Ctrl Pts',(-1.00306229115158,38.6006306393371,1.73735485143099));
#7790=CARTESIAN_POINT('Ctrl Pts',(-2.00612458230316,38.5422973060038,1.15823656762066));
#7791=CARTESIAN_POINT('Ctrl Pts',(-2.00612458230317,38.4839639726704,0.));
#7792=CARTESIAN_POINT('Ctrl Pts',(-2.00612458230317,38.4256306393371,-1.15823656762066));
#7793=CARTESIAN_POINT('Ctrl Pts',(-1.00306229115158,38.3672973060038,-1.73735485143099));
#7794=CARTESIAN_POINT('Ctrl Pts',(-1.41843070519206E-16,38.3089639726704,
-2.31647313524132));
#7795=CARTESIAN_POINT('Ctrl Pts',(1.00306229115158,38.2506306393371,-1.73735485143099));
#7796=CARTESIAN_POINT('Ctrl Pts',(2.00612458230317,38.1922973060038,-1.15823656762066));
#7797=CARTESIAN_POINT('Ctrl Pts',(2.00612458230317,38.1339639726704,-2.45679404840839E-16));
#7798=CARTESIAN_POINT('Ctrl Pts',(2.00612458230317,38.0756306393371,1.15823656762066));
#7799=CARTESIAN_POINT('Ctrl Pts',(1.00306229115158,38.0172973060038,1.73735485143099));
#7800=CARTESIAN_POINT('Ctrl Pts',(4.25529211557617E-16,37.9589639726704,
2.31647313524132));
#7801=CARTESIAN_POINT('Ctrl Pts',(-1.00306229115158,37.9006306393371,1.73735485143099));
#7802=CARTESIAN_POINT('Ctrl Pts',(-2.00612458230316,37.8422973060038,1.15823656762066));
#7803=CARTESIAN_POINT('Ctrl Pts',(-2.00612458230317,37.7839639726704,0.));
#7804=CARTESIAN_POINT('Ctrl Pts',(-2.00612458230317,37.7256306393371,-1.15823656762066));
#7805=CARTESIAN_POINT('Ctrl Pts',(-1.00306229115158,37.6672973060038,-1.73735485143099));
#7806=CARTESIAN_POINT('Ctrl Pts',(-1.41843070519206E-16,37.6089639726704,
-2.31647313524132));
#7807=CARTESIAN_POINT('Ctrl Pts',(1.00306229115158,37.5506306393371,-1.73735485143099));
#7808=CARTESIAN_POINT('Ctrl Pts',(2.00612458230317,37.4922973060038,-1.15823656762066));
#7809=CARTESIAN_POINT('Ctrl Pts',(2.00612458230317,37.4339639726704,-2.45679404840839E-16));
#7810=CARTESIAN_POINT('Ctrl Pts',(2.00612458230317,37.3756306393371,1.15823656762066));
#7811=CARTESIAN_POINT('Ctrl Pts',(1.00306229115158,37.3172973060038,1.73735485143099));
#7812=CARTESIAN_POINT('Ctrl Pts',(4.25529211557617E-16,37.2589639726704,
2.31647313524132));
#7813=CARTESIAN_POINT('Ctrl Pts',(-1.00306229115158,37.2006306393371,1.73735485143099));
#7814=CARTESIAN_POINT('Ctrl Pts',(-2.00612458230316,37.1422973060038,1.15823656762066));
#7815=CARTESIAN_POINT('Ctrl Pts',(-2.00612458230317,37.0839639726704,0.));
#7816=CARTESIAN_POINT('Ctrl Pts',(-2.00612458230317,37.0256306393371,-1.15823656762066));
#7817=CARTESIAN_POINT('Ctrl Pts',(-1.00306229115158,36.9672973060038,-1.73735485143099));
#7818=CARTESIAN_POINT('Ctrl Pts',(-1.41843070519206E-16,36.9089639726704,
-2.31647313524132));
#7819=CARTESIAN_POINT('Ctrl Pts',(1.00306229115158,36.8506306393371,-1.73735485143099));
#7820=CARTESIAN_POINT('Ctrl Pts',(2.00612458230317,36.7922973060038,-1.15823656762066));
#7821=CARTESIAN_POINT('Ctrl Pts',(2.00612458230317,36.7339639726704,-2.45679404840839E-16));
#7822=CARTESIAN_POINT('Ctrl Pts',(2.00612458230317,36.6756306393371,1.15823656762066));
#7823=CARTESIAN_POINT('Ctrl Pts',(1.00306229115158,36.6172973060038,1.73735485143099));
#7824=CARTESIAN_POINT('Ctrl Pts',(4.25529211557617E-16,36.5589639726704,
2.31647313524132));
#7825=CARTESIAN_POINT('Ctrl Pts',(-1.00306229115158,36.5006306393371,1.73735485143099));
#7826=CARTESIAN_POINT('Ctrl Pts',(-2.00612458230316,36.4422973060038,1.15823656762066));
#7827=CARTESIAN_POINT('Ctrl Pts',(-2.00612458230317,36.3839639726704,0.));
#7828=CARTESIAN_POINT('Ctrl Pts',(-2.00612458230317,36.3256306393371,-1.15823656762066));
#7829=CARTESIAN_POINT('Ctrl Pts',(-1.00306229115158,36.2672973060038,-1.73735485143099));
#7830=CARTESIAN_POINT('Ctrl Pts',(-1.41843070519206E-16,36.2089639726704,
-2.31647313524132));
#7831=CARTESIAN_POINT('Ctrl Pts',(1.00306229115158,36.1506306393371,-1.73735485143099));
#7832=CARTESIAN_POINT('Ctrl Pts',(2.00612458230317,36.0922973060038,-1.15823656762066));
#7833=CARTESIAN_POINT('Ctrl Pts',(2.00612458230317,36.0339639726704,-2.45679404840839E-16));
#7834=CARTESIAN_POINT('Ctrl Pts',(2.00612458230317,35.9756306393371,1.15823656762066));
#7835=CARTESIAN_POINT('Ctrl Pts',(1.00306229115158,35.9172973060038,1.73735485143099));
#7836=CARTESIAN_POINT('Ctrl Pts',(4.25529211557617E-16,35.8589639726704,
2.31647313524132));
#7837=CARTESIAN_POINT('Ctrl Pts',(-1.00306229115158,35.8006306393371,1.73735485143099));
#7838=CARTESIAN_POINT('Ctrl Pts',(-2.00612458230316,35.7422973060038,1.15823656762066));
#7839=CARTESIAN_POINT('Ctrl Pts',(-2.00612458230317,35.6839639726704,0.));
#7840=CARTESIAN_POINT('Ctrl Pts',(-2.00612458230317,35.6256306393371,-1.15823656762066));
#7841=CARTESIAN_POINT('Ctrl Pts',(-1.00306229115158,35.5672973060038,-1.73735485143099));
#7842=CARTESIAN_POINT('Ctrl Pts',(-1.41843070519206E-16,35.5089639726704,
-2.31647313524132));
#7843=CARTESIAN_POINT('Ctrl Pts',(1.00306229115158,35.4506306393371,-1.73735485143099));
#7844=CARTESIAN_POINT('Ctrl Pts',(2.00612458230317,35.3922973060038,-1.15823656762066));
#7845=CARTESIAN_POINT('Ctrl Pts',(2.00612458230317,35.3339639726704,-2.45679404840839E-16));
#7846=CARTESIAN_POINT('Ctrl Pts',(2.00612458230317,35.2756306393371,1.15823656762066));
#7847=CARTESIAN_POINT('Ctrl Pts',(1.00306229115158,35.2172973060038,1.73735485143099));
#7848=CARTESIAN_POINT('Ctrl Pts',(4.25529211557617E-16,35.1589639726704,
2.31647313524132));
#7849=CARTESIAN_POINT('Ctrl Pts',(-1.00306229115158,35.1006306393371,1.73735485143099));
#7850=CARTESIAN_POINT('Ctrl Pts',(-2.00612458230316,35.0422973060038,1.15823656762066));
#7851=CARTESIAN_POINT('Ctrl Pts',(-2.00612458230317,34.9839639726704,0.));
#7852=CARTESIAN_POINT('Ctrl Pts',(-2.00612458230317,34.9256306393371,-1.15823656762066));
#7853=CARTESIAN_POINT('Ctrl Pts',(-1.00306229115158,34.8672973060038,-1.73735485143099));
#7854=CARTESIAN_POINT('Ctrl Pts',(-1.41843070519206E-16,34.8089639726704,
-2.31647313524132));
#7855=CARTESIAN_POINT('Ctrl Pts',(1.00306229115158,34.7506306393371,-1.73735485143099));
#7856=CARTESIAN_POINT('Ctrl Pts',(2.00612458230317,34.6922973060038,-1.15823656762066));
#7857=CARTESIAN_POINT('Ctrl Pts',(2.00612458230317,34.6339639726704,-2.45679404840839E-16));
#7858=CARTESIAN_POINT('Ctrl Pts',(2.00612458230317,34.5756306393371,1.15823656762066));
#7859=CARTESIAN_POINT('Ctrl Pts',(1.00306229115158,34.5172973060038,1.73735485143099));
#7860=CARTESIAN_POINT('Ctrl Pts',(4.25529211557617E-16,34.4589639726704,
2.31647313524132));
#7861=CARTESIAN_POINT('Ctrl Pts',(-1.00306229115158,34.4006306393371,1.73735485143099));
#7862=CARTESIAN_POINT('Ctrl Pts',(-2.00612458230316,34.3422973060038,1.15823656762066));
#7863=CARTESIAN_POINT('Ctrl Pts',(-2.00612458230317,34.2839639726704,0.));
#7864=CARTESIAN_POINT('Ctrl Pts',(-2.00612458230317,34.2256306393371,-1.15823656762066));
#7865=CARTESIAN_POINT('Ctrl Pts',(-1.00306229115158,34.1672973060038,-1.73735485143099));
#7866=CARTESIAN_POINT('Ctrl Pts',(-1.41843070519206E-16,34.1089639726704,
-2.31647313524132));
#7867=CARTESIAN_POINT('Ctrl Pts',(1.00306229115158,34.0506306393371,-1.73735485143099));
#7868=CARTESIAN_POINT('Ctrl Pts',(2.00612458230317,33.9922973060038,-1.15823656762066));
#7869=CARTESIAN_POINT('Ctrl Pts',(2.00612458230317,33.9339639726704,-2.45679404840839E-16));
#7870=CARTESIAN_POINT('Ctrl Pts',(2.00612458230317,33.8756306393371,1.15823656762066));
#7871=CARTESIAN_POINT('Ctrl Pts',(1.00306229115158,33.8172973060038,1.73735485143099));
#7872=CARTESIAN_POINT('Ctrl Pts',(4.25529211557617E-16,33.7589639726704,
2.31647313524132));
#7873=CARTESIAN_POINT('Ctrl Pts',(-1.00306229115158,33.7006306393371,1.73735485143099));
#7874=CARTESIAN_POINT('Ctrl Pts',(-2.00612458230316,33.6422973060038,1.15823656762066));
#7875=CARTESIAN_POINT('Ctrl Pts',(-2.00612458230317,33.5839639726704,0.));
#7876=CARTESIAN_POINT('Ctrl Pts',(-2.00612458230317,33.5256306393371,-1.15823656762066));
#7877=CARTESIAN_POINT('Ctrl Pts',(-1.00306229115158,33.4672973060038,-1.73735485143099));
#7878=CARTESIAN_POINT('Ctrl Pts',(-1.41843070519206E-16,33.4089639726704,
-2.31647313524132));
#7879=CARTESIAN_POINT('Ctrl Pts',(1.00306229115158,33.3506306393371,-1.73735485143099));
#7880=CARTESIAN_POINT('Ctrl Pts',(2.00612458230317,33.2922973060038,-1.15823656762066));
#7881=CARTESIAN_POINT('Ctrl Pts',(2.00612458230317,33.2339639726704,-2.45679404840839E-16));
#7882=CARTESIAN_POINT('Ctrl Pts',(2.00612458230317,33.1756306393371,1.15823656762066));
#7883=CARTESIAN_POINT('Ctrl Pts',(1.00306229115158,33.1172973060038,1.73735485143099));
#7884=CARTESIAN_POINT('Ctrl Pts',(4.25529211557617E-16,33.0589639726704,
2.31647313524132));
#7885=CARTESIAN_POINT('Ctrl Pts',(-1.00306229115158,33.0006306393371,1.73735485143099));
#7886=CARTESIAN_POINT('Ctrl Pts',(-2.00612458230316,32.9422973060038,1.15823656762066));
#7887=CARTESIAN_POINT('Ctrl Pts',(-2.00612458230317,32.8839639726704,0.));
#7888=CARTESIAN_POINT('Ctrl Pts',(-2.00612458230317,32.8256306393371,-1.15823656762066));
#7889=CARTESIAN_POINT('Ctrl Pts',(-1.00306229115158,32.7672973060038,-1.73735485143099));
#7890=CARTESIAN_POINT('Ctrl Pts',(-1.41843070519206E-16,32.7089639726704,
-2.31647313524132));
#7891=CARTESIAN_POINT('Ctrl Pts',(1.00306229115158,32.6506306393371,-1.73735485143099));
#7892=CARTESIAN_POINT('Ctrl Pts',(2.00612458230317,32.5922973060038,-1.15823656762066));
#7893=CARTESIAN_POINT('Ctrl Pts',(2.00612458230317,32.5339639726704,-2.45679404840839E-16));
#7894=CARTESIAN_POINT('Ctrl Pts',(2.00612458230317,32.4756306393371,1.15823656762066));
#7895=CARTESIAN_POINT('Ctrl Pts',(1.00306229115158,32.4172973060038,1.73735485143099));
#7896=CARTESIAN_POINT('Ctrl Pts',(4.25529211557617E-16,32.3589639726704,
2.31647313524132));
#7897=CARTESIAN_POINT('Ctrl Pts',(-1.00306229115158,32.3006306393371,1.73735485143099));
#7898=CARTESIAN_POINT('Ctrl Pts',(-2.00612458230316,32.2422973060038,1.15823656762066));
#7899=CARTESIAN_POINT('Ctrl Pts',(-2.00612458230317,32.1839639726704,0.));
#7900=CARTESIAN_POINT('Ctrl Pts',(-2.00612458230317,32.1256306393371,-1.15823656762066));
#7901=CARTESIAN_POINT('Ctrl Pts',(-1.00306229115158,32.0672973060038,-1.73735485143099));
#7902=CARTESIAN_POINT('Ctrl Pts',(-1.41843070519206E-16,32.0089639726704,
-2.31647313524132));
#7903=CARTESIAN_POINT('Ctrl Pts',(1.00306229115158,31.9506306393371,-1.73735485143099));
#7904=CARTESIAN_POINT('Ctrl Pts',(2.00612458230317,31.8922973060038,-1.15823656762066));
#7905=CARTESIAN_POINT('Ctrl Pts',(2.00612458230317,31.8339639726704,-2.45679404840839E-16));
#7906=CARTESIAN_POINT('Ctrl Pts',(2.00612458230317,31.7756306393371,1.15823656762066));
#7907=CARTESIAN_POINT('Ctrl Pts',(1.00306229115158,31.7172973060038,1.73735485143099));
#7908=CARTESIAN_POINT('Ctrl Pts',(4.25529211557617E-16,31.6589639726704,
2.31647313524132));
#7909=CARTESIAN_POINT('Ctrl Pts',(-1.00306229115158,31.6006306393371,1.73735485143099));
#7910=CARTESIAN_POINT('Ctrl Pts',(-2.00612458230316,31.5422973060038,1.15823656762066));
#7911=CARTESIAN_POINT('Ctrl Pts',(-2.00612458230317,31.4839639726704,0.));
#7912=CARTESIAN_POINT('Ctrl Pts',(-2.00612458230317,31.4256306393371,-1.15823656762066));
#7913=CARTESIAN_POINT('Ctrl Pts',(-1.00306229115158,31.3672973060038,-1.73735485143099));
#7914=CARTESIAN_POINT('Ctrl Pts',(-1.41843070519206E-16,31.3089639726704,
-2.31647313524132));
#7915=CARTESIAN_POINT('Ctrl Pts',(1.00306229115158,31.2506306393371,-1.73735485143099));
#7916=CARTESIAN_POINT('Ctrl Pts',(2.00612458230317,31.1922973060038,-1.15823656762066));
#7917=CARTESIAN_POINT('Ctrl Pts',(2.00612458230317,31.1339639726704,-2.45679404840839E-16));
#7918=CARTESIAN_POINT('Ctrl Pts',(2.00612458230317,31.0756306393371,1.15823656762066));
#7919=CARTESIAN_POINT('Ctrl Pts',(1.00306229115158,31.0172973060038,1.73735485143099));
#7920=CARTESIAN_POINT('Ctrl Pts',(4.25529211557617E-16,30.9589639726704,
2.31647313524132));
#7921=CARTESIAN_POINT('Ctrl Pts',(-1.00306229115158,30.9006306393371,1.73735485143099));
#7922=CARTESIAN_POINT('Ctrl Pts',(-2.00612458230316,30.8422973060038,1.15823656762066));
#7923=CARTESIAN_POINT('Ctrl Pts',(-2.00612458230317,30.7839639726704,0.));
#7924=CARTESIAN_POINT('Ctrl Pts',(-2.00612458230317,30.7256306393371,-1.15823656762066));
#7925=CARTESIAN_POINT('Ctrl Pts',(-1.00306229115158,30.6672973060038,-1.73735485143099));
#7926=CARTESIAN_POINT('Ctrl Pts',(-1.41843070519206E-16,30.6089639726704,
-2.31647313524132));
#7927=CARTESIAN_POINT('Ctrl Pts',(1.00306229115158,30.5506306393371,-1.73735485143099));
#7928=CARTESIAN_POINT('Ctrl Pts',(2.00612458230317,30.4922973060038,-1.15823656762066));
#7929=CARTESIAN_POINT('Ctrl Pts',(2.00612458230317,30.4339639726704,-2.45679404840839E-16));
#7930=CARTESIAN_POINT('Ctrl Pts',(2.00612458230317,30.3756306393371,1.15823656762066));
#7931=CARTESIAN_POINT('Ctrl Pts',(1.00306229115158,30.3172973060038,1.73735485143099));
#7932=CARTESIAN_POINT('Ctrl Pts',(4.25529211557617E-16,30.2589639726704,
2.31647313524132));
#7933=CARTESIAN_POINT('Ctrl Pts',(-1.00306229115158,30.2006306393371,1.73735485143099));
#7934=CARTESIAN_POINT('Ctrl Pts',(-2.00612458230316,30.1422973060038,1.15823656762066));
#7935=CARTESIAN_POINT('Ctrl Pts',(-2.00612458230317,30.0839639726704,0.));
#7936=CARTESIAN_POINT('Ctrl Pts',(-2.00612458230317,30.0256306393371,-1.15823656762066));
#7937=CARTESIAN_POINT('Ctrl Pts',(-1.00306229115158,29.9672973060038,-1.73735485143099));
#7938=CARTESIAN_POINT('Ctrl Pts',(-1.41843070519206E-16,29.9089639726704,
-2.31647313524132));
#7939=CARTESIAN_POINT('Ctrl Pts',(1.00306229115158,29.8506306393371,-1.73735485143099));
#7940=CARTESIAN_POINT('Ctrl Pts',(2.00612458230317,29.7922973060038,-1.15823656762066));
#7941=CARTESIAN_POINT('Ctrl Pts',(2.00612458230317,29.7339639726704,-2.45679404840839E-16));
#7942=CARTESIAN_POINT('Ctrl Pts',(2.00612458230317,29.6756306393371,1.15823656762066));
#7943=CARTESIAN_POINT('Ctrl Pts',(1.00306229115158,29.6172973060038,1.73735485143099));
#7944=CARTESIAN_POINT('Ctrl Pts',(4.25529211557617E-16,29.5589639726704,
2.31647313524132));
#7945=CARTESIAN_POINT('Ctrl Pts',(-1.00306229115158,29.5006306393371,1.73735485143099));
#7946=CARTESIAN_POINT('Ctrl Pts',(-2.00612458230316,29.4422973060038,1.15823656762066));
#7947=CARTESIAN_POINT('Ctrl Pts',(-2.00612458230317,29.3839639726704,0.));
#7948=CARTESIAN_POINT('Ctrl Pts',(-2.00612458230317,29.3256306393371,-1.15823656762066));
#7949=CARTESIAN_POINT('Ctrl Pts',(-1.00306229115158,29.2672973060038,-1.73735485143099));
#7950=CARTESIAN_POINT('Ctrl Pts',(-1.41843070519206E-16,29.2089639726704,
-2.31647313524132));
#7951=CARTESIAN_POINT('Ctrl Pts',(1.00306229115158,29.1506306393371,-1.73735485143099));
#7952=CARTESIAN_POINT('Ctrl Pts',(2.00612458230317,29.0922973060038,-1.15823656762066));
#7953=CARTESIAN_POINT('Ctrl Pts',(2.00612458230317,29.0339639726704,-2.45679404840839E-16));
#7954=CARTESIAN_POINT('Ctrl Pts',(2.00612458230317,28.9756306393371,1.15823656762066));
#7955=CARTESIAN_POINT('Ctrl Pts',(1.00306229115158,28.9172973060038,1.73735485143099));
#7956=CARTESIAN_POINT('Ctrl Pts',(4.25529211557617E-16,28.8589639726704,
2.31647313524132));
#7957=CARTESIAN_POINT('Ctrl Pts',(-1.00306229115158,28.8006306393371,1.73735485143099));
#7958=CARTESIAN_POINT('Ctrl Pts',(-2.00612458230316,28.7422973060038,1.15823656762066));
#7959=CARTESIAN_POINT('Ctrl Pts',(-2.00612458230317,28.6839639726704,0.));
#7960=CARTESIAN_POINT('Ctrl Pts',(-2.00612458230317,28.6256306393371,-1.15823656762066));
#7961=CARTESIAN_POINT('Ctrl Pts',(-1.00306229115158,28.5672973060038,-1.73735485143099));
#7962=CARTESIAN_POINT('Ctrl Pts',(-1.41843070519206E-16,28.5089639726704,
-2.31647313524132));
#7963=CARTESIAN_POINT('Ctrl Pts',(1.00306229115158,28.4506306393371,-1.73735485143099));
#7964=CARTESIAN_POINT('Ctrl Pts',(2.00612458230317,28.3922973060038,-1.15823656762066));
#7965=CARTESIAN_POINT('Ctrl Pts',(2.00612458230317,28.3339639726704,-2.45679404840839E-16));
#7966=CARTESIAN_POINT('Ctrl Pts',(2.00612458230317,28.2756306393371,1.15823656762066));
#7967=CARTESIAN_POINT('Ctrl Pts',(1.00306229115158,28.2172973060038,1.73735485143099));
#7968=CARTESIAN_POINT('Ctrl Pts',(4.25529211557617E-16,28.1589639726704,
2.31647313524132));
#7969=CARTESIAN_POINT('Ctrl Pts',(-1.00306229115158,28.1006306393371,1.73735485143099));
#7970=CARTESIAN_POINT('Ctrl Pts',(-2.00612458230316,28.0422973060038,1.15823656762066));
#7971=CARTESIAN_POINT('Ctrl Pts',(-2.00612458230317,27.9839639726704,0.));
#7972=CARTESIAN_POINT('Ctrl Pts',(-2.00612458230317,27.9256306393371,-1.15823656762066));
#7973=CARTESIAN_POINT('Ctrl Pts',(-1.00306229115158,27.8672973060038,-1.73735485143099));
#7974=CARTESIAN_POINT('Ctrl Pts',(-1.41843070519206E-16,27.8089639726704,
-2.31647313524132));
#7975=CARTESIAN_POINT('Ctrl Pts',(1.00306229115158,27.7506306393371,-1.73735485143099));
#7976=CARTESIAN_POINT('Ctrl Pts',(2.00612458230317,27.6922973060038,-1.15823656762066));
#7977=CARTESIAN_POINT('Ctrl Pts',(2.00612458230317,27.6339639726704,-2.45679404840839E-16));
#7978=CARTESIAN_POINT('Ctrl Pts',(2.00612458230317,27.5756306393371,1.15823656762066));
#7979=CARTESIAN_POINT('Ctrl Pts',(1.00306229115158,27.5172973060038,1.73735485143099));
#7980=CARTESIAN_POINT('Ctrl Pts',(4.25529211557617E-16,27.4589639726704,
2.31647313524132));
#7981=CARTESIAN_POINT('Ctrl Pts',(-1.00306229115158,27.4006306393371,1.73735485143099));
#7982=CARTESIAN_POINT('Ctrl Pts',(-2.00612458230316,27.3422973060038,1.15823656762066));
#7983=CARTESIAN_POINT('Ctrl Pts',(-2.00612458230317,27.2839639726704,0.));
#7984=CARTESIAN_POINT('Ctrl Pts',(-2.00612458230317,27.2256306393371,-1.15823656762066));
#7985=CARTESIAN_POINT('Ctrl Pts',(-1.00306229115158,27.1672973060038,-1.73735485143099));
#7986=CARTESIAN_POINT('Ctrl Pts',(-1.41843070519206E-16,27.1089639726704,
-2.31647313524132));
#7987=CARTESIAN_POINT('Ctrl Pts',(1.00306229115158,27.0506306393371,-1.73735485143099));
#7988=CARTESIAN_POINT('Ctrl Pts',(2.00612458230317,26.9922973060038,-1.15823656762066));
#7989=CARTESIAN_POINT('Ctrl Pts',(2.00612458230317,26.9339639726704,-2.45679404840839E-16));
#7990=CARTESIAN_POINT('Ctrl Pts',(2.00612458230317,26.8756306393371,1.15823656762066));
#7991=CARTESIAN_POINT('Ctrl Pts',(1.00306229115158,26.8172973060038,1.73735485143099));
#7992=CARTESIAN_POINT('Ctrl Pts',(4.25529211557617E-16,26.7589639726704,
2.31647313524132));
#7993=CARTESIAN_POINT('Ctrl Pts',(-1.00306229115158,26.7006306393371,1.73735485143099));
#7994=CARTESIAN_POINT('Ctrl Pts',(-2.00612458230316,26.6422973060038,1.15823656762066));
#7995=CARTESIAN_POINT('Ctrl Pts',(-2.00612458230317,26.5839639726704,0.));
#7996=CARTESIAN_POINT('Ctrl Pts',(-2.00612458230317,26.5256306393371,-1.15823656762066));
#7997=CARTESIAN_POINT('Ctrl Pts',(-1.00306229115158,26.4672973060038,-1.73735485143099));
#7998=CARTESIAN_POINT('Ctrl Pts',(-1.41843070519206E-16,26.4089639726704,
-2.31647313524132));
#7999=CARTESIAN_POINT('Ctrl Pts',(1.00306229115158,26.3506306393371,-1.73735485143099));
#8000=CARTESIAN_POINT('Ctrl Pts',(2.00612458230317,26.2922973060038,-1.15823656762066));
#8001=CARTESIAN_POINT('Ctrl Pts',(2.00612458230317,26.2339639726704,-2.45679404840839E-16));
#8002=CARTESIAN_POINT('Ctrl Pts',(2.00612458230317,26.1756306393371,1.15823656762066));
#8003=CARTESIAN_POINT('Ctrl Pts',(1.00306229115158,26.1172973060038,1.73735485143099));
#8004=CARTESIAN_POINT('Ctrl Pts',(4.25529211557617E-16,26.0589639726704,
2.31647313524132));
#8005=CARTESIAN_POINT('Ctrl Pts',(-1.00306229115158,26.0006306393371,1.73735485143099));
#8006=CARTESIAN_POINT('Ctrl Pts',(-2.00612458230316,25.9422973060038,1.15823656762066));
#8007=CARTESIAN_POINT('Ctrl Pts',(-2.00612458230317,25.8839639726704,0.));
#8008=CARTESIAN_POINT('Ctrl Pts',(-2.00612458230317,25.8256306393371,-1.15823656762066));
#8009=CARTESIAN_POINT('Ctrl Pts',(-1.00306229115158,25.7672973060038,-1.73735485143099));
#8010=CARTESIAN_POINT('Ctrl Pts',(-1.41843070519206E-16,25.7089639726704,
-2.31647313524132));
#8011=CARTESIAN_POINT('Ctrl Pts',(1.00306229115158,25.6506306393371,-1.73735485143099));
#8012=CARTESIAN_POINT('Ctrl Pts',(2.00612458230317,25.5922973060038,-1.15823656762066));
#8013=CARTESIAN_POINT('Ctrl Pts',(2.00612458230317,25.5339639726704,-2.45679404840839E-16));
#8014=CARTESIAN_POINT('Ctrl Pts',(2.00612458230317,25.4756306393371,1.15823656762066));
#8015=CARTESIAN_POINT('Ctrl Pts',(1.00306229115158,25.4172973060038,1.73735485143099));
#8016=CARTESIAN_POINT('Ctrl Pts',(4.25529211557617E-16,25.3589639726704,
2.31647313524132));
#8017=CARTESIAN_POINT('Ctrl Pts',(-1.00306229115158,25.3006306393371,1.73735485143099));
#8018=CARTESIAN_POINT('Ctrl Pts',(-2.00612458230316,25.2422973060038,1.15823656762066));
#8019=CARTESIAN_POINT('Ctrl Pts',(-2.00612458230317,25.1839639726704,0.));
#8020=CARTESIAN_POINT('Ctrl Pts',(-2.00612458230317,25.1256306393371,-1.15823656762066));
#8021=CARTESIAN_POINT('Ctrl Pts',(-1.00306229115158,25.0672973060038,-1.73735485143099));
#8022=CARTESIAN_POINT('Ctrl Pts',(-1.41843070519206E-16,25.0089639726704,
-2.31647313524132));
#8023=CARTESIAN_POINT('Ctrl Pts',(1.00306229115158,24.9506306393371,-1.73735485143099));
#8024=CARTESIAN_POINT('Ctrl Pts',(2.00612458230317,24.8922973060038,-1.15823656762066));
#8025=CARTESIAN_POINT('Ctrl Pts',(2.00612458230317,24.8339639726704,-2.45679404840839E-16));
#8026=CARTESIAN_POINT('Ctrl Pts',(2.00612458230317,24.7756306393371,1.15823656762066));
#8027=CARTESIAN_POINT('Ctrl Pts',(1.00306229115158,24.7172973060038,1.73735485143099));
#8028=CARTESIAN_POINT('Ctrl Pts',(4.25529211557617E-16,24.6589639726704,
2.31647313524132));
#8029=CARTESIAN_POINT('Ctrl Pts',(-1.00306229115158,24.6006306393371,1.73735485143099));
#8030=CARTESIAN_POINT('Ctrl Pts',(-2.00612458230316,24.5422973060038,1.15823656762066));
#8031=CARTESIAN_POINT('Ctrl Pts',(-2.00612458230317,24.4839639726704,0.));
#8032=CARTESIAN_POINT('Ctrl Pts',(-2.00612458230317,24.4256306393371,-1.15823656762066));
#8033=CARTESIAN_POINT('Ctrl Pts',(-1.00306229115158,24.3672973060038,-1.73735485143099));
#8034=CARTESIAN_POINT('Ctrl Pts',(-1.41843070519206E-16,24.3089639726704,
-2.31647313524132));
#8035=CARTESIAN_POINT('Ctrl Pts',(1.00306229115158,24.2506306393371,-1.73735485143099));
#8036=CARTESIAN_POINT('Ctrl Pts',(2.00612458230317,24.1922973060038,-1.15823656762066));
#8037=CARTESIAN_POINT('Ctrl Pts',(2.00612458230317,24.1339639726704,-2.45679404840839E-16));
#8038=CARTESIAN_POINT('Ctrl Pts',(2.00612458230317,24.0756306393371,1.15823656762066));
#8039=CARTESIAN_POINT('Ctrl Pts',(1.00306229115158,24.0172973060038,1.73735485143099));
#8040=CARTESIAN_POINT('Ctrl Pts',(4.25529211557617E-16,23.9589639726704,
2.31647313524132));
#8041=CARTESIAN_POINT('Ctrl Pts',(-1.00306229115158,23.9006306393371,1.73735485143099));
#8042=CARTESIAN_POINT('Ctrl Pts',(-2.00612458230316,23.8422973060038,1.15823656762066));
#8043=CARTESIAN_POINT('Ctrl Pts',(-2.00612458230317,23.7839639726704,0.));
#8044=CARTESIAN_POINT('Ctrl Pts',(-2.00612458230317,23.7256306393371,-1.15823656762066));
#8045=CARTESIAN_POINT('Ctrl Pts',(-1.00306229115158,23.6672973060038,-1.73735485143099));
#8046=CARTESIAN_POINT('Ctrl Pts',(-1.41843070519206E-16,23.6089639726704,
-2.31647313524132));
#8047=CARTESIAN_POINT('Ctrl Pts',(1.00306229115158,23.5506306393371,-1.73735485143099));
#8048=CARTESIAN_POINT('Ctrl Pts',(2.00612458230317,23.4922973060038,-1.15823656762066));
#8049=CARTESIAN_POINT('Ctrl Pts',(2.00612458230317,23.4339639726704,-2.45679404840839E-16));
#8050=CARTESIAN_POINT('Ctrl Pts',(2.00612458230317,23.3756306393371,1.15823656762066));
#8051=CARTESIAN_POINT('Ctrl Pts',(1.00306229115158,23.3172973060038,1.73735485143099));
#8052=CARTESIAN_POINT('Ctrl Pts',(4.25529211557617E-16,23.2589639726704,
2.31647313524132));
#8053=CARTESIAN_POINT('Ctrl Pts',(-1.00306229115158,23.2006306393371,1.73735485143099));
#8054=CARTESIAN_POINT('Ctrl Pts',(-2.00612458230316,23.1422973060038,1.15823656762066));
#8055=CARTESIAN_POINT('Ctrl Pts',(-2.00612458230317,23.0839639726704,0.));
#8056=CARTESIAN_POINT('Ctrl Pts',(-2.00612458230317,23.0256306393371,-1.15823656762066));
#8057=CARTESIAN_POINT('Ctrl Pts',(-1.00306229115158,22.9672973060038,-1.73735485143099));
#8058=CARTESIAN_POINT('Ctrl Pts',(-1.41843070519206E-16,22.9089639726704,
-2.31647313524132));
#8059=CARTESIAN_POINT('Ctrl Pts',(1.00306229115158,22.8506306393371,-1.73735485143099));
#8060=CARTESIAN_POINT('Ctrl Pts',(2.00612458230317,22.7922973060038,-1.15823656762066));
#8061=CARTESIAN_POINT('Ctrl Pts',(2.00612458230317,22.7339639726704,-2.45679404840839E-16));
#8062=CARTESIAN_POINT('Ctrl Pts',(2.00612458230317,22.6756306393371,1.15823656762066));
#8063=CARTESIAN_POINT('Ctrl Pts',(1.00306229115158,22.6172973060038,1.73735485143099));
#8064=CARTESIAN_POINT('Ctrl Pts',(4.25529211557617E-16,22.5589639726704,
2.31647313524132));
#8065=CARTESIAN_POINT('Ctrl Pts',(-1.00306229115158,22.5006306393371,1.73735485143099));
#8066=CARTESIAN_POINT('Ctrl Pts',(-2.00612458230316,22.4422973060038,1.15823656762066));
#8067=CARTESIAN_POINT('Ctrl Pts',(-2.00612458230317,22.3839639726704,0.));
#8068=CARTESIAN_POINT('Ctrl Pts',(-2.00612458230317,22.3256306393371,-1.15823656762066));
#8069=CARTESIAN_POINT('Ctrl Pts',(-1.00306229115158,22.2672973060038,-1.73735485143099));
#8070=CARTESIAN_POINT('Ctrl Pts',(-1.41843070519206E-16,22.2089639726704,
-2.31647313524132));
#8071=CARTESIAN_POINT('Ctrl Pts',(1.00306229115158,22.1506306393371,-1.73735485143099));
#8072=CARTESIAN_POINT('Ctrl Pts',(2.00612458230317,22.0922973060038,-1.15823656762066));
#8073=CARTESIAN_POINT('Ctrl Pts',(2.00612458230317,22.0339639726704,-2.45679404840839E-16));
#8074=CARTESIAN_POINT('Ctrl Pts',(2.00612458230317,21.9756306393371,1.15823656762066));
#8075=CARTESIAN_POINT('Ctrl Pts',(1.00306229115158,21.9172973060038,1.73735485143099));
#8076=CARTESIAN_POINT('Ctrl Pts',(4.25529211557617E-16,21.8589639726704,
2.31647313524132));
#8077=CARTESIAN_POINT('Ctrl Pts',(-1.00306229115158,21.8006306393371,1.73735485143099));
#8078=CARTESIAN_POINT('Ctrl Pts',(-2.00612458230316,21.7422973060038,1.15823656762066));
#8079=CARTESIAN_POINT('Ctrl Pts',(-2.00612458230317,21.6839639726704,0.));
#8080=CARTESIAN_POINT('Ctrl Pts',(-2.00612458230317,21.6256306393371,-1.15823656762066));
#8081=CARTESIAN_POINT('Ctrl Pts',(-1.00306229115158,21.5672973060038,-1.73735485143099));
#8082=CARTESIAN_POINT('Ctrl Pts',(-1.41843070519206E-16,21.5089639726704,
-2.31647313524132));
#8083=CARTESIAN_POINT('Ctrl Pts',(1.00306229115158,21.4506306393371,-1.73735485143099));
#8084=CARTESIAN_POINT('Ctrl Pts',(2.00612458230317,21.3922973060038,-1.15823656762066));
#8085=CARTESIAN_POINT('Ctrl Pts',(2.00612458230317,21.3339639726704,-2.45679404840839E-16));
#8086=CARTESIAN_POINT('Ctrl Pts',(2.00612458230317,21.2756306393371,1.15823656762066));
#8087=CARTESIAN_POINT('Ctrl Pts',(1.00306229115158,21.2172973060038,1.73735485143099));
#8088=CARTESIAN_POINT('Ctrl Pts',(4.25529211557617E-16,21.1589639726704,
2.31647313524132));
#8089=CARTESIAN_POINT('Ctrl Pts',(-1.00306229115158,21.1006306393371,1.73735485143099));
#8090=CARTESIAN_POINT('Ctrl Pts',(-2.00612458230316,21.0422973060038,1.15823656762066));
#8091=CARTESIAN_POINT('Ctrl Pts',(-2.00612458230317,20.9839639726704,0.));
#8092=CARTESIAN_POINT('Ctrl Pts',(-2.00612458230317,20.9256306393371,-1.15823656762066));
#8093=CARTESIAN_POINT('Ctrl Pts',(-1.00306229115158,20.8672973060038,-1.73735485143099));
#8094=CARTESIAN_POINT('Ctrl Pts',(-1.41843070519206E-16,20.8089639726704,
-2.31647313524132));
#8095=CARTESIAN_POINT('Ctrl Pts',(1.00306229115158,20.7506306393371,-1.73735485143099));
#8096=CARTESIAN_POINT('Ctrl Pts',(2.00612458230317,20.6922973060038,-1.15823656762066));
#8097=CARTESIAN_POINT('Ctrl Pts',(2.00612458230317,20.6339639726704,-2.45679404840839E-16));
#8098=CARTESIAN_POINT('Ctrl Pts',(2.00612458230317,20.5756306393371,1.15823656762066));
#8099=CARTESIAN_POINT('Ctrl Pts',(1.00306229115158,20.5172973060038,1.73735485143099));
#8100=CARTESIAN_POINT('Ctrl Pts',(4.25529211557617E-16,20.4589639726704,
2.31647313524132));
#8101=CARTESIAN_POINT('Ctrl Pts',(-1.00306229115158,20.4006306393371,1.73735485143099));
#8102=CARTESIAN_POINT('Ctrl Pts',(-2.00612458230316,20.3422973060038,1.15823656762066));
#8103=CARTESIAN_POINT('Ctrl Pts',(-2.00612458230317,20.2839639726704,0.));
#8104=CARTESIAN_POINT('Ctrl Pts',(-2.00612458230317,20.2256306393371,-1.15823656762066));
#8105=CARTESIAN_POINT('Ctrl Pts',(-1.00306229115158,20.1672973060038,-1.73735485143099));
#8106=CARTESIAN_POINT('Ctrl Pts',(-1.41843070519206E-16,20.1089639726704,
-2.31647313524132));
#8107=CARTESIAN_POINT('Ctrl Pts',(1.00306229115158,20.0506306393371,-1.73735485143099));
#8108=CARTESIAN_POINT('Ctrl Pts',(2.00612458230317,19.9922973060038,-1.15823656762066));
#8109=CARTESIAN_POINT('Ctrl Pts',(2.00612458230317,19.9339639726704,-2.45679404840839E-16));
#8110=CARTESIAN_POINT('Ctrl Pts',(2.00612458230317,19.8756306393371,1.15823656762066));
#8111=CARTESIAN_POINT('Ctrl Pts',(1.00306229115158,19.8172973060038,1.73735485143099));
#8112=CARTESIAN_POINT('Ctrl Pts',(4.25529211557617E-16,19.7589639726704,
2.31647313524132));
#8113=CARTESIAN_POINT('Ctrl Pts',(-1.00306229115158,19.7006306393371,1.73735485143099));
#8114=CARTESIAN_POINT('Ctrl Pts',(-2.00612458230316,19.6422973060038,1.15823656762066));
#8115=CARTESIAN_POINT('Ctrl Pts',(-2.00612458230317,19.5839639726704,0.));
#8116=CARTESIAN_POINT('Ctrl Pts',(-2.00612458230317,19.5256306393371,-1.15823656762066));
#8117=CARTESIAN_POINT('Ctrl Pts',(-1.00306229115158,19.4672973060038,-1.73735485143099));
#8118=CARTESIAN_POINT('Ctrl Pts',(-1.41843070519206E-16,19.4089639726704,
-2.31647313524132));
#8119=CARTESIAN_POINT('Ctrl Pts',(1.00306229115158,19.3506306393371,-1.73735485143099));
#8120=CARTESIAN_POINT('Ctrl Pts',(2.00612458230317,19.2922973060038,-1.15823656762066));
#8121=CARTESIAN_POINT('Ctrl Pts',(2.00612458230317,19.2339639726704,-2.45679404840839E-16));
#8122=CARTESIAN_POINT('Ctrl Pts',(2.00612458230317,19.1756306393371,1.15823656762066));
#8123=CARTESIAN_POINT('Ctrl Pts',(1.00306229115158,19.1172973060038,1.73735485143099));
#8124=CARTESIAN_POINT('Ctrl Pts',(4.25529211557617E-16,19.0589639726704,
2.31647313524132));
#8125=CARTESIAN_POINT('Ctrl Pts',(-1.00306229115158,19.0006306393371,1.73735485143099));
#8126=CARTESIAN_POINT('Ctrl Pts',(-2.00612458230316,18.9422973060038,1.15823656762066));
#8127=CARTESIAN_POINT('Ctrl Pts',(-2.00612458230317,18.8839639726704,0.));
#8128=CARTESIAN_POINT('Ctrl Pts',(-2.00612458230317,18.8256306393371,-1.15823656762066));
#8129=CARTESIAN_POINT('Ctrl Pts',(-1.00306229115158,18.7672973060038,-1.73735485143099));
#8130=CARTESIAN_POINT('Ctrl Pts',(-1.41843070519206E-16,18.7089639726704,
-2.31647313524132));
#8131=CARTESIAN_POINT('Ctrl Pts',(1.00306229115158,18.6506306393371,-1.73735485143099));
#8132=CARTESIAN_POINT('Ctrl Pts',(2.00612458230317,18.5922973060038,-1.15823656762066));
#8133=CARTESIAN_POINT('Ctrl Pts',(2.00612458230317,18.5339639726704,-2.45679404840839E-16));
#8134=CARTESIAN_POINT('Ctrl Pts',(2.00612458230317,18.4756306393371,1.15823656762066));
#8135=CARTESIAN_POINT('Ctrl Pts',(1.00306229115158,18.4172973060038,1.73735485143099));
#8136=CARTESIAN_POINT('Ctrl Pts',(4.25529211557617E-16,18.3589639726704,
2.31647313524132));
#8137=CARTESIAN_POINT('Ctrl Pts',(-1.00306229115158,18.3006306393371,1.73735485143099));
#8138=CARTESIAN_POINT('Ctrl Pts',(-2.00612458230316,18.2422973060038,1.15823656762066));
#8139=CARTESIAN_POINT('Ctrl Pts',(-2.00612458230317,18.1839639726704,0.));
#8140=CARTESIAN_POINT('Ctrl Pts',(-2.00612458230317,18.1256306393371,-1.15823656762066));
#8141=CARTESIAN_POINT('Ctrl Pts',(-1.00306229115158,18.0672973060038,-1.73735485143099));
#8142=CARTESIAN_POINT('Ctrl Pts',(-1.41843070519206E-16,18.0089639726704,
-2.31647313524132));
#8143=CARTESIAN_POINT('Ctrl Pts',(1.00306229115158,17.9506306393371,-1.73735485143099));
#8144=CARTESIAN_POINT('Ctrl Pts',(2.00612458230317,17.8922973060038,-1.15823656762066));
#8145=CARTESIAN_POINT('Ctrl Pts',(2.00612458230317,17.8339639726704,-2.45679404840839E-16));
#8146=CARTESIAN_POINT('Ctrl Pts',(2.00612458230317,17.7756306393371,1.15823656762066));
#8147=CARTESIAN_POINT('Ctrl Pts',(1.00306229115158,17.7172973060038,1.73735485143099));
#8148=CARTESIAN_POINT('Ctrl Pts',(4.25529211557617E-16,17.6589639726704,
2.31647313524132));
#8149=CARTESIAN_POINT('Ctrl Pts',(-1.00306229115158,17.6006306393371,1.73735485143099));
#8150=CARTESIAN_POINT('Ctrl Pts',(-2.00612458230316,17.5422973060038,1.15823656762066));
#8151=CARTESIAN_POINT('Ctrl Pts',(-2.00612458230317,17.4839639726704,0.));
#8152=CARTESIAN_POINT('Ctrl Pts',(-2.00612458230317,17.4256306393371,-1.15823656762066));
#8153=CARTESIAN_POINT('Ctrl Pts',(-1.00306229115158,17.3672973060038,-1.73735485143099));
#8154=CARTESIAN_POINT('Ctrl Pts',(-1.41843070519206E-16,17.3089639726704,
-2.31647313524132));
#8155=CARTESIAN_POINT('Ctrl Pts',(1.00306229115158,17.2506306393371,-1.73735485143099));
#8156=CARTESIAN_POINT('Ctrl Pts',(2.00612458230317,17.1922973060038,-1.15823656762066));
#8157=CARTESIAN_POINT('Ctrl Pts',(2.00612458230317,17.1339639726704,-2.45679404840839E-16));
#8158=CARTESIAN_POINT('Ctrl Pts',(2.00612458230317,17.0756306393371,1.15823656762066));
#8159=CARTESIAN_POINT('Ctrl Pts',(1.00306229115158,17.0172973060038,1.73735485143099));
#8160=CARTESIAN_POINT('Ctrl Pts',(4.25529211557617E-16,16.9589639726704,
2.31647313524132));
#8161=CARTESIAN_POINT('Ctrl Pts',(-1.00306229115158,16.9006306393371,1.73735485143099));
#8162=CARTESIAN_POINT('Ctrl Pts',(-2.00612458230316,16.8422973060038,1.15823656762066));
#8163=CARTESIAN_POINT('Ctrl Pts',(-2.00612458230317,16.7839639726704,0.));
#8164=CARTESIAN_POINT('Ctrl Pts',(-2.00612458230317,16.7256306393371,-1.15823656762066));
#8165=CARTESIAN_POINT('Ctrl Pts',(-1.00306229115158,16.6672973060038,-1.73735485143099));
#8166=CARTESIAN_POINT('Ctrl Pts',(-1.41843070519206E-16,16.6089639726704,
-2.31647313524132));
#8167=CARTESIAN_POINT('Ctrl Pts',(1.00306229115158,16.5506306393371,-1.73735485143099));
#8168=CARTESIAN_POINT('Ctrl Pts',(2.00612458230317,16.4922973060038,-1.15823656762066));
#8169=CARTESIAN_POINT('Ctrl Pts',(2.00612458230317,16.4339639726704,-2.45679404840839E-16));
#8170=CARTESIAN_POINT('Ctrl Pts',(2.00612458230317,16.3756306393371,1.15823656762066));
#8171=CARTESIAN_POINT('Ctrl Pts',(1.00306229115158,16.3172973060038,1.73735485143099));
#8172=CARTESIAN_POINT('Ctrl Pts',(4.25529211557617E-16,16.2589639726704,
2.31647313524132));
#8173=CARTESIAN_POINT('Ctrl Pts',(-1.00306229115158,16.2006306393371,1.73735485143099));
#8174=CARTESIAN_POINT('Ctrl Pts',(-2.00612458230316,16.1422973060038,1.15823656762066));
#8175=CARTESIAN_POINT('Ctrl Pts',(-2.00612458230317,16.0839639726704,0.));
#8176=CARTESIAN_POINT('Ctrl Pts',(-2.00612458230317,16.0256306393371,-1.15823656762066));
#8177=CARTESIAN_POINT('Ctrl Pts',(-1.00306229115158,15.9672973060038,-1.73735485143099));
#8178=CARTESIAN_POINT('Ctrl Pts',(-1.41843070519206E-16,15.9089639726704,
-2.31647313524132));
#8179=CARTESIAN_POINT('Ctrl Pts',(1.00306229115158,15.8506306393371,-1.73735485143099));
#8180=CARTESIAN_POINT('Ctrl Pts',(2.00612458230317,15.7922973060038,-1.15823656762066));
#8181=CARTESIAN_POINT('Ctrl Pts',(2.00612458230317,15.7339639726704,-2.45679404840839E-16));
#8182=CARTESIAN_POINT('Ctrl Pts',(2.00612458230317,15.6756306393371,1.15823656762066));
#8183=CARTESIAN_POINT('Ctrl Pts',(1.00306229115158,15.6172973060038,1.73735485143099));
#8184=CARTESIAN_POINT('Ctrl Pts',(4.25529211557617E-16,15.5589639726704,
2.31647313524132));
#8185=CARTESIAN_POINT('Ctrl Pts',(-1.00306229115158,15.5006306393371,1.73735485143099));
#8186=CARTESIAN_POINT('Ctrl Pts',(-2.00612458230316,15.4422973060038,1.15823656762066));
#8187=CARTESIAN_POINT('Ctrl Pts',(-2.00612458230317,15.3839639726704,0.));
#8188=CARTESIAN_POINT('Ctrl Pts',(-2.00612458230317,15.3256306393371,-1.15823656762066));
#8189=CARTESIAN_POINT('Ctrl Pts',(-1.00306229115158,15.2672973060038,-1.73735485143099));
#8190=CARTESIAN_POINT('Ctrl Pts',(-1.41843070519206E-16,15.2089639726704,
-2.31647313524132));
#8191=CARTESIAN_POINT('Ctrl Pts',(1.00306229115158,15.1506306393371,-1.73735485143099));
#8192=CARTESIAN_POINT('Ctrl Pts',(2.00612458230317,15.0922973060038,-1.15823656762066));
#8193=CARTESIAN_POINT('Ctrl Pts',(2.00612458230317,15.0339639726704,-2.45679404840839E-16));
#8194=CARTESIAN_POINT('Ctrl Pts',(2.00612458230317,14.9756306393371,1.15823656762066));
#8195=CARTESIAN_POINT('Ctrl Pts',(1.00306229115158,14.9172973060038,1.73735485143099));
#8196=CARTESIAN_POINT('Ctrl Pts',(4.25529211557617E-16,14.8589639726704,
2.31647313524132));
#8197=CARTESIAN_POINT('Ctrl Pts',(-1.00306229115158,14.8006306393371,1.73735485143099));
#8198=CARTESIAN_POINT('Ctrl Pts',(-2.00612458230316,14.7422973060038,1.15823656762066));
#8199=CARTESIAN_POINT('Ctrl Pts',(-2.00612458230317,14.6839639726704,0.));
#8200=CARTESIAN_POINT('Ctrl Pts',(-2.00612458230317,14.6256306393371,-1.15823656762066));
#8201=CARTESIAN_POINT('Ctrl Pts',(-1.00306229115158,14.5672973060038,-1.73735485143099));
#8202=CARTESIAN_POINT('Ctrl Pts',(-1.41843070519206E-16,14.5089639726704,
-2.31647313524132));
#8203=CARTESIAN_POINT('Ctrl Pts',(1.00306229115158,14.4506306393371,-1.73735485143099));
#8204=CARTESIAN_POINT('Ctrl Pts',(2.00612458230317,14.3922973060038,-1.15823656762066));
#8205=CARTESIAN_POINT('Ctrl Pts',(2.00612458230317,14.3339639726704,-2.45679404840839E-16));
#8206=CARTESIAN_POINT('Ctrl Pts',(2.00612458230317,14.2756306393371,1.15823656762066));
#8207=CARTESIAN_POINT('Ctrl Pts',(1.00306229115158,14.2172973060038,1.73735485143099));
#8208=CARTESIAN_POINT('Ctrl Pts',(4.25529211557617E-16,14.1589639726704,
2.31647313524132));
#8209=CARTESIAN_POINT('Ctrl Pts',(-1.00306229115158,14.1006306393371,1.73735485143099));
#8210=CARTESIAN_POINT('Ctrl Pts',(-2.00612458230316,14.0422973060038,1.15823656762066));
#8211=CARTESIAN_POINT('Ctrl Pts',(-2.00612458230317,13.9839639726704,0.));
#8212=CARTESIAN_POINT('Ctrl Pts',(-2.00612458230317,13.9256306393371,-1.15823656762066));
#8213=CARTESIAN_POINT('Ctrl Pts',(-1.00306229115158,13.8672973060038,-1.73735485143099));
#8214=CARTESIAN_POINT('Ctrl Pts',(-1.41843070519206E-16,13.8089639726704,
-2.31647313524132));
#8215=CARTESIAN_POINT('Ctrl Pts',(1.00306229115158,13.7506306393371,-1.73735485143099));
#8216=CARTESIAN_POINT('Ctrl Pts',(2.00612458230317,13.6922973060038,-1.15823656762066));
#8217=CARTESIAN_POINT('Ctrl Pts',(2.00612458230317,13.6339639726704,-2.45679404840839E-16));
#8218=CARTESIAN_POINT('Ctrl Pts',(2.00612458230317,13.5756306393371,1.15823656762066));
#8219=CARTESIAN_POINT('Ctrl Pts',(1.00306229115158,13.5172973060038,1.73735485143099));
#8220=CARTESIAN_POINT('Ctrl Pts',(4.25529211557617E-16,13.4589639726704,
2.31647313524132));
#8221=CARTESIAN_POINT('Ctrl Pts',(-1.00306229115158,13.4006306393371,1.73735485143099));
#8222=CARTESIAN_POINT('Ctrl Pts',(-2.00612458230316,13.3422973060038,1.15823656762066));
#8223=CARTESIAN_POINT('Ctrl Pts',(-2.00612458230317,13.2839639726704,0.));
#8224=CARTESIAN_POINT('Ctrl Pts',(-2.00612458230317,13.2256306393371,-1.15823656762066));
#8225=CARTESIAN_POINT('Ctrl Pts',(-1.00306229115158,13.1672973060038,-1.73735485143099));
#8226=CARTESIAN_POINT('Ctrl Pts',(-1.41843070519206E-16,13.1089639726704,
-2.31647313524132));
#8227=CARTESIAN_POINT('Ctrl Pts',(1.00306229115158,13.0506306393371,-1.73735485143099));
#8228=CARTESIAN_POINT('Ctrl Pts',(2.00612458230317,12.9922973060038,-1.15823656762066));
#8229=CARTESIAN_POINT('Ctrl Pts',(2.00612458230317,12.9339639726704,-2.45679404840839E-16));
#8230=CARTESIAN_POINT('Ctrl Pts',(2.00612458230317,12.8756306393371,1.15823656762066));
#8231=CARTESIAN_POINT('Ctrl Pts',(1.00306229115158,12.8172973060038,1.73735485143099));
#8232=CARTESIAN_POINT('Ctrl Pts',(4.25529211557617E-16,12.7589639726704,
2.31647313524132));
#8233=CARTESIAN_POINT('Ctrl Pts',(-1.00306229115158,12.7006306393371,1.73735485143099));
#8234=CARTESIAN_POINT('Ctrl Pts',(-2.00612458230316,12.6422973060038,1.15823656762066));
#8235=CARTESIAN_POINT('Ctrl Pts',(-2.00612458230317,12.5839639726704,0.));
#8236=CARTESIAN_POINT('Ctrl Pts',(-2.00612458230317,12.5256306393371,-1.15823656762066));
#8237=CARTESIAN_POINT('Ctrl Pts',(-1.00306229115158,12.4672973060038,-1.73735485143099));
#8238=CARTESIAN_POINT('Ctrl Pts',(-1.41843070519206E-16,12.4089639726704,
-2.31647313524132));
#8239=CARTESIAN_POINT('Ctrl Pts',(1.00306229115158,12.3506306393371,-1.73735485143099));
#8240=CARTESIAN_POINT('Ctrl Pts',(2.00612458230317,12.2922973060038,-1.15823656762066));
#8241=CARTESIAN_POINT('Ctrl Pts',(2.00612458230317,12.2339639726704,-2.45679404840839E-16));
#8242=CARTESIAN_POINT('Ctrl Pts',(2.00612458230317,12.1756306393371,1.15823656762066));
#8243=CARTESIAN_POINT('Ctrl Pts',(1.00306229115158,12.1172973060038,1.73735485143099));
#8244=CARTESIAN_POINT('Ctrl Pts',(4.25529211557617E-16,12.0589639726704,
2.31647313524132));
#8245=CARTESIAN_POINT('Ctrl Pts',(-1.00306229115158,12.0006306393371,1.73735485143099));
#8246=CARTESIAN_POINT('Ctrl Pts',(-2.00612458230316,11.9422973060038,1.15823656762066));
#8247=CARTESIAN_POINT('Ctrl Pts',(-2.00612458230317,11.8839639726704,0.));
#8248=CARTESIAN_POINT('Ctrl Pts',(-2.00612458230317,11.8256306393371,-1.15823656762066));
#8249=CARTESIAN_POINT('Ctrl Pts',(-1.00306229115158,11.7672973060038,-1.73735485143099));
#8250=CARTESIAN_POINT('Ctrl Pts',(-1.41843070519206E-16,11.7089639726704,
-2.31647313524132));
#8251=CARTESIAN_POINT('Ctrl Pts',(1.00306229115158,11.6506306393371,-1.73735485143099));
#8252=CARTESIAN_POINT('Ctrl Pts',(2.00612458230317,11.5922973060038,-1.15823656762066));
#8253=CARTESIAN_POINT('Ctrl Pts',(2.00612458230317,11.5339639726704,-2.45679404840839E-16));
#8254=CARTESIAN_POINT('Ctrl Pts',(2.00612458230317,11.4756306393371,1.15823656762066));
#8255=CARTESIAN_POINT('Ctrl Pts',(1.00306229115158,11.4172973060038,1.73735485143099));
#8256=CARTESIAN_POINT('Ctrl Pts',(4.25529211557617E-16,11.3589639726704,
2.31647313524132));
#8257=CARTESIAN_POINT('Ctrl Pts',(-1.00306229115158,11.3006306393371,1.73735485143099));
#8258=CARTESIAN_POINT('Ctrl Pts',(-2.00612458230316,11.2422973060038,1.15823656762066));
#8259=CARTESIAN_POINT('Ctrl Pts',(-2.00612458230317,11.1839639726704,0.));
#8260=CARTESIAN_POINT('Ctrl Pts',(-2.00612458230317,11.1256306393371,-1.15823656762066));
#8261=CARTESIAN_POINT('Ctrl Pts',(-1.00306229115158,11.0672973060038,-1.73735485143099));
#8262=CARTESIAN_POINT('Ctrl Pts',(-1.41843070519206E-16,11.0089639726704,
-2.31647313524132));
#8263=CARTESIAN_POINT('Ctrl Pts',(1.00306229115158,10.9506306393371,-1.73735485143099));
#8264=CARTESIAN_POINT('Ctrl Pts',(2.00612458230317,10.8922973060038,-1.15823656762066));
#8265=CARTESIAN_POINT('Ctrl Pts',(2.00612458230317,10.8339639726704,-2.45679404840839E-16));
#8266=CARTESIAN_POINT('Ctrl Pts',(2.00612458230317,10.7756306393371,1.15823656762066));
#8267=CARTESIAN_POINT('Ctrl Pts',(1.00306229115158,10.7172973060038,1.73735485143099));
#8268=CARTESIAN_POINT('Ctrl Pts',(4.25529211557617E-16,10.6589639726704,
2.31647313524132));
#8269=CARTESIAN_POINT('Ctrl Pts',(-1.00306229115158,10.6006306393371,1.73735485143099));
#8270=CARTESIAN_POINT('Ctrl Pts',(-2.00612458230316,10.5422973060038,1.15823656762066));
#8271=CARTESIAN_POINT('Ctrl Pts',(-2.00612458230317,10.4839639726704,0.));
#8272=CARTESIAN_POINT('Ctrl Pts',(-2.00612458230317,10.4256306393371,-1.15823656762066));
#8273=CARTESIAN_POINT('Ctrl Pts',(-1.00306229115158,10.3672973060038,-1.73735485143099));
#8274=CARTESIAN_POINT('Ctrl Pts',(-1.41843070519206E-16,10.3089639726704,
-2.31647313524132));
#8275=CARTESIAN_POINT('Ctrl Pts',(1.00306229115158,10.2506306393371,-1.73735485143099));
#8276=CARTESIAN_POINT('Ctrl Pts',(2.00612458230317,10.1922973060038,-1.15823656762066));
#8277=CARTESIAN_POINT('Ctrl Pts',(2.00612458230317,10.1339639726704,-2.45679404840839E-16));
#8278=CARTESIAN_POINT('Ctrl Pts',(2.00612458230317,10.0756306393371,1.15823656762066));
#8279=CARTESIAN_POINT('Ctrl Pts',(1.00306229115158,10.0172973060038,1.73735485143099));
#8280=CARTESIAN_POINT('Ctrl Pts',(4.25529211557617E-16,9.95896397267043,
2.31647313524132));
#8281=CARTESIAN_POINT('Ctrl Pts',(-1.00306229115158,9.9006306393371,1.73735485143099));
#8282=CARTESIAN_POINT('Ctrl Pts',(-2.00612458230316,9.84229730600376,1.15823656762066));
#8283=CARTESIAN_POINT('Ctrl Pts',(-2.00612458230317,9.78396397267043,0.));
#8284=CARTESIAN_POINT('Ctrl Pts',(-2.00612458230317,9.7256306393371,-1.15823656762066));
#8285=CARTESIAN_POINT('Ctrl Pts',(-1.00306229115158,9.66729730600377,-1.73735485143099));
#8286=CARTESIAN_POINT('Ctrl Pts',(-1.41843070519206E-16,9.60896397267043,
-2.31647313524132));
#8287=CARTESIAN_POINT('Ctrl Pts',(1.00306229115158,9.5506306393371,-1.73735485143099));
#8288=CARTESIAN_POINT('Ctrl Pts',(2.00612458230317,9.49229730600377,-1.15823656762066));
#8289=CARTESIAN_POINT('Ctrl Pts',(2.00612458230317,9.43396397267043,-2.45679404840839E-16));
#8290=CARTESIAN_POINT('Ctrl Pts',(2.00612458230317,9.3756306393371,1.15823656762066));
#8291=CARTESIAN_POINT('Ctrl Pts',(1.00306229115158,9.31729730600377,1.73735485143099));
#8292=CARTESIAN_POINT('Ctrl Pts',(4.25529211557617E-16,9.25896397267043,
2.31647313524132));
#8293=CARTESIAN_POINT('Ctrl Pts',(-1.00306229115158,9.2006306393371,1.73735485143099));
#8294=CARTESIAN_POINT('Ctrl Pts',(-2.00612458230316,9.14229730600376,1.15823656762066));
#8295=CARTESIAN_POINT('Ctrl Pts',(-2.00612458230317,9.08396397267043,0.));
#8296=CARTESIAN_POINT('Ctrl Pts',(-2.00612458230317,9.0256306393371,-1.15823656762066));
#8297=CARTESIAN_POINT('Ctrl Pts',(-1.00306229115158,8.96729730600376,-1.73735485143099));
#8298=CARTESIAN_POINT('Ctrl Pts',(-1.41843070519206E-16,8.90896397267043,
-2.31647313524132));
#8299=CARTESIAN_POINT('Ctrl Pts',(1.00306229115158,8.8506306393371,-1.73735485143099));
#8300=CARTESIAN_POINT('Ctrl Pts',(2.00612458230317,8.79229730600376,-1.15823656762066));
#8301=CARTESIAN_POINT('Ctrl Pts',(2.00612458230317,8.73396397267044,-2.45679404840839E-16));
#8302=CARTESIAN_POINT('Ctrl Pts',(2.00612458230317,8.67563063933709,1.15823656762066));
#8303=CARTESIAN_POINT('Ctrl Pts',(1.00306229115158,8.61729730600377,1.73735485143099));
#8304=CARTESIAN_POINT('Ctrl Pts',(4.25529211557617E-16,8.55896397267043,
2.31647313524132));
#8305=CARTESIAN_POINT('Ctrl Pts',(-1.00306229115158,8.5006306393371,1.73735485143099));
#8306=CARTESIAN_POINT('Ctrl Pts',(-2.00612458230316,8.44229730600377,1.15823656762066));
#8307=CARTESIAN_POINT('Ctrl Pts',(-2.00612458230317,8.38396397267043,0.));
#8308=CARTESIAN_POINT('Ctrl Pts',(-2.00612458230317,8.3256306393371,-1.15823656762066));
#8309=CARTESIAN_POINT('Ctrl Pts',(-1.00306229115158,8.26729730600376,-1.73735485143099));
#8310=CARTESIAN_POINT('Ctrl Pts',(-1.41843070519206E-16,8.20896397267044,
-2.31647313524132));
#8311=CARTESIAN_POINT('Ctrl Pts',(1.00306229115158,8.1506306393371,-1.73735485143099));
#8312=CARTESIAN_POINT('Ctrl Pts',(2.00612458230317,8.09229730600377,-1.15823656762066));
#8313=CARTESIAN_POINT('Ctrl Pts',(2.00612458230317,8.03396397267043,-2.45679404840839E-16));
#8314=CARTESIAN_POINT('Ctrl Pts',(2.00612458230317,7.9756306393371,1.15823656762066));
#8315=CARTESIAN_POINT('Ctrl Pts',(1.00306229115158,7.91729730600376,1.73735485143099));
#8316=CARTESIAN_POINT('Ctrl Pts',(4.25529211557617E-16,7.85896397267043,
2.31647313524132));
#8317=CARTESIAN_POINT('Ctrl Pts',(-1.00306229115158,7.80063063933709,1.73735485143099));
#8318=CARTESIAN_POINT('Ctrl Pts',(-2.00612458230316,7.74229730600377,1.15823656762066));
#8319=CARTESIAN_POINT('Ctrl Pts',(-2.00612458230317,7.68396397267044,0.));
#8320=CARTESIAN_POINT('Ctrl Pts',(-2.00612458230317,7.6256306393371,-1.15823656762066));
#8321=CARTESIAN_POINT('Ctrl Pts',(-1.00306229115158,7.56729730600377,-1.73735485143099));
#8322=CARTESIAN_POINT('Ctrl Pts',(-1.41843070519206E-16,7.50896397267043,
-2.31647313524132));
#8323=CARTESIAN_POINT('Ctrl Pts',(1.00306229115158,7.4506306393371,-1.73735485143099));
#8324=CARTESIAN_POINT('Ctrl Pts',(2.00612458230317,7.39229730600376,-1.15823656762066));
#8325=CARTESIAN_POINT('Ctrl Pts',(2.00612458230317,7.33396397267044,-2.45679404840839E-16));
#8326=CARTESIAN_POINT('Ctrl Pts',(2.00612458230317,7.2756306393371,1.15823656762066));
#8327=CARTESIAN_POINT('Ctrl Pts',(1.00306229115158,7.21729730600377,1.73735485143099));
#8328=CARTESIAN_POINT('Ctrl Pts',(4.25529211557617E-16,7.15896397267043,
2.31647313524132));
#8329=CARTESIAN_POINT('Ctrl Pts',(-1.00306229115158,7.1006306393371,1.73735485143099));
#8330=CARTESIAN_POINT('Ctrl Pts',(-2.00612458230316,7.04229730600376,1.15823656762066));
#8331=CARTESIAN_POINT('Ctrl Pts',(-2.00612458230317,6.98396397267043,0.));
#8332=CARTESIAN_POINT('Ctrl Pts',(-2.00612458230317,6.92563063933711,-1.15823656762066));
#8333=CARTESIAN_POINT('Ctrl Pts',(-1.00306229115158,6.86729730600377,-1.73735485143099));
#8334=CARTESIAN_POINT('Ctrl Pts',(-1.41843070519206E-16,6.80896397267044,
-2.31647313524132));
#8335=CARTESIAN_POINT('Ctrl Pts',(1.00306229115158,6.7506306393371,-1.73735485143099));
#8336=CARTESIAN_POINT('Ctrl Pts',(2.00612458230317,6.69229730600377,-1.15823656762066));
#8337=CARTESIAN_POINT('Ctrl Pts',(2.00612458230317,6.63396397267043,-2.45679404840839E-16));
#8338=CARTESIAN_POINT('Ctrl Pts',(2.00612458230317,6.5756306393371,1.15823656762066));
#8339=CARTESIAN_POINT('Ctrl Pts',(1.00306229115158,6.51729730600376,1.73735485143099));
#8340=CARTESIAN_POINT('Ctrl Pts',(4.25529211557617E-16,6.45896397267044,
2.31647313524132));
#8341=CARTESIAN_POINT('Ctrl Pts',(-1.00306229115158,6.4006306393371,1.73735485143099));
#8342=CARTESIAN_POINT('Ctrl Pts',(-2.00612458230316,6.34229730600377,1.15823656762066));
#8343=CARTESIAN_POINT('Ctrl Pts',(-2.00612458230317,6.28396397267043,0.));
#8344=CARTESIAN_POINT('Ctrl Pts',(-2.00612458230317,6.2256306393371,-1.15823656762066));
#8345=CARTESIAN_POINT('Ctrl Pts',(-1.00306229115158,6.16729730600376,-1.73735485143099));
#8346=CARTESIAN_POINT('Ctrl Pts',(-1.41843070519206E-16,6.10896397267043,
-2.31647313524132));
#8347=CARTESIAN_POINT('Ctrl Pts',(1.00306229115158,6.05063063933711,-1.73735485143099));
#8348=CARTESIAN_POINT('Ctrl Pts',(2.00612458230317,5.99229730600376,-1.15823656762066));
#8349=CARTESIAN_POINT('Ctrl Pts',(2.00612458230317,5.93396397267044,-2.45679404840839E-16));
#8350=CARTESIAN_POINT('Ctrl Pts',(2.00612458230317,5.8756306393371,1.15823656762066));
#8351=CARTESIAN_POINT('Ctrl Pts',(1.00306229115158,5.81729730600377,1.73735485143099));
#8352=CARTESIAN_POINT('Ctrl Pts',(4.25529211557617E-16,5.75896397267043,
2.31647313524132));
#8353=CARTESIAN_POINT('Ctrl Pts',(-1.00306229115158,5.7006306393371,1.73735485143099));
#8354=CARTESIAN_POINT('Ctrl Pts',(-2.00612458230316,5.64229730600376,1.15823656762066));
#8355=CARTESIAN_POINT('Ctrl Pts',(-2.00612458230317,5.58396397267043,0.));
#8356=CARTESIAN_POINT('Ctrl Pts',(-2.00612458230317,5.52563063933709,-1.15823656762066));
#8357=CARTESIAN_POINT('Ctrl Pts',(-1.00306229115158,5.46729730600377,-1.73735485143099));
#8358=CARTESIAN_POINT('Ctrl Pts',(-1.41843070519206E-16,5.40896397267043,
-2.31647313524132));
#8359=CARTESIAN_POINT('Ctrl Pts',(1.00306229115158,5.3506306393371,-1.73735485143099));
#8360=CARTESIAN_POINT('Ctrl Pts',(2.00612458230317,5.29229730600377,-1.15823656762066));
#8361=CARTESIAN_POINT('Ctrl Pts',(2.00612458230317,5.23396397267043,-2.45679404840839E-16));
#8362=CARTESIAN_POINT('Ctrl Pts',(2.00612458230317,5.1756306393371,1.15823656762066));
#8363=CARTESIAN_POINT('Ctrl Pts',(1.00306229115158,5.11729730600376,1.73735485143099));
#8364=CARTESIAN_POINT('Ctrl Pts',(4.25529211557617E-16,5.05896397267044,
2.31647313524132));
#8365=CARTESIAN_POINT('Ctrl Pts',(-1.00306229115158,5.0006306393371,1.73735485143099));
#8366=CARTESIAN_POINT('Ctrl Pts',(-2.00612458230316,4.94229730600377,1.15823656762066));
#8367=CARTESIAN_POINT('Ctrl Pts',(-2.00612458230317,4.88396397267043,0.));
#8368=CARTESIAN_POINT('Ctrl Pts',(-2.00612458230317,4.8256306393371,-1.15823656762066));
#8369=CARTESIAN_POINT('Ctrl Pts',(-1.00306229115158,4.76729730600376,-1.73735485143099));
#8370=CARTESIAN_POINT('Ctrl Pts',(-1.41843070519206E-16,4.70896397267043,
-2.31647313524132));
#8371=CARTESIAN_POINT('Ctrl Pts',(1.00306229115158,4.65063063933709,-1.73735485143099));
#8372=CARTESIAN_POINT('Ctrl Pts',(2.00612458230317,4.59229730600377,-1.15823656762066));
#8373=CARTESIAN_POINT('Ctrl Pts',(2.00612458230317,4.53396397267044,-2.45679404840839E-16));
#8374=CARTESIAN_POINT('Ctrl Pts',(2.00612458230317,4.4756306393371,1.15823656762066));
#8375=CARTESIAN_POINT('Ctrl Pts',(1.00306229115158,4.41729730600377,1.73735485143099));
#8376=CARTESIAN_POINT('Ctrl Pts',(4.25529211557617E-16,4.35896397267043,
2.31647313524132));
#8377=CARTESIAN_POINT('Ctrl Pts',(-1.00306229115158,4.3006306393371,1.73735485143099));
#8378=CARTESIAN_POINT('Ctrl Pts',(-2.00612458230316,4.24229730600376,1.15823656762066));
#8379=CARTESIAN_POINT('Ctrl Pts',(-2.00612458230317,4.18396397267044,0.));
#8380=CARTESIAN_POINT('Ctrl Pts',(-2.00612458230317,4.1256306393371,-1.15823656762066));
#8381=CARTESIAN_POINT('Ctrl Pts',(-1.00306229115158,4.06729730600377,-1.73735485143099));
#8382=CARTESIAN_POINT('Ctrl Pts',(-1.41843070519206E-16,4.00896397267043,
-2.31647313524132));
#8383=CARTESIAN_POINT('Ctrl Pts',(1.00306229115158,3.9506306393371,-1.73735485143099));
#8384=CARTESIAN_POINT('Ctrl Pts',(2.00612458230317,3.89229730600376,-1.15823656762066));
#8385=CARTESIAN_POINT('Ctrl Pts',(2.00612458230317,3.83396397267043,-2.45679404840839E-16));
#8386=CARTESIAN_POINT('Ctrl Pts',(2.00612458230317,3.77563063933711,1.15823656762066));
#8387=CARTESIAN_POINT('Ctrl Pts',(1.00306229115158,3.71729730600377,1.73735485143099));
#8388=CARTESIAN_POINT('Ctrl Pts',(4.25529211557617E-16,3.65896397267044,
2.31647313524132));
#8389=CARTESIAN_POINT('Ctrl Pts',(-1.00306229115158,3.6006306393371,1.73735485143099));
#8390=CARTESIAN_POINT('Ctrl Pts',(-2.00612458230316,3.54229730600377,1.15823656762066));
#8391=CARTESIAN_POINT('Ctrl Pts',(-2.00612458230317,3.48396397267043,0.));
#8392=CARTESIAN_POINT('Ctrl Pts',(-2.00612458230317,3.4256306393371,-1.15823656762066));
#8393=CARTESIAN_POINT('Ctrl Pts',(-1.00306229115158,3.36729730600376,-1.73735485143099));
#8394=CARTESIAN_POINT('Ctrl Pts',(-1.41843070519206E-16,3.30896397267044,
-2.31647313524132));
#8395=CARTESIAN_POINT('Ctrl Pts',(1.00306229115158,3.25063063933709,-1.73735485143099));
#8396=CARTESIAN_POINT('Ctrl Pts',(2.00612458230317,3.19229730600377,-1.15823656762066));
#8397=CARTESIAN_POINT('Ctrl Pts',(2.00612458230317,3.13396397267043,-2.45679404840839E-16));
#8398=CARTESIAN_POINT('Ctrl Pts',(2.00612458230317,3.0756306393371,1.15823656762066));
#8399=CARTESIAN_POINT('Ctrl Pts',(1.00306229115158,3.01729730600376,1.73735485143099));
#8400=CARTESIAN_POINT('Ctrl Pts',(4.25529211557617E-16,2.95896397267043,
2.31647313524132));
#8401=CARTESIAN_POINT('Ctrl Pts',(-1.00306229115158,2.90063063933711,1.73735485143099));
#8402=CARTESIAN_POINT('Ctrl Pts',(-2.00612458230316,2.84229730600376,1.15823656762066));
#8403=CARTESIAN_POINT('Ctrl Pts',(-2.00612458230317,2.78396397267044,0.));
#8404=CARTESIAN_POINT('Ctrl Pts',(-2.00612458230317,2.7256306393371,-1.15823656762066));
#8405=CARTESIAN_POINT('Ctrl Pts',(-1.00306229115158,2.66729730600377,-1.73735485143099));
#8406=CARTESIAN_POINT('Ctrl Pts',(-1.41843070519206E-16,2.60896397267043,
-2.31647313524132));
#8407=CARTESIAN_POINT('Ctrl Pts',(1.00306229115158,2.5506306393371,-1.73735485143099));
#8408=CARTESIAN_POINT('Ctrl Pts',(2.00612458230317,2.49229730600376,-1.15823656762066));
#8409=CARTESIAN_POINT('Ctrl Pts',(2.00612458230317,2.43396397267043,-2.45679404840839E-16));
#8410=CARTESIAN_POINT('Ctrl Pts',(2.00612458230317,2.37563063933709,1.15823656762066));
#8411=CARTESIAN_POINT('Ctrl Pts',(1.00306229115158,2.31729730600377,1.73735485143099));
#8412=CARTESIAN_POINT('Ctrl Pts',(4.25529211557617E-16,2.25896397267043,
2.31647313524132));
#8413=CARTESIAN_POINT('Ctrl Pts',(-1.00306229115158,2.2006306393371,1.73735485143099));
#8414=CARTESIAN_POINT('Ctrl Pts',(-2.00612458230316,2.14229730600377,1.15823656762066));
#8415=CARTESIAN_POINT('Ctrl Pts',(-2.00612458230317,2.08396397267043,0.));
#8416=CARTESIAN_POINT('Ctrl Pts',(-2.00612458230317,2.0256306393371,-1.15823656762066));
#8417=CARTESIAN_POINT('Ctrl Pts',(-1.00306229115158,1.96729730600376,-1.73735485143099));
#8418=CARTESIAN_POINT('Ctrl Pts',(-1.41843070519206E-16,1.90896397267044,
-2.31647313524132));
#8419=CARTESIAN_POINT('Ctrl Pts',(1.00306229115158,1.8506306393371,-1.73735485143099));
#8420=CARTESIAN_POINT('Ctrl Pts',(2.00612458230317,1.79229730600377,-1.15823656762066));
#8421=CARTESIAN_POINT('Ctrl Pts',(2.00612458230317,1.73396397267043,-2.45679404840839E-16));
#8422=CARTESIAN_POINT('Ctrl Pts',(2.00612458230317,1.6756306393371,1.15823656762066));
#8423=CARTESIAN_POINT('Ctrl Pts',(1.00306229115158,1.61729730600376,1.73735485143099));
#8424=CARTESIAN_POINT('Ctrl Pts',(4.25529211557617E-16,1.55896397267043,
2.31647313524132));
#8425=CARTESIAN_POINT('Ctrl Pts',(-1.00306229115158,1.50063063933709,1.73735485143099));
#8426=CARTESIAN_POINT('Ctrl Pts',(-2.00612458230316,1.44229730600377,1.15823656762066));
#8427=CARTESIAN_POINT('Ctrl Pts',(-2.00612458230317,1.38396397267044,0.));
#8428=CARTESIAN_POINT('Ctrl Pts',(-2.00612458230317,1.3256306393371,-1.15823656762066));
#8429=CARTESIAN_POINT('Ctrl Pts',(-1.00306229115158,1.26729730600377,-1.73735485143099));
#8430=CARTESIAN_POINT('Ctrl Pts',(-1.41843070519206E-16,1.20896397267043,
-2.31647313524132));
#8431=CARTESIAN_POINT('Ctrl Pts',(1.00306229115158,1.1506306393371,-1.73735485143099));
#8432=CARTESIAN_POINT('Ctrl Pts',(2.00612458230317,1.09229730600376,-1.15823656762066));
#8433=CARTESIAN_POINT('Ctrl Pts',(2.00612458230317,1.03396397267044,-2.45679404840839E-16));
#8434=CARTESIAN_POINT('Ctrl Pts',(2.00612458230317,0.975630639337095,1.15823656762066));
#8435=CARTESIAN_POINT('Ctrl Pts',(1.00306229115158,0.917297306003768,1.73735485143099));
#8436=CARTESIAN_POINT('Ctrl Pts',(4.25529211557617E-16,0.858963972670427,
2.31647313524132));
#8437=CARTESIAN_POINT('Ctrl Pts',(-1.00306229115158,0.800630639337101,1.73735485143099));
#8438=CARTESIAN_POINT('Ctrl Pts',(-2.00612458230316,0.74229730600376,1.15823656762066));
#8439=CARTESIAN_POINT('Ctrl Pts',(-2.00612458230317,0.683963972670433,0.));
#8440=CARTESIAN_POINT('Ctrl Pts',(-2.00612458230317,0.625630639337106,-1.15823656762066));
#8441=CARTESIAN_POINT('Ctrl Pts',(-1.00306229115158,0.567297306003765,-1.73735485143099));
#8442=CARTESIAN_POINT('Ctrl Pts',(-1.41843070519206E-16,0.508963972670438,
-2.31647313524132));
#8443=CARTESIAN_POINT('Ctrl Pts',(1.00306229115158,0.450630639337097,-1.73735485143099));
#8444=CARTESIAN_POINT('Ctrl Pts',(2.00612458230317,0.39229730600377,-1.15823656762066));
#8445=CARTESIAN_POINT('Ctrl Pts',(2.00612458230317,0.33396397267043,-2.45679404840839E-16));
#8446=CARTESIAN_POINT('Ctrl Pts',(2.00612458230317,0.275630639337103,1.15823656762066));
#8447=CARTESIAN_POINT('Ctrl Pts',(1.00306229115158,0.217297306003762,1.73735485143099));
#8448=CARTESIAN_POINT('Ctrl Pts',(4.25529211557617E-16,0.158963972670435,
2.31647313524132));
#8449=CARTESIAN_POINT('Ctrl Pts',(-1.00306229115158,0.100630639337094,1.73735485143099));
#8450=CARTESIAN_POINT('Ctrl Pts',(-2.00612458230316,0.0422973060037674,
1.15823656762066));
#8451=CARTESIAN_POINT('Ctrl Pts',(-2.00612458230317,-0.0160360273295734,
0.));
#8452=CARTESIAN_POINT('Ctrl Pts',(-2.00612458230317,-0.0743693606629003,
-1.15823656762066));
#8453=CARTESIAN_POINT('Ctrl Pts',(-1.00306229115158,-0.132702693996241,
-1.73735485143099));
#8454=CARTESIAN_POINT('Ctrl Pts',(-1.41843070519206E-16,-0.191036027329568,
-2.31647313524132));
#8455=CARTESIAN_POINT('Ctrl Pts',(1.00306229115158,-0.249369360662895,-1.73735485143099));
#8456=CARTESIAN_POINT('Ctrl Pts',(2.00612458230317,-0.307702693996236,-1.15823656762066));
#8457=CARTESIAN_POINT('Ctrl Pts',(2.00612458230317,-0.366036027329563,-2.45679404840839E-16));
#8458=CARTESIAN_POINT('Ctrl Pts',(2.00612458230317,-0.424369360662903,1.15823656762066));
#8459=CARTESIAN_POINT('Ctrl Pts',(1.00306229115158,-0.48270269399623,1.73735485143099));
#8460=CARTESIAN_POINT('Ctrl Pts',(4.25529211557617E-16,-0.541036027329571,
2.31647313524132));
#8461=CARTESIAN_POINT('Ctrl Pts',(-1.00306229115158,-0.599369360662898,
1.73735485143099));
#8462=CARTESIAN_POINT('Ctrl Pts',(-2.00612458230316,-0.657702693996238,
1.15823656762066));
#8463=CARTESIAN_POINT('Ctrl Pts',(-2.00612458230317,-0.716036027329566,
0.));
#8464=CARTESIAN_POINT('Ctrl Pts',(-2.00612458230317,-0.774369360662906,
-1.15823656762066));
#8465=CARTESIAN_POINT('Ctrl Pts',(-1.00306229115158,-0.832702693996233,
-1.73735485143099));
#8466=CARTESIAN_POINT('Ctrl Pts',(-1.41843070519206E-16,-0.891036027329575,
-2.31647313524132));
#8467=CARTESIAN_POINT('Ctrl Pts',(1.00306229115158,-0.949369360662901,-1.73735485143099));
#8468=CARTESIAN_POINT('Ctrl Pts',(2.00612458230317,-1.00770269399623,-1.15823656762066));
#8469=CARTESIAN_POINT('Ctrl Pts',(2.00612458230317,-1.06603602732957,-2.45679404840839E-16));
#8470=CARTESIAN_POINT('Ctrl Pts',(2.00612458230317,-1.1243693606629,1.15823656762066));
#8471=CARTESIAN_POINT('Ctrl Pts',(1.00306229115158,-1.18270269399624,1.73735485143099));
#8472=CARTESIAN_POINT('Ctrl Pts',(4.25529211557617E-16,-1.24103602732956,
2.31647313524132));
#8473=CARTESIAN_POINT('Ctrl Pts',(-1.00306229115158,-1.2993693606629,1.73735485143099));
#8474=CARTESIAN_POINT('Ctrl Pts',(-2.00612458230316,-1.35770269399623,1.15823656762066));
#8475=CARTESIAN_POINT('Ctrl Pts',(-2.00612458230317,-1.41603602732957,0.));
#8476=CARTESIAN_POINT('Ctrl Pts',(-2.00612458230317,-1.4743693606629,-1.15823656762066));
#8477=CARTESIAN_POINT('Ctrl Pts',(-1.00306229115158,-1.53270269399624,-1.73735485143099));
#8478=CARTESIAN_POINT('Ctrl Pts',(-1.41843070519206E-16,-1.59103602732957,
-2.31647313524132));
#8479=CARTESIAN_POINT('Ctrl Pts',(1.00306229115158,-1.64936936066291,-1.73735485143099));
#8480=CARTESIAN_POINT('Ctrl Pts',(2.00612458230317,-1.70770269399623,-1.15823656762066));
#8481=CARTESIAN_POINT('Ctrl Pts',(2.00612458230317,-1.76603602732956,-2.45679404840839E-16));
#8482=CARTESIAN_POINT('Ctrl Pts',(2.00612458230317,-1.8243693606629,1.15823656762066));
#8483=CARTESIAN_POINT('Ctrl Pts',(1.00306229115158,-1.88270269399623,1.73735485143099));
#8484=CARTESIAN_POINT('Ctrl Pts',(4.25529211557617E-16,-1.94103602732957,
2.31647313524132));
#8485=CARTESIAN_POINT('Ctrl Pts',(-1.00306229115158,-1.9993693606629,1.73735485143099));
#8486=CARTESIAN_POINT('Ctrl Pts',(-2.00612458230316,-2.05770269399624,1.15823656762066));
#8487=CARTESIAN_POINT('Ctrl Pts',(-2.00612458230317,-2.11603602732956,0.));
#8488=CARTESIAN_POINT('Ctrl Pts',(-2.00612458230317,-2.17436936066291,-1.15823656762066));
#8489=CARTESIAN_POINT('Ctrl Pts',(-1.00306229115158,-2.23270269399623,-1.73735485143099));
#8490=CARTESIAN_POINT('Ctrl Pts',(-1.41843070519206E-16,-2.29103602732957,
-2.31647313524132));
#8491=CARTESIAN_POINT('Ctrl Pts',(1.00306229115158,-2.3493693606629,-1.73735485143099));
#8492=CARTESIAN_POINT('Ctrl Pts',(2.00612458230317,-2.40770269399624,-1.15823656762066));
#8493=CARTESIAN_POINT('Ctrl Pts',(2.00612458230317,-2.46603602732957,-2.45679404840839E-16));
#8494=CARTESIAN_POINT('Ctrl Pts',(2.00612458230317,-2.52436936066289,1.15823656762066));
#8495=CARTESIAN_POINT('Ctrl Pts',(1.00306229115158,-2.58270269399623,1.73735485143099));
#8496=CARTESIAN_POINT('Ctrl Pts',(0.74117398807312,-2.59793287243514,1.88855613371095));
#8497=CARTESIAN_POINT('Ctrl Pts',(0.446351454824861,-2.61507834909981,1.95583900628267));
#8498=CARTESIAN_POINT('Ctrl Pts',(-1.6211138875,71.6062500009559,0.));
#8499=CARTESIAN_POINT('Ctrl Pts',(-1.6211138875,71.5479166676226,-0.935950539335166));
#8500=CARTESIAN_POINT('Ctrl Pts',(-0.81055694375,71.4895833342893,-1.40392580900275));
#8501=CARTESIAN_POINT('Ctrl Pts',(-1.14620883215705E-16,71.4312500009559,
-1.87190107867033));
#8502=CARTESIAN_POINT('Ctrl Pts',(0.81055694375,71.3729166676226,-1.40392580900275));
#8503=CARTESIAN_POINT('Ctrl Pts',(1.6211138875,71.3145833342893,-0.935950539335166));
#8504=CARTESIAN_POINT('Ctrl Pts',(1.6211138875,71.2562500009559,-1.9852919333802E-16));
#8505=CARTESIAN_POINT('Ctrl Pts',(1.6211138875,71.1979166676226,0.935950539335165));
#8506=CARTESIAN_POINT('Ctrl Pts',(0.810556943750001,71.1395833342893,1.40392580900275));
#8507=CARTESIAN_POINT('Ctrl Pts',(3.43862649647115E-16,71.0812500009559,
1.87190107867033));
#8508=CARTESIAN_POINT('Ctrl Pts',(-0.810556943749999,71.0229166676226,1.40392580900275));
#8509=CARTESIAN_POINT('Ctrl Pts',(-1.6211138875,70.9645833342893,0.935950539335167));
#8510=CARTESIAN_POINT('Ctrl Pts',(-1.6211138875,70.9062500009559,0.));
#8511=CARTESIAN_POINT('Ctrl Pts',(-1.6211138875,70.8479166676226,-0.935950539335166));
#8512=CARTESIAN_POINT('Ctrl Pts',(-0.81055694375,70.7895833342893,-1.40392580900275));
#8513=CARTESIAN_POINT('Ctrl Pts',(-1.14620883215705E-16,70.7312500009559,
-1.87190107867033));
#8514=CARTESIAN_POINT('Ctrl Pts',(0.81055694375,70.6729166676226,-1.40392580900275));
#8515=CARTESIAN_POINT('Ctrl Pts',(1.6211138875,70.6145833342893,-0.935950539335166));
#8516=CARTESIAN_POINT('Ctrl Pts',(1.6211138875,70.5562500009559,-1.9852919333802E-16));
#8517=CARTESIAN_POINT('Ctrl Pts',(1.6211138875,70.4979166676226,0.935950539335165));
#8518=CARTESIAN_POINT('Ctrl Pts',(0.810556943750001,70.4395833342893,1.40392580900275));
#8519=CARTESIAN_POINT('Ctrl Pts',(3.43862649647115E-16,70.3812500009559,
1.87190107867033));
#8520=CARTESIAN_POINT('Ctrl Pts',(-0.810556943749999,70.3229166676226,1.40392580900275));
#8521=CARTESIAN_POINT('Ctrl Pts',(-1.6211138875,70.2645833342893,0.935950539335167));
#8522=CARTESIAN_POINT('Ctrl Pts',(-1.6211138875,70.2062500009559,0.));
#8523=CARTESIAN_POINT('Ctrl Pts',(-1.6211138875,70.1479166676226,-0.935950539335166));
#8524=CARTESIAN_POINT('Ctrl Pts',(-0.81055694375,70.0895833342893,-1.40392580900275));
#8525=CARTESIAN_POINT('Ctrl Pts',(-1.14620883215705E-16,70.0312500009559,
-1.87190107867033));
#8526=CARTESIAN_POINT('Ctrl Pts',(0.81055694375,69.9729166676226,-1.40392580900275));
#8527=CARTESIAN_POINT('Ctrl Pts',(1.6211138875,69.9145833342893,-0.935950539335166));
#8528=CARTESIAN_POINT('Ctrl Pts',(1.6211138875,69.8562500009559,-1.9852919333802E-16));
#8529=CARTESIAN_POINT('Ctrl Pts',(1.6211138875,69.7979166676226,0.935950539335165));
#8530=CARTESIAN_POINT('Ctrl Pts',(0.810556943750001,69.7395833342893,1.40392580900275));
#8531=CARTESIAN_POINT('Ctrl Pts',(3.43862649647115E-16,69.6812500009559,
1.87190107867033));
#8532=CARTESIAN_POINT('Ctrl Pts',(-0.810556943749999,69.6229166676226,1.40392580900275));
#8533=CARTESIAN_POINT('Ctrl Pts',(-1.6211138875,69.5645833342893,0.935950539335167));
#8534=CARTESIAN_POINT('Ctrl Pts',(-1.6211138875,69.5062500009559,0.));
#8535=CARTESIAN_POINT('Ctrl Pts',(-1.6211138875,69.4479166676226,-0.935950539335166));
#8536=CARTESIAN_POINT('Ctrl Pts',(-0.81055694375,69.3895833342893,-1.40392580900275));
#8537=CARTESIAN_POINT('Ctrl Pts',(-1.14620883215705E-16,69.3312500009559,
-1.87190107867033));
#8538=CARTESIAN_POINT('Ctrl Pts',(0.81055694375,69.2729166676226,-1.40392580900275));
#8539=CARTESIAN_POINT('Ctrl Pts',(1.6211138875,69.2145833342893,-0.935950539335166));
#8540=CARTESIAN_POINT('Ctrl Pts',(1.6211138875,69.1562500009559,-1.9852919333802E-16));
#8541=CARTESIAN_POINT('Ctrl Pts',(1.6211138875,69.0979166676226,0.935950539335165));
#8542=CARTESIAN_POINT('Ctrl Pts',(0.810556943750001,69.0395833342893,1.40392580900275));
#8543=CARTESIAN_POINT('Ctrl Pts',(3.43862649647115E-16,68.9812500009559,
1.87190107867033));
#8544=CARTESIAN_POINT('Ctrl Pts',(-0.810556943749999,68.9229166676226,1.40392580900275));
#8545=CARTESIAN_POINT('Ctrl Pts',(-1.6211138875,68.8645833342893,0.935950539335167));
#8546=CARTESIAN_POINT('Ctrl Pts',(-1.6211138875,68.8062500009559,0.));
#8547=CARTESIAN_POINT('Ctrl Pts',(-1.6211138875,68.7479166676226,-0.935950539335166));
#8548=CARTESIAN_POINT('Ctrl Pts',(-0.81055694375,68.6895833342893,-1.40392580900275));
#8549=CARTESIAN_POINT('Ctrl Pts',(-1.14620883215705E-16,68.6312500009559,
-1.87190107867033));
#8550=CARTESIAN_POINT('Ctrl Pts',(0.81055694375,68.5729166676226,-1.40392580900275));
#8551=CARTESIAN_POINT('Ctrl Pts',(1.6211138875,68.5145833342893,-0.935950539335166));
#8552=CARTESIAN_POINT('Ctrl Pts',(1.6211138875,68.4562500009559,-1.9852919333802E-16));
#8553=CARTESIAN_POINT('Ctrl Pts',(1.6211138875,68.3979166676226,0.935950539335165));
#8554=CARTESIAN_POINT('Ctrl Pts',(0.810556943750001,68.3395833342893,1.40392580900275));
#8555=CARTESIAN_POINT('Ctrl Pts',(3.43862649647115E-16,68.2812500009559,
1.87190107867033));
#8556=CARTESIAN_POINT('Ctrl Pts',(-0.810556943749999,68.2229166676226,1.40392580900275));
#8557=CARTESIAN_POINT('Ctrl Pts',(-1.6211138875,68.1645833342893,0.935950539335167));
#8558=CARTESIAN_POINT('Ctrl Pts',(-1.6211138875,68.1062500009559,0.));
#8559=CARTESIAN_POINT('Ctrl Pts',(-1.6211138875,68.0479166676226,-0.935950539335166));
#8560=CARTESIAN_POINT('Ctrl Pts',(-0.81055694375,67.9895833342893,-1.40392580900275));
#8561=CARTESIAN_POINT('Ctrl Pts',(-1.14620883215705E-16,67.9312500009559,
-1.87190107867033));
#8562=CARTESIAN_POINT('Ctrl Pts',(0.81055694375,67.8729166676226,-1.40392580900275));
#8563=CARTESIAN_POINT('Ctrl Pts',(1.6211138875,67.8145833342893,-0.935950539335166));
#8564=CARTESIAN_POINT('Ctrl Pts',(1.6211138875,67.7562500009559,-1.9852919333802E-16));
#8565=CARTESIAN_POINT('Ctrl Pts',(1.6211138875,67.6979166676226,0.935950539335165));
#8566=CARTESIAN_POINT('Ctrl Pts',(0.810556943750001,67.6395833342893,1.40392580900275));
#8567=CARTESIAN_POINT('Ctrl Pts',(3.43862649647115E-16,67.5812500009559,
1.87190107867033));
#8568=CARTESIAN_POINT('Ctrl Pts',(-0.810556943749999,67.5229166676226,1.40392580900275));
#8569=CARTESIAN_POINT('Ctrl Pts',(-1.6211138875,67.4645833342893,0.935950539335167));
#8570=CARTESIAN_POINT('Ctrl Pts',(-1.6211138875,67.4062500009559,0.));
#8571=CARTESIAN_POINT('Ctrl Pts',(-1.6211138875,67.3479166676226,-0.935950539335166));
#8572=CARTESIAN_POINT('Ctrl Pts',(-0.81055694375,67.2895833342893,-1.40392580900275));
#8573=CARTESIAN_POINT('Ctrl Pts',(-1.14620883215705E-16,67.2312500009559,
-1.87190107867033));
#8574=CARTESIAN_POINT('Ctrl Pts',(0.81055694375,67.1729166676226,-1.40392580900275));
#8575=CARTESIAN_POINT('Ctrl Pts',(1.6211138875,67.1145833342893,-0.935950539335166));
#8576=CARTESIAN_POINT('Ctrl Pts',(1.6211138875,67.0562500009559,-1.9852919333802E-16));
#8577=CARTESIAN_POINT('Ctrl Pts',(1.6211138875,66.9979166676226,0.935950539335165));
#8578=CARTESIAN_POINT('Ctrl Pts',(0.810556943750001,66.9395833342893,1.40392580900275));
#8579=CARTESIAN_POINT('Ctrl Pts',(3.43862649647115E-16,66.8812500009559,
1.87190107867033));
#8580=CARTESIAN_POINT('Ctrl Pts',(-0.810556943749999,66.8229166676226,1.40392580900275));
#8581=CARTESIAN_POINT('Ctrl Pts',(-1.6211138875,66.7645833342893,0.935950539335167));
#8582=CARTESIAN_POINT('Ctrl Pts',(-1.6211138875,66.7062500009559,0.));
#8583=CARTESIAN_POINT('Ctrl Pts',(-1.6211138875,66.6479166676226,-0.935950539335166));
#8584=CARTESIAN_POINT('Ctrl Pts',(-0.81055694375,66.5895833342893,-1.40392580900275));
#8585=CARTESIAN_POINT('Ctrl Pts',(-1.14620883215705E-16,66.5312500009559,
-1.87190107867033));
#8586=CARTESIAN_POINT('Ctrl Pts',(0.81055694375,66.4729166676226,-1.40392580900275));
#8587=CARTESIAN_POINT('Ctrl Pts',(1.6211138875,66.4145833342893,-0.935950539335166));
#8588=CARTESIAN_POINT('Ctrl Pts',(1.6211138875,66.3562500009559,-1.9852919333802E-16));
#8589=CARTESIAN_POINT('Ctrl Pts',(1.6211138875,66.2979166676226,0.935950539335165));
#8590=CARTESIAN_POINT('Ctrl Pts',(0.810556943750001,66.2395833342893,1.40392580900275));
#8591=CARTESIAN_POINT('Ctrl Pts',(3.43862649647115E-16,66.1812500009559,
1.87190107867033));
#8592=CARTESIAN_POINT('Ctrl Pts',(-0.810556943749999,66.1229166676226,1.40392580900275));
#8593=CARTESIAN_POINT('Ctrl Pts',(-1.6211138875,66.0645833342893,0.935950539335167));
#8594=CARTESIAN_POINT('Ctrl Pts',(-1.6211138875,66.0062500009559,0.));
#8595=CARTESIAN_POINT('Ctrl Pts',(-1.6211138875,65.9479166676226,-0.935950539335166));
#8596=CARTESIAN_POINT('Ctrl Pts',(-0.81055694375,65.8895833342893,-1.40392580900275));
#8597=CARTESIAN_POINT('Ctrl Pts',(-1.14620883215705E-16,65.8312500009559,
-1.87190107867033));
#8598=CARTESIAN_POINT('Ctrl Pts',(0.81055694375,65.7729166676226,-1.40392580900275));
#8599=CARTESIAN_POINT('Ctrl Pts',(1.6211138875,65.7145833342893,-0.935950539335166));
#8600=CARTESIAN_POINT('Ctrl Pts',(1.6211138875,65.6562500009559,-1.9852919333802E-16));
#8601=CARTESIAN_POINT('Ctrl Pts',(1.6211138875,65.5979166676226,0.935950539335165));
#8602=CARTESIAN_POINT('Ctrl Pts',(0.810556943750001,65.5395833342893,1.40392580900275));
#8603=CARTESIAN_POINT('Ctrl Pts',(3.43862649647115E-16,65.4812500009559,
1.87190107867033));
#8604=CARTESIAN_POINT('Ctrl Pts',(-0.810556943749999,65.4229166676226,1.40392580900275));
#8605=CARTESIAN_POINT('Ctrl Pts',(-1.6211138875,65.3645833342893,0.935950539335167));
#8606=CARTESIAN_POINT('Ctrl Pts',(-1.6211138875,65.3062500009559,0.));
#8607=CARTESIAN_POINT('Ctrl Pts',(-1.6211138875,65.2479166676226,-0.935950539335166));
#8608=CARTESIAN_POINT('Ctrl Pts',(-0.81055694375,65.1895833342893,-1.40392580900275));
#8609=CARTESIAN_POINT('Ctrl Pts',(-1.14620883215705E-16,65.1312500009559,
-1.87190107867033));
#8610=CARTESIAN_POINT('Ctrl Pts',(0.81055694375,65.0729166676226,-1.40392580900275));
#8611=CARTESIAN_POINT('Ctrl Pts',(1.6211138875,65.0145833342893,-0.935950539335166));
#8612=CARTESIAN_POINT('Ctrl Pts',(1.6211138875,64.9562500009559,-1.9852919333802E-16));
#8613=CARTESIAN_POINT('Ctrl Pts',(1.6211138875,64.8979166676226,0.935950539335165));
#8614=CARTESIAN_POINT('Ctrl Pts',(0.810556943750001,64.8395833342893,1.40392580900275));
#8615=CARTESIAN_POINT('Ctrl Pts',(3.43862649647115E-16,64.7812500009559,
1.87190107867033));
#8616=CARTESIAN_POINT('Ctrl Pts',(-0.810556943749999,64.7229166676226,1.40392580900275));
#8617=CARTESIAN_POINT('Ctrl Pts',(-1.6211138875,64.6645833342893,0.935950539335167));
#8618=CARTESIAN_POINT('Ctrl Pts',(-1.6211138875,64.6062500009559,0.));
#8619=CARTESIAN_POINT('Ctrl Pts',(-1.6211138875,64.5479166676226,-0.935950539335166));
#8620=CARTESIAN_POINT('Ctrl Pts',(-0.81055694375,64.4895833342893,-1.40392580900275));
#8621=CARTESIAN_POINT('Ctrl Pts',(-1.14620883215705E-16,64.4312500009559,
-1.87190107867033));
#8622=CARTESIAN_POINT('Ctrl Pts',(0.81055694375,64.3729166676226,-1.40392580900275));
#8623=CARTESIAN_POINT('Ctrl Pts',(1.6211138875,64.3145833342893,-0.935950539335166));
#8624=CARTESIAN_POINT('Ctrl Pts',(1.6211138875,64.2562500009559,-1.9852919333802E-16));
#8625=CARTESIAN_POINT('Ctrl Pts',(1.6211138875,64.1979166676226,0.935950539335165));
#8626=CARTESIAN_POINT('Ctrl Pts',(0.810556943750001,64.1395833342893,1.40392580900275));
#8627=CARTESIAN_POINT('Ctrl Pts',(3.43862649647115E-16,64.0812500009559,
1.87190107867033));
#8628=CARTESIAN_POINT('Ctrl Pts',(-0.810556943749999,64.0229166676226,1.40392580900275));
#8629=CARTESIAN_POINT('Ctrl Pts',(-1.6211138875,63.9645833342893,0.935950539335167));
#8630=CARTESIAN_POINT('Ctrl Pts',(-1.6211138875,63.9062500009559,0.));
#8631=CARTESIAN_POINT('Ctrl Pts',(-1.6211138875,63.8479166676226,-0.935950539335166));
#8632=CARTESIAN_POINT('Ctrl Pts',(-0.81055694375,63.7895833342893,-1.40392580900275));
#8633=CARTESIAN_POINT('Ctrl Pts',(-1.14620883215705E-16,63.7312500009559,
-1.87190107867033));
#8634=CARTESIAN_POINT('Ctrl Pts',(0.81055694375,63.6729166676226,-1.40392580900275));
#8635=CARTESIAN_POINT('Ctrl Pts',(1.6211138875,63.6145833342893,-0.935950539335166));
#8636=CARTESIAN_POINT('Ctrl Pts',(1.6211138875,63.5562500009559,-1.9852919333802E-16));
#8637=CARTESIAN_POINT('Ctrl Pts',(1.6211138875,63.4979166676226,0.935950539335165));
#8638=CARTESIAN_POINT('Ctrl Pts',(0.810556943750001,63.4395833342893,1.40392580900275));
#8639=CARTESIAN_POINT('Ctrl Pts',(3.43862649647115E-16,63.3812500009559,
1.87190107867033));
#8640=CARTESIAN_POINT('Ctrl Pts',(-0.810556943749999,63.3229166676226,1.40392580900275));
#8641=CARTESIAN_POINT('Ctrl Pts',(-1.6211138875,63.2645833342893,0.935950539335167));
#8642=CARTESIAN_POINT('Ctrl Pts',(-1.6211138875,63.2062500009559,0.));
#8643=CARTESIAN_POINT('Ctrl Pts',(-1.6211138875,63.1479166676226,-0.935950539335166));
#8644=CARTESIAN_POINT('Ctrl Pts',(-0.81055694375,63.0895833342893,-1.40392580900275));
#8645=CARTESIAN_POINT('Ctrl Pts',(-1.14620883215705E-16,63.0312500009559,
-1.87190107867033));
#8646=CARTESIAN_POINT('Ctrl Pts',(0.81055694375,62.9729166676226,-1.40392580900275));
#8647=CARTESIAN_POINT('Ctrl Pts',(1.6211138875,62.9145833342892,-0.935950539335166));
#8648=CARTESIAN_POINT('Ctrl Pts',(1.6211138875,62.8562500009559,-1.9852919333802E-16));
#8649=CARTESIAN_POINT('Ctrl Pts',(1.6211138875,62.7979166676226,0.935950539335165));
#8650=CARTESIAN_POINT('Ctrl Pts',(0.810556943750001,62.7395833342893,1.40392580900275));
#8651=CARTESIAN_POINT('Ctrl Pts',(3.43862649647115E-16,62.6812500009559,
1.87190107867033));
#8652=CARTESIAN_POINT('Ctrl Pts',(-0.810556943749999,62.6229166676226,1.40392580900275));
#8653=CARTESIAN_POINT('Ctrl Pts',(-1.6211138875,62.5645833342893,0.935950539335167));
#8654=CARTESIAN_POINT('Ctrl Pts',(-1.6211138875,62.5062500009559,0.));
#8655=CARTESIAN_POINT('Ctrl Pts',(-1.6211138875,62.4479166676226,-0.935950539335166));
#8656=CARTESIAN_POINT('Ctrl Pts',(-0.81055694375,62.3895833342893,-1.40392580900275));
#8657=CARTESIAN_POINT('Ctrl Pts',(-1.14620883215705E-16,62.3312500009559,
-1.87190107867033));
#8658=CARTESIAN_POINT('Ctrl Pts',(0.81055694375,62.2729166676226,-1.40392580900275));
#8659=CARTESIAN_POINT('Ctrl Pts',(1.6211138875,62.2145833342893,-0.935950539335166));
#8660=CARTESIAN_POINT('Ctrl Pts',(1.6211138875,62.1562500009559,-1.9852919333802E-16));
#8661=CARTESIAN_POINT('Ctrl Pts',(1.6211138875,62.0979166676226,0.935950539335165));
#8662=CARTESIAN_POINT('Ctrl Pts',(0.810556943750001,62.0395833342893,1.40392580900275));
#8663=CARTESIAN_POINT('Ctrl Pts',(3.43862649647115E-16,61.9812500009559,
1.87190107867033));
#8664=CARTESIAN_POINT('Ctrl Pts',(-0.810556943749999,61.9229166676226,1.40392580900275));
#8665=CARTESIAN_POINT('Ctrl Pts',(-1.6211138875,61.8645833342893,0.935950539335167));
#8666=CARTESIAN_POINT('Ctrl Pts',(-1.6211138875,61.8062500009559,0.));
#8667=CARTESIAN_POINT('Ctrl Pts',(-1.6211138875,61.7479166676226,-0.935950539335166));
#8668=CARTESIAN_POINT('Ctrl Pts',(-0.81055694375,61.6895833342893,-1.40392580900275));
#8669=CARTESIAN_POINT('Ctrl Pts',(-1.14620883215705E-16,61.6312500009559,
-1.87190107867033));
#8670=CARTESIAN_POINT('Ctrl Pts',(0.81055694375,61.5729166676226,-1.40392580900275));
#8671=CARTESIAN_POINT('Ctrl Pts',(1.6211138875,61.5145833342893,-0.935950539335166));
#8672=CARTESIAN_POINT('Ctrl Pts',(1.6211138875,61.4562500009559,-1.9852919333802E-16));
#8673=CARTESIAN_POINT('Ctrl Pts',(1.6211138875,61.3979166676226,0.935950539335165));
#8674=CARTESIAN_POINT('Ctrl Pts',(0.810556943750001,61.3395833342893,1.40392580900275));
#8675=CARTESIAN_POINT('Ctrl Pts',(3.43862649647115E-16,61.2812500009559,
1.87190107867033));
#8676=CARTESIAN_POINT('Ctrl Pts',(-0.810556943749999,61.2229166676226,1.40392580900275));
#8677=CARTESIAN_POINT('Ctrl Pts',(-1.6211138875,61.1645833342893,0.935950539335167));
#8678=CARTESIAN_POINT('Ctrl Pts',(-1.6211138875,61.1062500009559,0.));
#8679=CARTESIAN_POINT('Ctrl Pts',(-1.6211138875,61.0479166676226,-0.935950539335166));
#8680=CARTESIAN_POINT('Ctrl Pts',(-0.81055694375,60.9895833342893,-1.40392580900275));
#8681=CARTESIAN_POINT('Ctrl Pts',(-1.14620883215705E-16,60.9312500009559,
-1.87190107867033));
#8682=CARTESIAN_POINT('Ctrl Pts',(0.81055694375,60.8729166676226,-1.40392580900275));
#8683=CARTESIAN_POINT('Ctrl Pts',(1.6211138875,60.8145833342893,-0.935950539335166));
#8684=CARTESIAN_POINT('Ctrl Pts',(1.6211138875,60.7562500009559,-1.9852919333802E-16));
#8685=CARTESIAN_POINT('Ctrl Pts',(1.6211138875,60.6979166676226,0.935950539335165));
#8686=CARTESIAN_POINT('Ctrl Pts',(0.810556943750001,60.6395833342893,1.40392580900275));
#8687=CARTESIAN_POINT('Ctrl Pts',(3.43862649647115E-16,60.5812500009559,
1.87190107867033));
#8688=CARTESIAN_POINT('Ctrl Pts',(-0.810556943749999,60.5229166676226,1.40392580900275));
#8689=CARTESIAN_POINT('Ctrl Pts',(-1.6211138875,60.4645833342893,0.935950539335167));
#8690=CARTESIAN_POINT('Ctrl Pts',(-1.6211138875,60.4062500009559,0.));
#8691=CARTESIAN_POINT('Ctrl Pts',(-1.6211138875,60.3479166676226,-0.935950539335166));
#8692=CARTESIAN_POINT('Ctrl Pts',(-0.81055694375,60.2895833342893,-1.40392580900275));
#8693=CARTESIAN_POINT('Ctrl Pts',(-1.14620883215705E-16,60.2312500009559,
-1.87190107867033));
#8694=CARTESIAN_POINT('Ctrl Pts',(0.81055694375,60.1729166676226,-1.40392580900275));
#8695=CARTESIAN_POINT('Ctrl Pts',(1.6211138875,60.1145833342893,-0.935950539335166));
#8696=CARTESIAN_POINT('Ctrl Pts',(1.6211138875,60.0562500009559,-1.9852919333802E-16));
#8697=CARTESIAN_POINT('Ctrl Pts',(1.6211138875,59.9979166676226,0.935950539335165));
#8698=CARTESIAN_POINT('Ctrl Pts',(0.810556943750001,59.9395833342893,1.40392580900275));
#8699=CARTESIAN_POINT('Ctrl Pts',(3.43862649647115E-16,59.8812500009559,
1.87190107867033));
#8700=CARTESIAN_POINT('Ctrl Pts',(-0.810556943749999,59.8229166676226,1.40392580900275));
#8701=CARTESIAN_POINT('Ctrl Pts',(-1.6211138875,59.7645833342893,0.935950539335167));
#8702=CARTESIAN_POINT('Ctrl Pts',(-1.6211138875,59.7062500009559,0.));
#8703=CARTESIAN_POINT('Ctrl Pts',(-1.6211138875,59.6479166676226,-0.935950539335166));
#8704=CARTESIAN_POINT('Ctrl Pts',(-0.81055694375,59.5895833342893,-1.40392580900275));
#8705=CARTESIAN_POINT('Ctrl Pts',(-1.14620883215705E-16,59.5312500009559,
-1.87190107867033));
#8706=CARTESIAN_POINT('Ctrl Pts',(0.81055694375,59.4729166676226,-1.40392580900275));
#8707=CARTESIAN_POINT('Ctrl Pts',(1.6211138875,59.4145833342893,-0.935950539335166));
#8708=CARTESIAN_POINT('Ctrl Pts',(1.6211138875,59.3562500009559,-1.9852919333802E-16));
#8709=CARTESIAN_POINT('Ctrl Pts',(1.6211138875,59.2979166676226,0.935950539335165));
#8710=CARTESIAN_POINT('Ctrl Pts',(0.810556943750001,59.2395833342893,1.40392580900275));
#8711=CARTESIAN_POINT('Ctrl Pts',(3.43862649647115E-16,59.1812500009559,
1.87190107867033));
#8712=CARTESIAN_POINT('Ctrl Pts',(-0.810556943749999,59.1229166676226,1.40392580900275));
#8713=CARTESIAN_POINT('Ctrl Pts',(-1.6211138875,59.0645833342893,0.935950539335167));
#8714=CARTESIAN_POINT('Ctrl Pts',(-1.6211138875,59.0062500009559,0.));
#8715=CARTESIAN_POINT('Ctrl Pts',(-1.6211138875,58.9479166676226,-0.935950539335166));
#8716=CARTESIAN_POINT('Ctrl Pts',(-0.81055694375,58.8895833342893,-1.40392580900275));
#8717=CARTESIAN_POINT('Ctrl Pts',(-1.14620883215705E-16,58.8312500009559,
-1.87190107867033));
#8718=CARTESIAN_POINT('Ctrl Pts',(0.81055694375,58.7729166676226,-1.40392580900275));
#8719=CARTESIAN_POINT('Ctrl Pts',(1.6211138875,58.7145833342893,-0.935950539335166));
#8720=CARTESIAN_POINT('Ctrl Pts',(1.6211138875,58.6562500009559,-1.9852919333802E-16));
#8721=CARTESIAN_POINT('Ctrl Pts',(1.6211138875,58.5979166676226,0.935950539335165));
#8722=CARTESIAN_POINT('Ctrl Pts',(0.810556943750001,58.5395833342893,1.40392580900275));
#8723=CARTESIAN_POINT('Ctrl Pts',(3.43862649647115E-16,58.4812500009559,
1.87190107867033));
#8724=CARTESIAN_POINT('Ctrl Pts',(-0.810556943749999,58.4229166676226,1.40392580900275));
#8725=CARTESIAN_POINT('Ctrl Pts',(-1.6211138875,58.3645833342893,0.935950539335167));
#8726=CARTESIAN_POINT('Ctrl Pts',(-1.6211138875,58.3062500009559,0.));
#8727=CARTESIAN_POINT('Ctrl Pts',(-1.6211138875,58.2479166676226,-0.935950539335166));
#8728=CARTESIAN_POINT('Ctrl Pts',(-0.81055694375,58.1895833342893,-1.40392580900275));
#8729=CARTESIAN_POINT('Ctrl Pts',(-1.14620883215705E-16,58.1312500009559,
-1.87190107867033));
#8730=CARTESIAN_POINT('Ctrl Pts',(0.81055694375,58.0729166676226,-1.40392580900275));
#8731=CARTESIAN_POINT('Ctrl Pts',(1.6211138875,58.0145833342893,-0.935950539335166));
#8732=CARTESIAN_POINT('Ctrl Pts',(1.6211138875,57.9562500009559,-1.9852919333802E-16));
#8733=CARTESIAN_POINT('Ctrl Pts',(1.6211138875,57.8979166676226,0.935950539335165));
#8734=CARTESIAN_POINT('Ctrl Pts',(0.810556943750001,57.8395833342893,1.40392580900275));
#8735=CARTESIAN_POINT('Ctrl Pts',(3.43862649647115E-16,57.7812500009559,
1.87190107867033));
#8736=CARTESIAN_POINT('Ctrl Pts',(-0.810556943749999,57.7229166676226,1.40392580900275));
#8737=CARTESIAN_POINT('Ctrl Pts',(-1.6211138875,57.6645833342893,0.935950539335167));
#8738=CARTESIAN_POINT('Ctrl Pts',(-1.6211138875,57.6062500009559,0.));
#8739=CARTESIAN_POINT('Ctrl Pts',(-1.6211138875,57.5479166676226,-0.935950539335166));
#8740=CARTESIAN_POINT('Ctrl Pts',(-0.81055694375,57.4895833342893,-1.40392580900275));
#8741=CARTESIAN_POINT('Ctrl Pts',(-1.14620883215705E-16,57.4312500009559,
-1.87190107867033));
#8742=CARTESIAN_POINT('Ctrl Pts',(0.81055694375,57.3729166676226,-1.40392580900275));
#8743=CARTESIAN_POINT('Ctrl Pts',(1.6211138875,57.3145833342893,-0.935950539335166));
#8744=CARTESIAN_POINT('Ctrl Pts',(1.6211138875,57.2562500009559,-1.9852919333802E-16));
#8745=CARTESIAN_POINT('Ctrl Pts',(1.6211138875,57.1979166676226,0.935950539335165));
#8746=CARTESIAN_POINT('Ctrl Pts',(0.810556943750001,57.1395833342893,1.40392580900275));
#8747=CARTESIAN_POINT('Ctrl Pts',(3.43862649647115E-16,57.0812500009559,
1.87190107867033));
#8748=CARTESIAN_POINT('Ctrl Pts',(-0.810556943749999,57.0229166676226,1.40392580900275));
#8749=CARTESIAN_POINT('Ctrl Pts',(-1.6211138875,56.9645833342893,0.935950539335167));
#8750=CARTESIAN_POINT('Ctrl Pts',(-1.6211138875,56.9062500009559,0.));
#8751=CARTESIAN_POINT('Ctrl Pts',(-1.6211138875,56.8479166676226,-0.935950539335166));
#8752=CARTESIAN_POINT('Ctrl Pts',(-0.81055694375,56.7895833342893,-1.40392580900275));
#8753=CARTESIAN_POINT('Ctrl Pts',(-1.14620883215705E-16,56.7312500009559,
-1.87190107867033));
#8754=CARTESIAN_POINT('Ctrl Pts',(0.81055694375,56.6729166676226,-1.40392580900275));
#8755=CARTESIAN_POINT('Ctrl Pts',(1.6211138875,56.6145833342893,-0.935950539335166));
#8756=CARTESIAN_POINT('Ctrl Pts',(1.6211138875,56.5562500009559,-1.9852919333802E-16));
#8757=CARTESIAN_POINT('Ctrl Pts',(1.6211138875,56.4979166676226,0.935950539335165));
#8758=CARTESIAN_POINT('Ctrl Pts',(0.810556943750001,56.4395833342893,1.40392580900275));
#8759=CARTESIAN_POINT('Ctrl Pts',(3.43862649647115E-16,56.3812500009559,
1.87190107867033));
#8760=CARTESIAN_POINT('Ctrl Pts',(-0.810556943749999,56.3229166676226,1.40392580900275));
#8761=CARTESIAN_POINT('Ctrl Pts',(-1.6211138875,56.2645833342893,0.935950539335167));
#8762=CARTESIAN_POINT('Ctrl Pts',(-1.6211138875,56.2062500009559,0.));
#8763=CARTESIAN_POINT('Ctrl Pts',(-1.6211138875,56.1479166676226,-0.935950539335166));
#8764=CARTESIAN_POINT('Ctrl Pts',(-0.81055694375,56.0895833342893,-1.40392580900275));
#8765=CARTESIAN_POINT('Ctrl Pts',(-1.14620883215705E-16,56.0312500009559,
-1.87190107867033));
#8766=CARTESIAN_POINT('Ctrl Pts',(0.81055694375,55.9729166676226,-1.40392580900275));
#8767=CARTESIAN_POINT('Ctrl Pts',(1.6211138875,55.9145833342893,-0.935950539335166));
#8768=CARTESIAN_POINT('Ctrl Pts',(1.6211138875,55.8562500009559,-1.9852919333802E-16));
#8769=CARTESIAN_POINT('Ctrl Pts',(1.6211138875,55.7979166676226,0.935950539335165));
#8770=CARTESIAN_POINT('Ctrl Pts',(0.810556943750001,55.7395833342893,1.40392580900275));
#8771=CARTESIAN_POINT('Ctrl Pts',(3.43862649647115E-16,55.6812500009559,
1.87190107867033));
#8772=CARTESIAN_POINT('Ctrl Pts',(-0.810556943749999,55.6229166676226,1.40392580900275));
#8773=CARTESIAN_POINT('Ctrl Pts',(-1.6211138875,55.5645833342893,0.935950539335167));
#8774=CARTESIAN_POINT('Ctrl Pts',(-1.6211138875,55.5062500009559,0.));
#8775=CARTESIAN_POINT('Ctrl Pts',(-1.6211138875,55.4479166676226,-0.935950539335166));
#8776=CARTESIAN_POINT('Ctrl Pts',(-0.81055694375,55.3895833342893,-1.40392580900275));
#8777=CARTESIAN_POINT('Ctrl Pts',(-1.14620883215705E-16,55.3312500009559,
-1.87190107867033));
#8778=CARTESIAN_POINT('Ctrl Pts',(0.81055694375,55.2729166676226,-1.40392580900275));
#8779=CARTESIAN_POINT('Ctrl Pts',(1.6211138875,55.2145833342893,-0.935950539335166));
#8780=CARTESIAN_POINT('Ctrl Pts',(1.6211138875,55.1562500009559,-1.9852919333802E-16));
#8781=CARTESIAN_POINT('Ctrl Pts',(1.6211138875,55.0979166676226,0.935950539335165));
#8782=CARTESIAN_POINT('Ctrl Pts',(0.810556943750001,55.0395833342893,1.40392580900275));
#8783=CARTESIAN_POINT('Ctrl Pts',(3.43862649647115E-16,54.9812500009559,
1.87190107867033));
#8784=CARTESIAN_POINT('Ctrl Pts',(-0.810556943749999,54.9229166676226,1.40392580900275));
#8785=CARTESIAN_POINT('Ctrl Pts',(-1.6211138875,54.8645833342893,0.935950539335167));
#8786=CARTESIAN_POINT('Ctrl Pts',(-1.6211138875,54.8062500009559,0.));
#8787=CARTESIAN_POINT('Ctrl Pts',(-1.6211138875,54.7479166676226,-0.935950539335166));
#8788=CARTESIAN_POINT('Ctrl Pts',(-0.81055694375,54.6895833342893,-1.40392580900275));
#8789=CARTESIAN_POINT('Ctrl Pts',(-1.14620883215705E-16,54.6312500009559,
-1.87190107867033));
#8790=CARTESIAN_POINT('Ctrl Pts',(0.81055694375,54.5729166676226,-1.40392580900275));
#8791=CARTESIAN_POINT('Ctrl Pts',(1.6211138875,54.5145833342892,-0.935950539335166));
#8792=CARTESIAN_POINT('Ctrl Pts',(1.6211138875,54.4562500009559,-1.9852919333802E-16));
#8793=CARTESIAN_POINT('Ctrl Pts',(1.6211138875,54.3979166676226,0.935950539335165));
#8794=CARTESIAN_POINT('Ctrl Pts',(0.810556943750001,54.3395833342893,1.40392580900275));
#8795=CARTESIAN_POINT('Ctrl Pts',(3.43862649647115E-16,54.2812500009559,
1.87190107867033));
#8796=CARTESIAN_POINT('Ctrl Pts',(-0.810556943749999,54.2229166676226,1.40392580900275));
#8797=CARTESIAN_POINT('Ctrl Pts',(-1.6211138875,54.1645833342893,0.935950539335167));
#8798=CARTESIAN_POINT('Ctrl Pts',(-1.6211138875,54.1062500009559,0.));
#8799=CARTESIAN_POINT('Ctrl Pts',(-1.6211138875,54.0479166676226,-0.935950539335166));
#8800=CARTESIAN_POINT('Ctrl Pts',(-0.81055694375,53.9895833342893,-1.40392580900275));
#8801=CARTESIAN_POINT('Ctrl Pts',(-1.14620883215705E-16,53.9312500009559,
-1.87190107867033));
#8802=CARTESIAN_POINT('Ctrl Pts',(0.81055694375,53.8729166676226,-1.40392580900275));
#8803=CARTESIAN_POINT('Ctrl Pts',(1.6211138875,53.8145833342893,-0.935950539335166));
#8804=CARTESIAN_POINT('Ctrl Pts',(1.6211138875,53.7562500009559,-1.9852919333802E-16));
#8805=CARTESIAN_POINT('Ctrl Pts',(1.6211138875,53.6979166676226,0.935950539335165));
#8806=CARTESIAN_POINT('Ctrl Pts',(0.810556943750001,53.6395833342893,1.40392580900275));
#8807=CARTESIAN_POINT('Ctrl Pts',(3.43862649647115E-16,53.5812500009559,
1.87190107867033));
#8808=CARTESIAN_POINT('Ctrl Pts',(-0.810556943749999,53.5229166676226,1.40392580900275));
#8809=CARTESIAN_POINT('Ctrl Pts',(-1.6211138875,53.4645833342893,0.935950539335167));
#8810=CARTESIAN_POINT('Ctrl Pts',(-1.6211138875,53.4062500009559,0.));
#8811=CARTESIAN_POINT('Ctrl Pts',(-1.6211138875,53.3479166676226,-0.935950539335166));
#8812=CARTESIAN_POINT('Ctrl Pts',(-0.81055694375,53.2895833342893,-1.40392580900275));
#8813=CARTESIAN_POINT('Ctrl Pts',(-1.14620883215705E-16,53.2312500009559,
-1.87190107867033));
#8814=CARTESIAN_POINT('Ctrl Pts',(0.81055694375,53.1729166676226,-1.40392580900275));
#8815=CARTESIAN_POINT('Ctrl Pts',(1.6211138875,53.1145833342893,-0.935950539335166));
#8816=CARTESIAN_POINT('Ctrl Pts',(1.6211138875,53.0562500009559,-1.9852919333802E-16));
#8817=CARTESIAN_POINT('Ctrl Pts',(1.6211138875,52.9979166676226,0.935950539335165));
#8818=CARTESIAN_POINT('Ctrl Pts',(0.810556943750001,52.9395833342893,1.40392580900275));
#8819=CARTESIAN_POINT('Ctrl Pts',(3.43862649647115E-16,52.8812500009559,
1.87190107867033));
#8820=CARTESIAN_POINT('Ctrl Pts',(-0.810556943749999,52.8229166676226,1.40392580900275));
#8821=CARTESIAN_POINT('Ctrl Pts',(-1.6211138875,52.7645833342893,0.935950539335167));
#8822=CARTESIAN_POINT('Ctrl Pts',(-1.6211138875,52.7062500009559,0.));
#8823=CARTESIAN_POINT('Ctrl Pts',(-1.6211138875,52.6479166676226,-0.935950539335166));
#8824=CARTESIAN_POINT('Ctrl Pts',(-0.81055694375,52.5895833342893,-1.40392580900275));
#8825=CARTESIAN_POINT('Ctrl Pts',(-1.14620883215705E-16,52.5312500009559,
-1.87190107867033));
#8826=CARTESIAN_POINT('Ctrl Pts',(0.81055694375,52.4729166676226,-1.40392580900275));
#8827=CARTESIAN_POINT('Ctrl Pts',(1.6211138875,52.4145833342893,-0.935950539335166));
#8828=CARTESIAN_POINT('Ctrl Pts',(1.6211138875,52.3562500009559,-1.9852919333802E-16));
#8829=CARTESIAN_POINT('Ctrl Pts',(1.6211138875,52.2979166676226,0.935950539335165));
#8830=CARTESIAN_POINT('Ctrl Pts',(0.810556943750001,52.2395833342893,1.40392580900275));
#8831=CARTESIAN_POINT('Ctrl Pts',(3.43862649647115E-16,52.1812500009559,
1.87190107867033));
#8832=CARTESIAN_POINT('Ctrl Pts',(-0.810556943749999,52.1229166676226,1.40392580900275));
#8833=CARTESIAN_POINT('Ctrl Pts',(-1.6211138875,52.0645833342893,0.935950539335167));
#8834=CARTESIAN_POINT('Ctrl Pts',(-1.6211138875,52.0062500009559,0.));
#8835=CARTESIAN_POINT('Ctrl Pts',(-1.6211138875,51.9479166676226,-0.935950539335166));
#8836=CARTESIAN_POINT('Ctrl Pts',(-0.81055694375,51.8895833342893,-1.40392580900275));
#8837=CARTESIAN_POINT('Ctrl Pts',(-1.14620883215705E-16,51.8312500009559,
-1.87190107867033));
#8838=CARTESIAN_POINT('Ctrl Pts',(0.81055694375,51.7729166676226,-1.40392580900275));
#8839=CARTESIAN_POINT('Ctrl Pts',(1.6211138875,51.7145833342893,-0.935950539335166));
#8840=CARTESIAN_POINT('Ctrl Pts',(1.6211138875,51.6562500009559,-1.9852919333802E-16));
#8841=CARTESIAN_POINT('Ctrl Pts',(1.6211138875,51.5979166676226,0.935950539335165));
#8842=CARTESIAN_POINT('Ctrl Pts',(0.810556943750001,51.5395833342893,1.40392580900275));
#8843=CARTESIAN_POINT('Ctrl Pts',(3.43862649647115E-16,51.4812500009559,
1.87190107867033));
#8844=CARTESIAN_POINT('Ctrl Pts',(-0.810556943749999,51.4229166676226,1.40392580900275));
#8845=CARTESIAN_POINT('Ctrl Pts',(-1.6211138875,51.3645833342893,0.935950539335167));
#8846=CARTESIAN_POINT('Ctrl Pts',(-1.6211138875,51.3062500009559,0.));
#8847=CARTESIAN_POINT('Ctrl Pts',(-1.6211138875,51.2479166676226,-0.935950539335166));
#8848=CARTESIAN_POINT('Ctrl Pts',(-0.81055694375,51.1895833342893,-1.40392580900275));
#8849=CARTESIAN_POINT('Ctrl Pts',(-1.14620883215705E-16,51.1312500009559,
-1.87190107867033));
#8850=CARTESIAN_POINT('Ctrl Pts',(0.81055694375,51.0729166676226,-1.40392580900275));
#8851=CARTESIAN_POINT('Ctrl Pts',(1.6211138875,51.0145833342893,-0.935950539335166));
#8852=CARTESIAN_POINT('Ctrl Pts',(1.6211138875,50.9562500009559,-1.9852919333802E-16));
#8853=CARTESIAN_POINT('Ctrl Pts',(1.6211138875,50.8979166676226,0.935950539335165));
#8854=CARTESIAN_POINT('Ctrl Pts',(0.810556943750001,50.8395833342893,1.40392580900275));
#8855=CARTESIAN_POINT('Ctrl Pts',(3.43862649647115E-16,50.7812500009559,
1.87190107867033));
#8856=CARTESIAN_POINT('Ctrl Pts',(-0.810556943749999,50.7229166676226,1.40392580900275));
#8857=CARTESIAN_POINT('Ctrl Pts',(-1.6211138875,50.6645833342893,0.935950539335167));
#8858=CARTESIAN_POINT('Ctrl Pts',(-1.6211138875,50.6062500009559,0.));
#8859=CARTESIAN_POINT('Ctrl Pts',(-1.6211138875,50.5479166676226,-0.935950539335166));
#8860=CARTESIAN_POINT('Ctrl Pts',(-0.81055694375,50.4895833342893,-1.40392580900275));
#8861=CARTESIAN_POINT('Ctrl Pts',(-1.14620883215705E-16,50.4312500009559,
-1.87190107867033));
#8862=CARTESIAN_POINT('Ctrl Pts',(0.81055694375,50.3729166676226,-1.40392580900275));
#8863=CARTESIAN_POINT('Ctrl Pts',(1.6211138875,50.3145833342893,-0.935950539335166));
#8864=CARTESIAN_POINT('Ctrl Pts',(1.6211138875,50.2562500009559,-1.9852919333802E-16));
#8865=CARTESIAN_POINT('Ctrl Pts',(1.6211138875,50.1979166676226,0.935950539335165));
#8866=CARTESIAN_POINT('Ctrl Pts',(0.810556943750001,50.1395833342893,1.40392580900275));
#8867=CARTESIAN_POINT('Ctrl Pts',(3.43862649647115E-16,50.0812500009559,
1.87190107867033));
#8868=CARTESIAN_POINT('Ctrl Pts',(-0.810556943749999,50.0229166676226,1.40392580900275));
#8869=CARTESIAN_POINT('Ctrl Pts',(-1.6211138875,49.9645833342893,0.935950539335167));
#8870=CARTESIAN_POINT('Ctrl Pts',(-1.6211138875,49.9062500009559,0.));
#8871=CARTESIAN_POINT('Ctrl Pts',(-1.6211138875,49.8479166676226,-0.935950539335166));
#8872=CARTESIAN_POINT('Ctrl Pts',(-0.81055694375,49.7895833342893,-1.40392580900275));
#8873=CARTESIAN_POINT('Ctrl Pts',(-1.14620883215705E-16,49.7312500009559,
-1.87190107867033));
#8874=CARTESIAN_POINT('Ctrl Pts',(0.81055694375,49.6729166676226,-1.40392580900275));
#8875=CARTESIAN_POINT('Ctrl Pts',(1.6211138875,49.6145833342893,-0.935950539335166));
#8876=CARTESIAN_POINT('Ctrl Pts',(1.6211138875,49.5562500009559,-1.9852919333802E-16));
#8877=CARTESIAN_POINT('Ctrl Pts',(1.6211138875,49.4979166676226,0.935950539335165));
#8878=CARTESIAN_POINT('Ctrl Pts',(0.810556943750001,49.4395833342893,1.40392580900275));
#8879=CARTESIAN_POINT('Ctrl Pts',(3.43862649647115E-16,49.3812500009559,
1.87190107867033));
#8880=CARTESIAN_POINT('Ctrl Pts',(-0.810556943749999,49.3229166676226,1.40392580900275));
#8881=CARTESIAN_POINT('Ctrl Pts',(-1.6211138875,49.2645833342893,0.935950539335167));
#8882=CARTESIAN_POINT('Ctrl Pts',(-1.6211138875,49.2062500009559,0.));
#8883=CARTESIAN_POINT('Ctrl Pts',(-1.6211138875,49.1479166676226,-0.935950539335166));
#8884=CARTESIAN_POINT('Ctrl Pts',(-0.81055694375,49.0895833342893,-1.40392580900275));
#8885=CARTESIAN_POINT('Ctrl Pts',(-1.14620883215705E-16,49.0312500009559,
-1.87190107867033));
#8886=CARTESIAN_POINT('Ctrl Pts',(0.81055694375,48.9729166676226,-1.40392580900275));
#8887=CARTESIAN_POINT('Ctrl Pts',(1.6211138875,48.9145833342893,-0.935950539335166));
#8888=CARTESIAN_POINT('Ctrl Pts',(1.6211138875,48.8562500009559,-1.9852919333802E-16));
#8889=CARTESIAN_POINT('Ctrl Pts',(1.6211138875,48.7979166676226,0.935950539335165));
#8890=CARTESIAN_POINT('Ctrl Pts',(0.810556943750001,48.7395833342893,1.40392580900275));
#8891=CARTESIAN_POINT('Ctrl Pts',(3.43862649647115E-16,48.6812500009559,
1.87190107867033));
#8892=CARTESIAN_POINT('Ctrl Pts',(-0.810556943749999,48.6229166676226,1.40392580900275));
#8893=CARTESIAN_POINT('Ctrl Pts',(-1.6211138875,48.5645833342893,0.935950539335167));
#8894=CARTESIAN_POINT('Ctrl Pts',(-1.6211138875,48.5062500009559,0.));
#8895=CARTESIAN_POINT('Ctrl Pts',(-1.6211138875,48.4479166676226,-0.935950539335166));
#8896=CARTESIAN_POINT('Ctrl Pts',(-0.81055694375,48.3895833342893,-1.40392580900275));
#8897=CARTESIAN_POINT('Ctrl Pts',(-1.14620883215705E-16,48.3312500009559,
-1.87190107867033));
#8898=CARTESIAN_POINT('Ctrl Pts',(0.81055694375,48.2729166676226,-1.40392580900275));
#8899=CARTESIAN_POINT('Ctrl Pts',(1.6211138875,48.2145833342893,-0.935950539335166));
#8900=CARTESIAN_POINT('Ctrl Pts',(1.6211138875,48.1562500009559,-1.9852919333802E-16));
#8901=CARTESIAN_POINT('Ctrl Pts',(1.6211138875,48.0979166676226,0.935950539335165));
#8902=CARTESIAN_POINT('Ctrl Pts',(0.810556943750001,48.0395833342893,1.40392580900275));
#8903=CARTESIAN_POINT('Ctrl Pts',(3.43862649647115E-16,47.9812500009559,
1.87190107867033));
#8904=CARTESIAN_POINT('Ctrl Pts',(-0.810556943749999,47.9229166676226,1.40392580900275));
#8905=CARTESIAN_POINT('Ctrl Pts',(-1.6211138875,47.8645833342893,0.935950539335167));
#8906=CARTESIAN_POINT('Ctrl Pts',(-1.6211138875,47.8062500009559,0.));
#8907=CARTESIAN_POINT('Ctrl Pts',(-1.6211138875,47.7479166676226,-0.935950539335166));
#8908=CARTESIAN_POINT('Ctrl Pts',(-0.81055694375,47.6895833342893,-1.40392580900275));
#8909=CARTESIAN_POINT('Ctrl Pts',(-1.14620883215705E-16,47.6312500009559,
-1.87190107867033));
#8910=CARTESIAN_POINT('Ctrl Pts',(0.81055694375,47.5729166676226,-1.40392580900275));
#8911=CARTESIAN_POINT('Ctrl Pts',(1.6211138875,47.5145833342893,-0.935950539335166));
#8912=CARTESIAN_POINT('Ctrl Pts',(1.6211138875,47.4562500009559,-1.9852919333802E-16));
#8913=CARTESIAN_POINT('Ctrl Pts',(1.6211138875,47.3979166676226,0.935950539335165));
#8914=CARTESIAN_POINT('Ctrl Pts',(0.810556943750001,47.3395833342893,1.40392580900275));
#8915=CARTESIAN_POINT('Ctrl Pts',(3.43862649647115E-16,47.2812500009559,
1.87190107867033));
#8916=CARTESIAN_POINT('Ctrl Pts',(-0.810556943749999,47.2229166676226,1.40392580900275));
#8917=CARTESIAN_POINT('Ctrl Pts',(-1.6211138875,47.1645833342893,0.935950539335167));
#8918=CARTESIAN_POINT('Ctrl Pts',(-1.6211138875,47.1062500009559,0.));
#8919=CARTESIAN_POINT('Ctrl Pts',(-1.6211138875,47.0479166676226,-0.935950539335166));
#8920=CARTESIAN_POINT('Ctrl Pts',(-0.81055694375,46.9895833342893,-1.40392580900275));
#8921=CARTESIAN_POINT('Ctrl Pts',(-1.14620883215705E-16,46.9312500009559,
-1.87190107867033));
#8922=CARTESIAN_POINT('Ctrl Pts',(0.81055694375,46.8729166676226,-1.40392580900275));
#8923=CARTESIAN_POINT('Ctrl Pts',(1.6211138875,46.8145833342893,-0.935950539335166));
#8924=CARTESIAN_POINT('Ctrl Pts',(1.6211138875,46.7562500009559,-1.9852919333802E-16));
#8925=CARTESIAN_POINT('Ctrl Pts',(1.6211138875,46.6979166676226,0.935950539335165));
#8926=CARTESIAN_POINT('Ctrl Pts',(0.810556943750001,46.6395833342893,1.40392580900275));
#8927=CARTESIAN_POINT('Ctrl Pts',(3.43862649647115E-16,46.5812500009559,
1.87190107867033));
#8928=CARTESIAN_POINT('Ctrl Pts',(-0.810556943749999,46.5229166676226,1.40392580900275));
#8929=CARTESIAN_POINT('Ctrl Pts',(-1.6211138875,46.4645833342893,0.935950539335167));
#8930=CARTESIAN_POINT('Ctrl Pts',(-1.6211138875,46.4062500009559,0.));
#8931=CARTESIAN_POINT('Ctrl Pts',(-1.6211138875,46.3479166676226,-0.935950539335166));
#8932=CARTESIAN_POINT('Ctrl Pts',(-0.81055694375,46.2895833342893,-1.40392580900275));
#8933=CARTESIAN_POINT('Ctrl Pts',(-1.14620883215705E-16,46.2312500009559,
-1.87190107867033));
#8934=CARTESIAN_POINT('Ctrl Pts',(0.81055694375,46.1729166676226,-1.40392580900275));
#8935=CARTESIAN_POINT('Ctrl Pts',(1.6211138875,46.1145833342893,-0.935950539335166));
#8936=CARTESIAN_POINT('Ctrl Pts',(1.6211138875,46.0562500009559,-1.9852919333802E-16));
#8937=CARTESIAN_POINT('Ctrl Pts',(1.6211138875,45.9979166676226,0.935950539335165));
#8938=CARTESIAN_POINT('Ctrl Pts',(0.810556943750001,45.9395833342893,1.40392580900275));
#8939=CARTESIAN_POINT('Ctrl Pts',(3.43862649647115E-16,45.8812500009559,
1.87190107867033));
#8940=CARTESIAN_POINT('Ctrl Pts',(-0.810556943749999,45.8229166676226,1.40392580900275));
#8941=CARTESIAN_POINT('Ctrl Pts',(-1.6211138875,45.7645833342893,0.935950539335167));
#8942=CARTESIAN_POINT('Ctrl Pts',(-1.6211138875,45.7062500009559,0.));
#8943=CARTESIAN_POINT('Ctrl Pts',(-1.6211138875,45.6479166676226,-0.935950539335166));
#8944=CARTESIAN_POINT('Ctrl Pts',(-0.81055694375,45.5895833342893,-1.40392580900275));
#8945=CARTESIAN_POINT('Ctrl Pts',(-1.14620883215705E-16,45.5312500009559,
-1.87190107867033));
#8946=CARTESIAN_POINT('Ctrl Pts',(0.81055694375,45.4729166676226,-1.40392580900275));
#8947=CARTESIAN_POINT('Ctrl Pts',(1.6211138875,45.4145833342893,-0.935950539335166));
#8948=CARTESIAN_POINT('Ctrl Pts',(1.6211138875,45.3562500009559,-1.9852919333802E-16));
#8949=CARTESIAN_POINT('Ctrl Pts',(1.6211138875,45.2979166676226,0.935950539335165));
#8950=CARTESIAN_POINT('Ctrl Pts',(0.810556943750001,45.2395833342893,1.40392580900275));
#8951=CARTESIAN_POINT('Ctrl Pts',(3.43862649647115E-16,45.1812500009559,
1.87190107867033));
#8952=CARTESIAN_POINT('Ctrl Pts',(-0.810556943749999,45.1229166676226,1.40392580900275));
#8953=CARTESIAN_POINT('Ctrl Pts',(-1.6211138875,45.0645833342893,0.935950539335167));
#8954=CARTESIAN_POINT('Ctrl Pts',(-1.6211138875,45.0062500009559,0.));
#8955=CARTESIAN_POINT('Ctrl Pts',(-1.6211138875,44.9479166676226,-0.935950539335166));
#8956=CARTESIAN_POINT('Ctrl Pts',(-0.81055694375,44.8895833342893,-1.40392580900275));
#8957=CARTESIAN_POINT('Ctrl Pts',(-1.14620883215705E-16,44.8312500009559,
-1.87190107867033));
#8958=CARTESIAN_POINT('Ctrl Pts',(0.81055694375,44.7729166676226,-1.40392580900275));
#8959=CARTESIAN_POINT('Ctrl Pts',(1.6211138875,44.7145833342893,-0.935950539335166));
#8960=CARTESIAN_POINT('Ctrl Pts',(1.6211138875,44.6562500009559,-1.9852919333802E-16));
#8961=CARTESIAN_POINT('Ctrl Pts',(1.6211138875,44.5979166676226,0.935950539335165));
#8962=CARTESIAN_POINT('Ctrl Pts',(0.810556943750001,44.5395833342893,1.40392580900275));
#8963=CARTESIAN_POINT('Ctrl Pts',(3.43862649647115E-16,44.4812500009559,
1.87190107867033));
#8964=CARTESIAN_POINT('Ctrl Pts',(-0.810556943749999,44.4229166676226,1.40392580900275));
#8965=CARTESIAN_POINT('Ctrl Pts',(-1.6211138875,44.3645833342893,0.935950539335167));
#8966=CARTESIAN_POINT('Ctrl Pts',(-1.6211138875,44.3062500009559,0.));
#8967=CARTESIAN_POINT('Ctrl Pts',(-1.6211138875,44.2479166676226,-0.935950539335166));
#8968=CARTESIAN_POINT('Ctrl Pts',(-0.81055694375,44.1895833342893,-1.40392580900275));
#8969=CARTESIAN_POINT('Ctrl Pts',(-1.14620883215705E-16,44.1312500009559,
-1.87190107867033));
#8970=CARTESIAN_POINT('Ctrl Pts',(0.81055694375,44.0729166676226,-1.40392580900275));
#8971=CARTESIAN_POINT('Ctrl Pts',(1.6211138875,44.0145833342893,-0.935950539335166));
#8972=CARTESIAN_POINT('Ctrl Pts',(1.6211138875,43.9562500009559,-1.9852919333802E-16));
#8973=CARTESIAN_POINT('Ctrl Pts',(1.6211138875,43.8979166676226,0.935950539335165));
#8974=CARTESIAN_POINT('Ctrl Pts',(0.810556943750001,43.8395833342893,1.40392580900275));
#8975=CARTESIAN_POINT('Ctrl Pts',(3.43862649647115E-16,43.7812500009559,
1.87190107867033));
#8976=CARTESIAN_POINT('Ctrl Pts',(-0.810556943749999,43.7229166676226,1.40392580900275));
#8977=CARTESIAN_POINT('Ctrl Pts',(-1.6211138875,43.6645833342893,0.935950539335167));
#8978=CARTESIAN_POINT('Ctrl Pts',(-1.6211138875,43.6062500009559,0.));
#8979=CARTESIAN_POINT('Ctrl Pts',(-1.6211138875,43.5479166676226,-0.935950539335166));
#8980=CARTESIAN_POINT('Ctrl Pts',(-0.81055694375,43.4895833342893,-1.40392580900275));
#8981=CARTESIAN_POINT('Ctrl Pts',(-1.14620883215705E-16,43.4312500009559,
-1.87190107867033));
#8982=CARTESIAN_POINT('Ctrl Pts',(0.81055694375,43.3729166676226,-1.40392580900275));
#8983=CARTESIAN_POINT('Ctrl Pts',(1.6211138875,43.3145833342893,-0.935950539335166));
#8984=CARTESIAN_POINT('Ctrl Pts',(1.6211138875,43.2562500009559,-1.9852919333802E-16));
#8985=CARTESIAN_POINT('Ctrl Pts',(1.6211138875,43.1979166676226,0.935950539335165));
#8986=CARTESIAN_POINT('Ctrl Pts',(0.810556943750001,43.1395833342893,1.40392580900275));
#8987=CARTESIAN_POINT('Ctrl Pts',(3.43862649647115E-16,43.0812500009559,
1.87190107867033));
#8988=CARTESIAN_POINT('Ctrl Pts',(-0.810556943749999,43.0229166676226,1.40392580900275));
#8989=CARTESIAN_POINT('Ctrl Pts',(-1.6211138875,42.9645833342893,0.935950539335167));
#8990=CARTESIAN_POINT('Ctrl Pts',(-1.6211138875,42.9062500009559,0.));
#8991=CARTESIAN_POINT('Ctrl Pts',(-1.6211138875,42.8479166676226,-0.935950539335166));
#8992=CARTESIAN_POINT('Ctrl Pts',(-0.81055694375,42.7895833342893,-1.40392580900275));
#8993=CARTESIAN_POINT('Ctrl Pts',(-1.14620883215705E-16,42.7312500009559,
-1.87190107867033));
#8994=CARTESIAN_POINT('Ctrl Pts',(0.81055694375,42.6729166676226,-1.40392580900275));
#8995=CARTESIAN_POINT('Ctrl Pts',(1.6211138875,42.6145833342893,-0.935950539335166));
#8996=CARTESIAN_POINT('Ctrl Pts',(1.6211138875,42.5562500009559,-1.9852919333802E-16));
#8997=CARTESIAN_POINT('Ctrl Pts',(1.6211138875,42.4979166676226,0.935950539335165));
#8998=CARTESIAN_POINT('Ctrl Pts',(0.810556943750001,42.4395833342893,1.40392580900275));
#8999=CARTESIAN_POINT('Ctrl Pts',(3.43862649647115E-16,42.3812500009559,
1.87190107867033));
#9000=CARTESIAN_POINT('Ctrl Pts',(-0.810556943749999,42.3229166676226,1.40392580900275));
#9001=CARTESIAN_POINT('Ctrl Pts',(-1.6211138875,42.2645833342893,0.935950539335167));
#9002=CARTESIAN_POINT('Ctrl Pts',(-1.6211138875,42.2062500009559,0.));
#9003=CARTESIAN_POINT('Ctrl Pts',(-1.6211138875,42.1479166676226,-0.935950539335166));
#9004=CARTESIAN_POINT('Ctrl Pts',(-0.81055694375,42.0895833342893,-1.40392580900275));
#9005=CARTESIAN_POINT('Ctrl Pts',(-1.14620883215705E-16,42.0312500009559,
-1.87190107867033));
#9006=CARTESIAN_POINT('Ctrl Pts',(0.81055694375,41.9729166676226,-1.40392580900275));
#9007=CARTESIAN_POINT('Ctrl Pts',(1.6211138875,41.9145833342893,-0.935950539335166));
#9008=CARTESIAN_POINT('Ctrl Pts',(1.6211138875,41.8562500009559,-1.9852919333802E-16));
#9009=CARTESIAN_POINT('Ctrl Pts',(1.6211138875,41.7979166676226,0.935950539335165));
#9010=CARTESIAN_POINT('Ctrl Pts',(0.810556943750001,41.7395833342893,1.40392580900275));
#9011=CARTESIAN_POINT('Ctrl Pts',(3.43862649647115E-16,41.6812500009559,
1.87190107867033));
#9012=CARTESIAN_POINT('Ctrl Pts',(-0.810556943749999,41.6229166676226,1.40392580900275));
#9013=CARTESIAN_POINT('Ctrl Pts',(-1.6211138875,41.5645833342893,0.935950539335167));
#9014=CARTESIAN_POINT('Ctrl Pts',(-1.6211138875,41.5062500009559,0.));
#9015=CARTESIAN_POINT('Ctrl Pts',(-1.6211138875,41.4479166676226,-0.935950539335166));
#9016=CARTESIAN_POINT('Ctrl Pts',(-0.81055694375,41.3895833342893,-1.40392580900275));
#9017=CARTESIAN_POINT('Ctrl Pts',(-1.14620883215705E-16,41.3312500009559,
-1.87190107867033));
#9018=CARTESIAN_POINT('Ctrl Pts',(0.81055694375,41.2729166676226,-1.40392580900275));
#9019=CARTESIAN_POINT('Ctrl Pts',(1.6211138875,41.2145833342893,-0.935950539335166));
#9020=CARTESIAN_POINT('Ctrl Pts',(1.6211138875,41.1562500009559,-1.9852919333802E-16));
#9021=CARTESIAN_POINT('Ctrl Pts',(1.6211138875,41.0979166676226,0.935950539335165));
#9022=CARTESIAN_POINT('Ctrl Pts',(0.810556943750001,41.0395833342893,1.40392580900275));
#9023=CARTESIAN_POINT('Ctrl Pts',(3.43862649647115E-16,40.9812500009559,
1.87190107867033));
#9024=CARTESIAN_POINT('Ctrl Pts',(-0.810556943749999,40.9229166676226,1.40392580900275));
#9025=CARTESIAN_POINT('Ctrl Pts',(-1.6211138875,40.8645833342893,0.935950539335167));
#9026=CARTESIAN_POINT('Ctrl Pts',(-1.6211138875,40.8062500009559,0.));
#9027=CARTESIAN_POINT('Ctrl Pts',(-1.6211138875,40.7479166676226,-0.935950539335166));
#9028=CARTESIAN_POINT('Ctrl Pts',(-0.81055694375,40.6895833342893,-1.40392580900275));
#9029=CARTESIAN_POINT('Ctrl Pts',(-1.14620883215705E-16,40.6312500009559,
-1.87190107867033));
#9030=CARTESIAN_POINT('Ctrl Pts',(0.81055694375,40.5729166676226,-1.40392580900275));
#9031=CARTESIAN_POINT('Ctrl Pts',(1.6211138875,40.5145833342893,-0.935950539335166));
#9032=CARTESIAN_POINT('Ctrl Pts',(1.6211138875,40.4562500009559,-1.9852919333802E-16));
#9033=CARTESIAN_POINT('Ctrl Pts',(1.6211138875,40.3979166676226,0.935950539335165));
#9034=CARTESIAN_POINT('Ctrl Pts',(0.810556943750001,40.3395833342893,1.40392580900275));
#9035=CARTESIAN_POINT('Ctrl Pts',(3.43862649647115E-16,40.2812500009559,
1.87190107867033));
#9036=CARTESIAN_POINT('Ctrl Pts',(-0.810556943749999,40.2229166676226,1.40392580900275));
#9037=CARTESIAN_POINT('Ctrl Pts',(-1.6211138875,40.1645833342893,0.935950539335167));
#9038=CARTESIAN_POINT('Ctrl Pts',(-1.6211138875,40.1062500009559,0.));
#9039=CARTESIAN_POINT('Ctrl Pts',(-1.6211138875,40.0479166676226,-0.935950539335166));
#9040=CARTESIAN_POINT('Ctrl Pts',(-0.81055694375,39.9895833342893,-1.40392580900275));
#9041=CARTESIAN_POINT('Ctrl Pts',(-1.14620883215705E-16,39.9312500009559,
-1.87190107867033));
#9042=CARTESIAN_POINT('Ctrl Pts',(0.81055694375,39.8729166676226,-1.40392580900275));
#9043=CARTESIAN_POINT('Ctrl Pts',(1.6211138875,39.8145833342893,-0.935950539335166));
#9044=CARTESIAN_POINT('Ctrl Pts',(1.6211138875,39.7562500009559,-1.9852919333802E-16));
#9045=CARTESIAN_POINT('Ctrl Pts',(1.6211138875,39.6979166676226,0.935950539335165));
#9046=CARTESIAN_POINT('Ctrl Pts',(0.810556943750001,39.6395833342893,1.40392580900275));
#9047=CARTESIAN_POINT('Ctrl Pts',(3.43862649647115E-16,39.5812500009559,
1.87190107867033));
#9048=CARTESIAN_POINT('Ctrl Pts',(-0.810556943749999,39.5229166676226,1.40392580900275));
#9049=CARTESIAN_POINT('Ctrl Pts',(-1.6211138875,39.4645833342893,0.935950539335167));
#9050=CARTESIAN_POINT('Ctrl Pts',(-1.6211138875,39.4062500009559,0.));
#9051=CARTESIAN_POINT('Ctrl Pts',(-1.6211138875,39.3479166676226,-0.935950539335166));
#9052=CARTESIAN_POINT('Ctrl Pts',(-0.81055694375,39.2895833342893,-1.40392580900275));
#9053=CARTESIAN_POINT('Ctrl Pts',(-1.14620883215705E-16,39.2312500009559,
-1.87190107867033));
#9054=CARTESIAN_POINT('Ctrl Pts',(0.81055694375,39.1729166676226,-1.40392580900275));
#9055=CARTESIAN_POINT('Ctrl Pts',(1.6211138875,39.1145833342893,-0.935950539335166));
#9056=CARTESIAN_POINT('Ctrl Pts',(1.6211138875,39.0562500009559,-1.9852919333802E-16));
#9057=CARTESIAN_POINT('Ctrl Pts',(1.6211138875,38.9979166676226,0.935950539335165));
#9058=CARTESIAN_POINT('Ctrl Pts',(0.810556943750001,38.9395833342893,1.40392580900275));
#9059=CARTESIAN_POINT('Ctrl Pts',(3.43862649647115E-16,38.8812500009559,
1.87190107867033));
#9060=CARTESIAN_POINT('Ctrl Pts',(-0.810556943749999,38.8229166676226,1.40392580900275));
#9061=CARTESIAN_POINT('Ctrl Pts',(-1.6211138875,38.7645833342893,0.935950539335167));
#9062=CARTESIAN_POINT('Ctrl Pts',(-1.6211138875,38.7062500009559,0.));
#9063=CARTESIAN_POINT('Ctrl Pts',(-1.6211138875,38.6479166676226,-0.935950539335166));
#9064=CARTESIAN_POINT('Ctrl Pts',(-0.81055694375,38.5895833342893,-1.40392580900275));
#9065=CARTESIAN_POINT('Ctrl Pts',(-1.14620883215705E-16,38.5312500009559,
-1.87190107867033));
#9066=CARTESIAN_POINT('Ctrl Pts',(0.81055694375,38.4729166676226,-1.40392580900275));
#9067=CARTESIAN_POINT('Ctrl Pts',(1.6211138875,38.4145833342893,-0.935950539335166));
#9068=CARTESIAN_POINT('Ctrl Pts',(1.6211138875,38.3562500009559,-1.9852919333802E-16));
#9069=CARTESIAN_POINT('Ctrl Pts',(1.6211138875,38.2979166676226,0.935950539335165));
#9070=CARTESIAN_POINT('Ctrl Pts',(0.810556943750001,38.2395833342893,1.40392580900275));
#9071=CARTESIAN_POINT('Ctrl Pts',(3.43862649647115E-16,38.1812500009559,
1.87190107867033));
#9072=CARTESIAN_POINT('Ctrl Pts',(-0.810556943749999,38.1229166676226,1.40392580900275));
#9073=CARTESIAN_POINT('Ctrl Pts',(-1.6211138875,38.0645833342893,0.935950539335167));
#9074=CARTESIAN_POINT('Ctrl Pts',(-1.6211138875,38.0062500009559,0.));
#9075=CARTESIAN_POINT('Ctrl Pts',(-1.6211138875,37.9479166676226,-0.935950539335166));
#9076=CARTESIAN_POINT('Ctrl Pts',(-0.81055694375,37.8895833342893,-1.40392580900275));
#9077=CARTESIAN_POINT('Ctrl Pts',(-1.14620883215705E-16,37.8312500009559,
-1.87190107867033));
#9078=CARTESIAN_POINT('Ctrl Pts',(0.81055694375,37.7729166676226,-1.40392580900275));
#9079=CARTESIAN_POINT('Ctrl Pts',(1.6211138875,37.7145833342893,-0.935950539335166));
#9080=CARTESIAN_POINT('Ctrl Pts',(1.6211138875,37.6562500009559,-1.9852919333802E-16));
#9081=CARTESIAN_POINT('Ctrl Pts',(1.6211138875,37.5979166676226,0.935950539335165));
#9082=CARTESIAN_POINT('Ctrl Pts',(0.810556943750001,37.5395833342893,1.40392580900275));
#9083=CARTESIAN_POINT('Ctrl Pts',(3.43862649647115E-16,37.4812500009559,
1.87190107867033));
#9084=CARTESIAN_POINT('Ctrl Pts',(-0.810556943749999,37.4229166676226,1.40392580900275));
#9085=CARTESIAN_POINT('Ctrl Pts',(-1.6211138875,37.3645833342893,0.935950539335167));
#9086=CARTESIAN_POINT('Ctrl Pts',(-1.6211138875,37.3062500009559,0.));
#9087=CARTESIAN_POINT('Ctrl Pts',(-1.6211138875,37.2479166676226,-0.935950539335166));
#9088=CARTESIAN_POINT('Ctrl Pts',(-0.81055694375,37.1895833342893,-1.40392580900275));
#9089=CARTESIAN_POINT('Ctrl Pts',(-1.14620883215705E-16,37.1312500009559,
-1.87190107867033));
#9090=CARTESIAN_POINT('Ctrl Pts',(0.81055694375,37.0729166676226,-1.40392580900275));
#9091=CARTESIAN_POINT('Ctrl Pts',(1.6211138875,37.0145833342893,-0.935950539335166));
#9092=CARTESIAN_POINT('Ctrl Pts',(1.6211138875,36.9562500009559,-1.9852919333802E-16));
#9093=CARTESIAN_POINT('Ctrl Pts',(1.6211138875,36.8979166676226,0.935950539335165));
#9094=CARTESIAN_POINT('Ctrl Pts',(0.810556943750001,36.8395833342893,1.40392580900275));
#9095=CARTESIAN_POINT('Ctrl Pts',(3.43862649647115E-16,36.7812500009559,
1.87190107867033));
#9096=CARTESIAN_POINT('Ctrl Pts',(-0.810556943749999,36.7229166676226,1.40392580900275));
#9097=CARTESIAN_POINT('Ctrl Pts',(-1.6211138875,36.6645833342893,0.935950539335167));
#9098=CARTESIAN_POINT('Ctrl Pts',(-1.6211138875,36.6062500009559,0.));
#9099=CARTESIAN_POINT('Ctrl Pts',(-1.6211138875,36.5479166676226,-0.935950539335166));
#9100=CARTESIAN_POINT('Ctrl Pts',(-0.81055694375,36.4895833342893,-1.40392580900275));
#9101=CARTESIAN_POINT('Ctrl Pts',(-1.14620883215705E-16,36.4312500009559,
-1.87190107867033));
#9102=CARTESIAN_POINT('Ctrl Pts',(0.81055694375,36.3729166676226,-1.40392580900275));
#9103=CARTESIAN_POINT('Ctrl Pts',(1.6211138875,36.3145833342893,-0.935950539335166));
#9104=CARTESIAN_POINT('Ctrl Pts',(1.6211138875,36.2562500009559,-1.9852919333802E-16));
#9105=CARTESIAN_POINT('Ctrl Pts',(1.6211138875,36.1979166676226,0.935950539335165));
#9106=CARTESIAN_POINT('Ctrl Pts',(0.810556943750001,36.1395833342893,1.40392580900275));
#9107=CARTESIAN_POINT('Ctrl Pts',(3.43862649647115E-16,36.0812500009559,
1.87190107867033));
#9108=CARTESIAN_POINT('Ctrl Pts',(-0.810556943749999,36.0229166676226,1.40392580900275));
#9109=CARTESIAN_POINT('Ctrl Pts',(-1.6211138875,35.9645833342893,0.935950539335167));
#9110=CARTESIAN_POINT('Ctrl Pts',(-1.6211138875,35.9062500009559,0.));
#9111=CARTESIAN_POINT('Ctrl Pts',(-1.6211138875,35.8479166676226,-0.935950539335166));
#9112=CARTESIAN_POINT('Ctrl Pts',(-0.81055694375,35.7895833342893,-1.40392580900275));
#9113=CARTESIAN_POINT('Ctrl Pts',(-1.14620883215705E-16,35.7312500009559,
-1.87190107867033));
#9114=CARTESIAN_POINT('Ctrl Pts',(0.81055694375,35.6729166676226,-1.40392580900275));
#9115=CARTESIAN_POINT('Ctrl Pts',(1.6211138875,35.6145833342893,-0.935950539335166));
#9116=CARTESIAN_POINT('Ctrl Pts',(1.6211138875,35.5562500009559,-1.9852919333802E-16));
#9117=CARTESIAN_POINT('Ctrl Pts',(1.6211138875,35.4979166676226,0.935950539335165));
#9118=CARTESIAN_POINT('Ctrl Pts',(0.810556943750001,35.4395833342893,1.40392580900275));
#9119=CARTESIAN_POINT('Ctrl Pts',(3.43862649647115E-16,35.3812500009559,
1.87190107867033));
#9120=CARTESIAN_POINT('Ctrl Pts',(-0.810556943749999,35.3229166676226,1.40392580900275));
#9121=CARTESIAN_POINT('Ctrl Pts',(-1.6211138875,35.2645833342893,0.935950539335167));
#9122=CARTESIAN_POINT('Ctrl Pts',(-1.6211138875,35.2062500009559,0.));
#9123=CARTESIAN_POINT('Ctrl Pts',(-1.6211138875,35.1479166676226,-0.935950539335166));
#9124=CARTESIAN_POINT('Ctrl Pts',(-0.81055694375,35.0895833342893,-1.40392580900275));
#9125=CARTESIAN_POINT('Ctrl Pts',(-1.14620883215705E-16,35.0312500009559,
-1.87190107867033));
#9126=CARTESIAN_POINT('Ctrl Pts',(0.81055694375,34.9729166676226,-1.40392580900275));
#9127=CARTESIAN_POINT('Ctrl Pts',(1.6211138875,34.9145833342893,-0.935950539335166));
#9128=CARTESIAN_POINT('Ctrl Pts',(1.6211138875,34.8562500009559,-1.9852919333802E-16));
#9129=CARTESIAN_POINT('Ctrl Pts',(1.6211138875,34.7979166676226,0.935950539335165));
#9130=CARTESIAN_POINT('Ctrl Pts',(0.810556943750001,34.7395833342893,1.40392580900275));
#9131=CARTESIAN_POINT('Ctrl Pts',(3.43862649647115E-16,34.6812500009559,
1.87190107867033));
#9132=CARTESIAN_POINT('Ctrl Pts',(-0.810556943749999,34.6229166676226,1.40392580900275));
#9133=CARTESIAN_POINT('Ctrl Pts',(-1.6211138875,34.5645833342893,0.935950539335167));
#9134=CARTESIAN_POINT('Ctrl Pts',(-1.6211138875,34.5062500009559,0.));
#9135=CARTESIAN_POINT('Ctrl Pts',(-1.6211138875,34.4479166676226,-0.935950539335166));
#9136=CARTESIAN_POINT('Ctrl Pts',(-0.81055694375,34.3895833342893,-1.40392580900275));
#9137=CARTESIAN_POINT('Ctrl Pts',(-1.14620883215705E-16,34.3312500009559,
-1.87190107867033));
#9138=CARTESIAN_POINT('Ctrl Pts',(0.81055694375,34.2729166676226,-1.40392580900275));
#9139=CARTESIAN_POINT('Ctrl Pts',(1.6211138875,34.2145833342893,-0.935950539335166));
#9140=CARTESIAN_POINT('Ctrl Pts',(1.6211138875,34.1562500009559,-1.9852919333802E-16));
#9141=CARTESIAN_POINT('Ctrl Pts',(1.6211138875,34.0979166676226,0.935950539335165));
#9142=CARTESIAN_POINT('Ctrl Pts',(0.810556943750001,34.0395833342893,1.40392580900275));
#9143=CARTESIAN_POINT('Ctrl Pts',(3.43862649647115E-16,33.9812500009559,
1.87190107867033));
#9144=CARTESIAN_POINT('Ctrl Pts',(-0.810556943749999,33.9229166676226,1.40392580900275));
#9145=CARTESIAN_POINT('Ctrl Pts',(-1.6211138875,33.8645833342893,0.935950539335167));
#9146=CARTESIAN_POINT('Ctrl Pts',(-1.6211138875,33.8062500009559,0.));
#9147=CARTESIAN_POINT('Ctrl Pts',(-1.6211138875,33.7479166676226,-0.935950539335166));
#9148=CARTESIAN_POINT('Ctrl Pts',(-0.81055694375,33.6895833342893,-1.40392580900275));
#9149=CARTESIAN_POINT('Ctrl Pts',(-1.14620883215705E-16,33.6312500009559,
-1.87190107867033));
#9150=CARTESIAN_POINT('Ctrl Pts',(0.81055694375,33.5729166676226,-1.40392580900275));
#9151=CARTESIAN_POINT('Ctrl Pts',(1.6211138875,33.5145833342893,-0.935950539335166));
#9152=CARTESIAN_POINT('Ctrl Pts',(1.6211138875,33.4562500009559,-1.9852919333802E-16));
#9153=CARTESIAN_POINT('Ctrl Pts',(1.6211138875,33.3979166676226,0.935950539335165));
#9154=CARTESIAN_POINT('Ctrl Pts',(0.810556943750001,33.3395833342893,1.40392580900275));
#9155=CARTESIAN_POINT('Ctrl Pts',(3.43862649647115E-16,33.2812500009559,
1.87190107867033));
#9156=CARTESIAN_POINT('Ctrl Pts',(-0.810556943749999,33.2229166676226,1.40392580900275));
#9157=CARTESIAN_POINT('Ctrl Pts',(-1.6211138875,33.1645833342893,0.935950539335167));
#9158=CARTESIAN_POINT('Ctrl Pts',(-1.6211138875,33.1062500009559,0.));
#9159=CARTESIAN_POINT('Ctrl Pts',(-1.6211138875,33.0479166676226,-0.935950539335166));
#9160=CARTESIAN_POINT('Ctrl Pts',(-0.81055694375,32.9895833342893,-1.40392580900275));
#9161=CARTESIAN_POINT('Ctrl Pts',(-1.14620883215705E-16,32.9312500009559,
-1.87190107867033));
#9162=CARTESIAN_POINT('Ctrl Pts',(0.81055694375,32.8729166676226,-1.40392580900275));
#9163=CARTESIAN_POINT('Ctrl Pts',(1.6211138875,32.8145833342893,-0.935950539335166));
#9164=CARTESIAN_POINT('Ctrl Pts',(1.6211138875,32.7562500009559,-1.9852919333802E-16));
#9165=CARTESIAN_POINT('Ctrl Pts',(1.6211138875,32.6979166676226,0.935950539335165));
#9166=CARTESIAN_POINT('Ctrl Pts',(0.810556943750001,32.6395833342893,1.40392580900275));
#9167=CARTESIAN_POINT('Ctrl Pts',(3.43862649647115E-16,32.5812500009559,
1.87190107867033));
#9168=CARTESIAN_POINT('Ctrl Pts',(-0.810556943749999,32.5229166676226,1.40392580900275));
#9169=CARTESIAN_POINT('Ctrl Pts',(-1.6211138875,32.4645833342893,0.935950539335167));
#9170=CARTESIAN_POINT('Ctrl Pts',(-1.6211138875,32.4062500009559,0.));
#9171=CARTESIAN_POINT('Ctrl Pts',(-1.6211138875,32.3479166676226,-0.935950539335166));
#9172=CARTESIAN_POINT('Ctrl Pts',(-0.81055694375,32.2895833342893,-1.40392580900275));
#9173=CARTESIAN_POINT('Ctrl Pts',(-1.14620883215705E-16,32.2312500009559,
-1.87190107867033));
#9174=CARTESIAN_POINT('Ctrl Pts',(0.81055694375,32.1729166676226,-1.40392580900275));
#9175=CARTESIAN_POINT('Ctrl Pts',(1.6211138875,32.1145833342893,-0.935950539335166));
#9176=CARTESIAN_POINT('Ctrl Pts',(1.6211138875,32.0562500009559,-1.9852919333802E-16));
#9177=CARTESIAN_POINT('Ctrl Pts',(1.6211138875,31.9979166676226,0.935950539335165));
#9178=CARTESIAN_POINT('Ctrl Pts',(0.810556943750001,31.9395833342893,1.40392580900275));
#9179=CARTESIAN_POINT('Ctrl Pts',(3.43862649647115E-16,31.8812500009559,
1.87190107867033));
#9180=CARTESIAN_POINT('Ctrl Pts',(-0.810556943749999,31.8229166676226,1.40392580900275));
#9181=CARTESIAN_POINT('Ctrl Pts',(-1.6211138875,31.7645833342893,0.935950539335167));
#9182=CARTESIAN_POINT('Ctrl Pts',(-1.6211138875,31.7062500009559,0.));
#9183=CARTESIAN_POINT('Ctrl Pts',(-1.6211138875,31.6479166676226,-0.935950539335166));
#9184=CARTESIAN_POINT('Ctrl Pts',(-0.81055694375,31.5895833342893,-1.40392580900275));
#9185=CARTESIAN_POINT('Ctrl Pts',(-1.14620883215705E-16,31.5312500009559,
-1.87190107867033));
#9186=CARTESIAN_POINT('Ctrl Pts',(0.81055694375,31.4729166676226,-1.40392580900275));
#9187=CARTESIAN_POINT('Ctrl Pts',(1.6211138875,31.4145833342893,-0.935950539335166));
#9188=CARTESIAN_POINT('Ctrl Pts',(1.6211138875,31.3562500009559,-1.9852919333802E-16));
#9189=CARTESIAN_POINT('Ctrl Pts',(1.6211138875,31.2979166676226,0.935950539335165));
#9190=CARTESIAN_POINT('Ctrl Pts',(0.810556943750001,31.2395833342893,1.40392580900275));
#9191=CARTESIAN_POINT('Ctrl Pts',(3.43862649647115E-16,31.1812500009559,
1.87190107867033));
#9192=CARTESIAN_POINT('Ctrl Pts',(-0.810556943749999,31.1229166676226,1.40392580900275));
#9193=CARTESIAN_POINT('Ctrl Pts',(-1.6211138875,31.0645833342893,0.935950539335167));
#9194=CARTESIAN_POINT('Ctrl Pts',(-1.6211138875,31.0062500009559,0.));
#9195=CARTESIAN_POINT('Ctrl Pts',(-1.6211138875,30.9479166676226,-0.935950539335166));
#9196=CARTESIAN_POINT('Ctrl Pts',(-0.81055694375,30.8895833342893,-1.40392580900275));
#9197=CARTESIAN_POINT('Ctrl Pts',(-1.14620883215705E-16,30.8312500009559,
-1.87190107867033));
#9198=CARTESIAN_POINT('Ctrl Pts',(0.81055694375,30.7729166676226,-1.40392580900275));
#9199=CARTESIAN_POINT('Ctrl Pts',(1.6211138875,30.7145833342893,-0.935950539335166));
#9200=CARTESIAN_POINT('Ctrl Pts',(1.6211138875,30.6562500009559,-1.9852919333802E-16));
#9201=CARTESIAN_POINT('Ctrl Pts',(1.6211138875,30.5979166676226,0.935950539335165));
#9202=CARTESIAN_POINT('Ctrl Pts',(0.810556943750001,30.5395833342893,1.40392580900275));
#9203=CARTESIAN_POINT('Ctrl Pts',(3.43862649647115E-16,30.4812500009559,
1.87190107867033));
#9204=CARTESIAN_POINT('Ctrl Pts',(-0.810556943749999,30.4229166676226,1.40392580900275));
#9205=CARTESIAN_POINT('Ctrl Pts',(-1.6211138875,30.3645833342893,0.935950539335167));
#9206=CARTESIAN_POINT('Ctrl Pts',(-1.6211138875,30.3062500009559,0.));
#9207=CARTESIAN_POINT('Ctrl Pts',(-1.6211138875,30.2479166676226,-0.935950539335166));
#9208=CARTESIAN_POINT('Ctrl Pts',(-0.81055694375,30.1895833342893,-1.40392580900275));
#9209=CARTESIAN_POINT('Ctrl Pts',(-1.14620883215705E-16,30.1312500009559,
-1.87190107867033));
#9210=CARTESIAN_POINT('Ctrl Pts',(0.81055694375,30.0729166676226,-1.40392580900275));
#9211=CARTESIAN_POINT('Ctrl Pts',(1.6211138875,30.0145833342893,-0.935950539335166));
#9212=CARTESIAN_POINT('Ctrl Pts',(1.6211138875,29.9562500009559,-1.9852919333802E-16));
#9213=CARTESIAN_POINT('Ctrl Pts',(1.6211138875,29.8979166676226,0.935950539335165));
#9214=CARTESIAN_POINT('Ctrl Pts',(0.810556943750001,29.8395833342893,1.40392580900275));
#9215=CARTESIAN_POINT('Ctrl Pts',(3.43862649647115E-16,29.7812500009559,
1.87190107867033));
#9216=CARTESIAN_POINT('Ctrl Pts',(-0.810556943749999,29.7229166676226,1.40392580900275));
#9217=CARTESIAN_POINT('Ctrl Pts',(-1.6211138875,29.6645833342893,0.935950539335167));
#9218=CARTESIAN_POINT('Ctrl Pts',(-1.6211138875,29.6062500009559,0.));
#9219=CARTESIAN_POINT('Ctrl Pts',(-1.6211138875,29.5479166676226,-0.935950539335166));
#9220=CARTESIAN_POINT('Ctrl Pts',(-0.81055694375,29.4895833342893,-1.40392580900275));
#9221=CARTESIAN_POINT('Ctrl Pts',(-1.14620883215705E-16,29.4312500009559,
-1.87190107867033));
#9222=CARTESIAN_POINT('Ctrl Pts',(0.81055694375,29.3729166676226,-1.40392580900275));
#9223=CARTESIAN_POINT('Ctrl Pts',(1.6211138875,29.3145833342893,-0.935950539335166));
#9224=CARTESIAN_POINT('Ctrl Pts',(1.6211138875,29.2562500009559,-1.9852919333802E-16));
#9225=CARTESIAN_POINT('Ctrl Pts',(1.6211138875,29.1979166676226,0.935950539335165));
#9226=CARTESIAN_POINT('Ctrl Pts',(0.810556943750001,29.1395833342893,1.40392580900275));
#9227=CARTESIAN_POINT('Ctrl Pts',(3.43862649647115E-16,29.0812500009559,
1.87190107867033));
#9228=CARTESIAN_POINT('Ctrl Pts',(-0.810556943749999,29.0229166676226,1.40392580900275));
#9229=CARTESIAN_POINT('Ctrl Pts',(-1.6211138875,28.9645833342893,0.935950539335167));
#9230=CARTESIAN_POINT('Ctrl Pts',(-1.6211138875,28.9062500009559,0.));
#9231=CARTESIAN_POINT('Ctrl Pts',(-1.6211138875,28.8479166676226,-0.935950539335166));
#9232=CARTESIAN_POINT('Ctrl Pts',(-0.81055694375,28.7895833342893,-1.40392580900275));
#9233=CARTESIAN_POINT('Ctrl Pts',(-1.14620883215705E-16,28.7312500009559,
-1.87190107867033));
#9234=CARTESIAN_POINT('Ctrl Pts',(0.81055694375,28.6729166676226,-1.40392580900275));
#9235=CARTESIAN_POINT('Ctrl Pts',(1.6211138875,28.6145833342893,-0.935950539335166));
#9236=CARTESIAN_POINT('Ctrl Pts',(1.6211138875,28.5562500009559,-1.9852919333802E-16));
#9237=CARTESIAN_POINT('Ctrl Pts',(1.6211138875,28.4979166676226,0.935950539335165));
#9238=CARTESIAN_POINT('Ctrl Pts',(0.810556943750001,28.4395833342893,1.40392580900275));
#9239=CARTESIAN_POINT('Ctrl Pts',(3.43862649647115E-16,28.3812500009559,
1.87190107867033));
#9240=CARTESIAN_POINT('Ctrl Pts',(-0.810556943749999,28.3229166676226,1.40392580900275));
#9241=CARTESIAN_POINT('Ctrl Pts',(-1.6211138875,28.2645833342893,0.935950539335167));
#9242=CARTESIAN_POINT('Ctrl Pts',(-1.6211138875,28.2062500009559,0.));
#9243=CARTESIAN_POINT('Ctrl Pts',(-1.6211138875,28.1479166676226,-0.935950539335166));
#9244=CARTESIAN_POINT('Ctrl Pts',(-0.81055694375,28.0895833342893,-1.40392580900275));
#9245=CARTESIAN_POINT('Ctrl Pts',(-1.14620883215705E-16,28.0312500009559,
-1.87190107867033));
#9246=CARTESIAN_POINT('Ctrl Pts',(0.81055694375,27.9729166676226,-1.40392580900275));
#9247=CARTESIAN_POINT('Ctrl Pts',(1.6211138875,27.9145833342893,-0.935950539335166));
#9248=CARTESIAN_POINT('Ctrl Pts',(1.6211138875,27.8562500009559,-1.9852919333802E-16));
#9249=CARTESIAN_POINT('Ctrl Pts',(1.6211138875,27.7979166676226,0.935950539335165));
#9250=CARTESIAN_POINT('Ctrl Pts',(0.810556943750001,27.7395833342893,1.40392580900275));
#9251=CARTESIAN_POINT('Ctrl Pts',(3.43862649647115E-16,27.6812500009559,
1.87190107867033));
#9252=CARTESIAN_POINT('Ctrl Pts',(-0.810556943749999,27.6229166676226,1.40392580900275));
#9253=CARTESIAN_POINT('Ctrl Pts',(-1.6211138875,27.5645833342893,0.935950539335167));
#9254=CARTESIAN_POINT('Ctrl Pts',(-1.6211138875,27.5062500009559,0.));
#9255=CARTESIAN_POINT('Ctrl Pts',(-1.6211138875,27.4479166676226,-0.935950539335166));
#9256=CARTESIAN_POINT('Ctrl Pts',(-0.81055694375,27.3895833342893,-1.40392580900275));
#9257=CARTESIAN_POINT('Ctrl Pts',(-1.14620883215705E-16,27.3312500009559,
-1.87190107867033));
#9258=CARTESIAN_POINT('Ctrl Pts',(0.81055694375,27.2729166676226,-1.40392580900275));
#9259=CARTESIAN_POINT('Ctrl Pts',(1.6211138875,27.2145833342893,-0.935950539335166));
#9260=CARTESIAN_POINT('Ctrl Pts',(1.6211138875,27.1562500009559,-1.9852919333802E-16));
#9261=CARTESIAN_POINT('Ctrl Pts',(1.6211138875,27.0979166676226,0.935950539335165));
#9262=CARTESIAN_POINT('Ctrl Pts',(0.810556943750001,27.0395833342893,1.40392580900275));
#9263=CARTESIAN_POINT('Ctrl Pts',(3.43862649647115E-16,26.9812500009559,
1.87190107867033));
#9264=CARTESIAN_POINT('Ctrl Pts',(-0.810556943749999,26.9229166676226,1.40392580900275));
#9265=CARTESIAN_POINT('Ctrl Pts',(-1.6211138875,26.8645833342893,0.935950539335167));
#9266=CARTESIAN_POINT('Ctrl Pts',(-1.6211138875,26.8062500009559,0.));
#9267=CARTESIAN_POINT('Ctrl Pts',(-1.6211138875,26.7479166676226,-0.935950539335166));
#9268=CARTESIAN_POINT('Ctrl Pts',(-0.81055694375,26.6895833342893,-1.40392580900275));
#9269=CARTESIAN_POINT('Ctrl Pts',(-1.14620883215705E-16,26.6312500009559,
-1.87190107867033));
#9270=CARTESIAN_POINT('Ctrl Pts',(0.81055694375,26.5729166676226,-1.40392580900275));
#9271=CARTESIAN_POINT('Ctrl Pts',(1.6211138875,26.5145833342893,-0.935950539335166));
#9272=CARTESIAN_POINT('Ctrl Pts',(1.6211138875,26.4562500009559,-1.9852919333802E-16));
#9273=CARTESIAN_POINT('Ctrl Pts',(1.6211138875,26.3979166676226,0.935950539335165));
#9274=CARTESIAN_POINT('Ctrl Pts',(0.810556943750001,26.3395833342893,1.40392580900275));
#9275=CARTESIAN_POINT('Ctrl Pts',(3.43862649647115E-16,26.2812500009559,
1.87190107867033));
#9276=CARTESIAN_POINT('Ctrl Pts',(-0.810556943749999,26.2229166676226,1.40392580900275));
#9277=CARTESIAN_POINT('Ctrl Pts',(-1.6211138875,26.1645833342893,0.935950539335167));
#9278=CARTESIAN_POINT('Ctrl Pts',(-1.6211138875,26.1062500009559,0.));
#9279=CARTESIAN_POINT('Ctrl Pts',(-1.6211138875,26.0479166676226,-0.935950539335166));
#9280=CARTESIAN_POINT('Ctrl Pts',(-0.81055694375,25.9895833342893,-1.40392580900275));
#9281=CARTESIAN_POINT('Ctrl Pts',(-1.14620883215705E-16,25.9312500009559,
-1.87190107867033));
#9282=CARTESIAN_POINT('Ctrl Pts',(0.81055694375,25.8729166676226,-1.40392580900275));
#9283=CARTESIAN_POINT('Ctrl Pts',(1.6211138875,25.8145833342893,-0.935950539335166));
#9284=CARTESIAN_POINT('Ctrl Pts',(1.6211138875,25.7562500009559,-1.9852919333802E-16));
#9285=CARTESIAN_POINT('Ctrl Pts',(1.6211138875,25.6979166676226,0.935950539335165));
#9286=CARTESIAN_POINT('Ctrl Pts',(0.810556943750001,25.6395833342893,1.40392580900275));
#9287=CARTESIAN_POINT('Ctrl Pts',(3.43862649647115E-16,25.5812500009559,
1.87190107867033));
#9288=CARTESIAN_POINT('Ctrl Pts',(-0.810556943749999,25.5229166676226,1.40392580900275));
#9289=CARTESIAN_POINT('Ctrl Pts',(-1.6211138875,25.4645833342893,0.935950539335167));
#9290=CARTESIAN_POINT('Ctrl Pts',(-1.6211138875,25.4062500009559,0.));
#9291=CARTESIAN_POINT('Ctrl Pts',(-1.6211138875,25.3479166676226,-0.935950539335166));
#9292=CARTESIAN_POINT('Ctrl Pts',(-0.81055694375,25.2895833342893,-1.40392580900275));
#9293=CARTESIAN_POINT('Ctrl Pts',(-1.14620883215705E-16,25.2312500009559,
-1.87190107867033));
#9294=CARTESIAN_POINT('Ctrl Pts',(0.81055694375,25.1729166676226,-1.40392580900275));
#9295=CARTESIAN_POINT('Ctrl Pts',(1.6211138875,25.1145833342893,-0.935950539335166));
#9296=CARTESIAN_POINT('Ctrl Pts',(1.6211138875,25.0562500009559,-1.9852919333802E-16));
#9297=CARTESIAN_POINT('Ctrl Pts',(1.6211138875,24.9979166676226,0.935950539335165));
#9298=CARTESIAN_POINT('Ctrl Pts',(0.810556943750001,24.9395833342893,1.40392580900275));
#9299=CARTESIAN_POINT('Ctrl Pts',(3.43862649647115E-16,24.8812500009559,
1.87190107867033));
#9300=CARTESIAN_POINT('Ctrl Pts',(-0.810556943749999,24.8229166676226,1.40392580900275));
#9301=CARTESIAN_POINT('Ctrl Pts',(-1.6211138875,24.7645833342893,0.935950539335167));
#9302=CARTESIAN_POINT('Ctrl Pts',(-1.6211138875,24.7062500009559,0.));
#9303=CARTESIAN_POINT('Ctrl Pts',(-1.6211138875,24.6479166676226,-0.935950539335166));
#9304=CARTESIAN_POINT('Ctrl Pts',(-0.81055694375,24.5895833342893,-1.40392580900275));
#9305=CARTESIAN_POINT('Ctrl Pts',(-1.14620883215705E-16,24.5312500009559,
-1.87190107867033));
#9306=CARTESIAN_POINT('Ctrl Pts',(0.81055694375,24.4729166676226,-1.40392580900275));
#9307=CARTESIAN_POINT('Ctrl Pts',(1.6211138875,24.4145833342893,-0.935950539335166));
#9308=CARTESIAN_POINT('Ctrl Pts',(1.6211138875,24.3562500009559,-1.9852919333802E-16));
#9309=CARTESIAN_POINT('Ctrl Pts',(1.6211138875,24.2979166676226,0.935950539335165));
#9310=CARTESIAN_POINT('Ctrl Pts',(0.810556943750001,24.2395833342893,1.40392580900275));
#9311=CARTESIAN_POINT('Ctrl Pts',(3.43862649647115E-16,24.1812500009559,
1.87190107867033));
#9312=CARTESIAN_POINT('Ctrl Pts',(-0.810556943749999,24.1229166676226,1.40392580900275));
#9313=CARTESIAN_POINT('Ctrl Pts',(-1.6211138875,24.0645833342893,0.935950539335167));
#9314=CARTESIAN_POINT('Ctrl Pts',(-1.6211138875,24.0062500009559,0.));
#9315=CARTESIAN_POINT('Ctrl Pts',(-1.6211138875,23.9479166676226,-0.935950539335166));
#9316=CARTESIAN_POINT('Ctrl Pts',(-0.81055694375,23.8895833342893,-1.40392580900275));
#9317=CARTESIAN_POINT('Ctrl Pts',(-1.14620883215705E-16,23.8312500009559,
-1.87190107867033));
#9318=CARTESIAN_POINT('Ctrl Pts',(0.81055694375,23.7729166676226,-1.40392580900275));
#9319=CARTESIAN_POINT('Ctrl Pts',(1.6211138875,23.7145833342893,-0.935950539335166));
#9320=CARTESIAN_POINT('Ctrl Pts',(1.6211138875,23.6562500009559,-1.9852919333802E-16));
#9321=CARTESIAN_POINT('Ctrl Pts',(1.6211138875,23.5979166676226,0.935950539335165));
#9322=CARTESIAN_POINT('Ctrl Pts',(0.810556943750001,23.5395833342893,1.40392580900275));
#9323=CARTESIAN_POINT('Ctrl Pts',(3.43862649647115E-16,23.4812500009559,
1.87190107867033));
#9324=CARTESIAN_POINT('Ctrl Pts',(-0.810556943749999,23.4229166676226,1.40392580900275));
#9325=CARTESIAN_POINT('Ctrl Pts',(-1.6211138875,23.3645833342893,0.935950539335167));
#9326=CARTESIAN_POINT('Ctrl Pts',(-1.6211138875,23.3062500009559,0.));
#9327=CARTESIAN_POINT('Ctrl Pts',(-1.6211138875,23.2479166676226,-0.935950539335166));
#9328=CARTESIAN_POINT('Ctrl Pts',(-0.81055694375,23.1895833342893,-1.40392580900275));
#9329=CARTESIAN_POINT('Ctrl Pts',(-1.14620883215705E-16,23.1312500009559,
-1.87190107867033));
#9330=CARTESIAN_POINT('Ctrl Pts',(0.81055694375,23.0729166676226,-1.40392580900275));
#9331=CARTESIAN_POINT('Ctrl Pts',(1.6211138875,23.0145833342893,-0.935950539335166));
#9332=CARTESIAN_POINT('Ctrl Pts',(1.6211138875,22.9562500009559,-1.9852919333802E-16));
#9333=CARTESIAN_POINT('Ctrl Pts',(1.6211138875,22.8979166676226,0.935950539335165));
#9334=CARTESIAN_POINT('Ctrl Pts',(0.810556943750001,22.8395833342893,1.40392580900275));
#9335=CARTESIAN_POINT('Ctrl Pts',(3.43862649647115E-16,22.7812500009559,
1.87190107867033));
#9336=CARTESIAN_POINT('Ctrl Pts',(-0.810556943749999,22.7229166676226,1.40392580900275));
#9337=CARTESIAN_POINT('Ctrl Pts',(-1.6211138875,22.6645833342893,0.935950539335167));
#9338=CARTESIAN_POINT('Ctrl Pts',(-1.6211138875,22.6062500009559,0.));
#9339=CARTESIAN_POINT('Ctrl Pts',(-1.6211138875,22.5479166676226,-0.935950539335166));
#9340=CARTESIAN_POINT('Ctrl Pts',(-0.81055694375,22.4895833342893,-1.40392580900275));
#9341=CARTESIAN_POINT('Ctrl Pts',(-1.14620883215705E-16,22.4312500009559,
-1.87190107867033));
#9342=CARTESIAN_POINT('Ctrl Pts',(0.81055694375,22.3729166676226,-1.40392580900275));
#9343=CARTESIAN_POINT('Ctrl Pts',(1.6211138875,22.3145833342893,-0.935950539335166));
#9344=CARTESIAN_POINT('Ctrl Pts',(1.6211138875,22.2562500009559,-1.9852919333802E-16));
#9345=CARTESIAN_POINT('Ctrl Pts',(1.6211138875,22.1979166676226,0.935950539335165));
#9346=CARTESIAN_POINT('Ctrl Pts',(0.810556943750001,22.1395833342893,1.40392580900275));
#9347=CARTESIAN_POINT('Ctrl Pts',(3.43862649647115E-16,22.0812500009559,
1.87190107867033));
#9348=CARTESIAN_POINT('Ctrl Pts',(-0.810556943749999,22.0229166676226,1.40392580900275));
#9349=CARTESIAN_POINT('Ctrl Pts',(-1.6211138875,21.9645833342893,0.935950539335167));
#9350=CARTESIAN_POINT('Ctrl Pts',(-1.6211138875,21.9062500009559,0.));
#9351=CARTESIAN_POINT('Ctrl Pts',(-1.6211138875,21.8479166676226,-0.935950539335166));
#9352=CARTESIAN_POINT('Ctrl Pts',(-0.81055694375,21.7895833342893,-1.40392580900275));
#9353=CARTESIAN_POINT('Ctrl Pts',(-1.14620883215705E-16,21.7312500009559,
-1.87190107867033));
#9354=CARTESIAN_POINT('Ctrl Pts',(0.81055694375,21.6729166676226,-1.40392580900275));
#9355=CARTESIAN_POINT('Ctrl Pts',(1.6211138875,21.6145833342893,-0.935950539335166));
#9356=CARTESIAN_POINT('Ctrl Pts',(1.6211138875,21.5562500009559,-1.9852919333802E-16));
#9357=CARTESIAN_POINT('Ctrl Pts',(1.6211138875,21.4979166676226,0.935950539335165));
#9358=CARTESIAN_POINT('Ctrl Pts',(0.810556943750001,21.4395833342893,1.40392580900275));
#9359=CARTESIAN_POINT('Ctrl Pts',(3.43862649647115E-16,21.3812500009559,
1.87190107867033));
#9360=CARTESIAN_POINT('Ctrl Pts',(-0.810556943749999,21.3229166676226,1.40392580900275));
#9361=CARTESIAN_POINT('Ctrl Pts',(-1.6211138875,21.2645833342893,0.935950539335167));
#9362=CARTESIAN_POINT('Ctrl Pts',(-1.6211138875,21.2062500009559,0.));
#9363=CARTESIAN_POINT('Ctrl Pts',(-1.6211138875,21.1479166676226,-0.935950539335166));
#9364=CARTESIAN_POINT('Ctrl Pts',(-0.81055694375,21.0895833342893,-1.40392580900275));
#9365=CARTESIAN_POINT('Ctrl Pts',(-1.14620883215705E-16,21.0312500009559,
-1.87190107867033));
#9366=CARTESIAN_POINT('Ctrl Pts',(0.81055694375,20.9729166676226,-1.40392580900275));
#9367=CARTESIAN_POINT('Ctrl Pts',(1.6211138875,20.9145833342893,-0.935950539335166));
#9368=CARTESIAN_POINT('Ctrl Pts',(1.6211138875,20.8562500009559,-1.9852919333802E-16));
#9369=CARTESIAN_POINT('Ctrl Pts',(1.6211138875,20.7979166676226,0.935950539335165));
#9370=CARTESIAN_POINT('Ctrl Pts',(0.810556943750001,20.7395833342893,1.40392580900275));
#9371=CARTESIAN_POINT('Ctrl Pts',(3.43862649647115E-16,20.6812500009559,
1.87190107867033));
#9372=CARTESIAN_POINT('Ctrl Pts',(-0.810556943749999,20.6229166676226,1.40392580900275));
#9373=CARTESIAN_POINT('Ctrl Pts',(-1.6211138875,20.5645833342893,0.935950539335167));
#9374=CARTESIAN_POINT('Ctrl Pts',(-1.6211138875,20.5062500009559,0.));
#9375=CARTESIAN_POINT('Ctrl Pts',(-1.6211138875,20.4479166676226,-0.935950539335166));
#9376=CARTESIAN_POINT('Ctrl Pts',(-0.81055694375,20.3895833342893,-1.40392580900275));
#9377=CARTESIAN_POINT('Ctrl Pts',(-1.14620883215705E-16,20.3312500009559,
-1.87190107867033));
#9378=CARTESIAN_POINT('Ctrl Pts',(0.81055694375,20.2729166676226,-1.40392580900275));
#9379=CARTESIAN_POINT('Ctrl Pts',(1.6211138875,20.2145833342893,-0.935950539335166));
#9380=CARTESIAN_POINT('Ctrl Pts',(1.6211138875,20.1562500009559,-1.9852919333802E-16));
#9381=CARTESIAN_POINT('Ctrl Pts',(1.6211138875,20.0979166676226,0.935950539335165));
#9382=CARTESIAN_POINT('Ctrl Pts',(0.810556943750001,20.0395833342893,1.40392580900275));
#9383=CARTESIAN_POINT('Ctrl Pts',(3.43862649647115E-16,19.9812500009559,
1.87190107867033));
#9384=CARTESIAN_POINT('Ctrl Pts',(-0.810556943749999,19.9229166676226,1.40392580900275));
#9385=CARTESIAN_POINT('Ctrl Pts',(-1.6211138875,19.8645833342893,0.935950539335167));
#9386=CARTESIAN_POINT('Ctrl Pts',(-1.6211138875,19.8062500009559,0.));
#9387=CARTESIAN_POINT('Ctrl Pts',(-1.6211138875,19.7479166676226,-0.935950539335166));
#9388=CARTESIAN_POINT('Ctrl Pts',(-0.81055694375,19.6895833342893,-1.40392580900275));
#9389=CARTESIAN_POINT('Ctrl Pts',(-1.14620883215705E-16,19.6312500009559,
-1.87190107867033));
#9390=CARTESIAN_POINT('Ctrl Pts',(0.81055694375,19.5729166676226,-1.40392580900275));
#9391=CARTESIAN_POINT('Ctrl Pts',(1.6211138875,19.5145833342893,-0.935950539335166));
#9392=CARTESIAN_POINT('Ctrl Pts',(1.6211138875,19.4562500009559,-1.9852919333802E-16));
#9393=CARTESIAN_POINT('Ctrl Pts',(1.6211138875,19.3979166676226,0.935950539335165));
#9394=CARTESIAN_POINT('Ctrl Pts',(0.810556943750001,19.3395833342893,1.40392580900275));
#9395=CARTESIAN_POINT('Ctrl Pts',(3.43862649647115E-16,19.2812500009559,
1.87190107867033));
#9396=CARTESIAN_POINT('Ctrl Pts',(-0.810556943749999,19.2229166676226,1.40392580900275));
#9397=CARTESIAN_POINT('Ctrl Pts',(-1.6211138875,19.1645833342893,0.935950539335167));
#9398=CARTESIAN_POINT('Ctrl Pts',(-1.6211138875,19.1062500009559,0.));
#9399=CARTESIAN_POINT('Ctrl Pts',(-1.6211138875,19.0479166676226,-0.935950539335166));
#9400=CARTESIAN_POINT('Ctrl Pts',(-0.81055694375,18.9895833342893,-1.40392580900275));
#9401=CARTESIAN_POINT('Ctrl Pts',(-1.14620883215705E-16,18.9312500009559,
-1.87190107867033));
#9402=CARTESIAN_POINT('Ctrl Pts',(0.81055694375,18.8729166676226,-1.40392580900275));
#9403=CARTESIAN_POINT('Ctrl Pts',(1.6211138875,18.8145833342893,-0.935950539335166));
#9404=CARTESIAN_POINT('Ctrl Pts',(1.6211138875,18.7562500009559,-1.9852919333802E-16));
#9405=CARTESIAN_POINT('Ctrl Pts',(1.6211138875,18.6979166676226,0.935950539335165));
#9406=CARTESIAN_POINT('Ctrl Pts',(0.810556943750001,18.6395833342893,1.40392580900275));
#9407=CARTESIAN_POINT('Ctrl Pts',(3.43862649647115E-16,18.5812500009559,
1.87190107867033));
#9408=CARTESIAN_POINT('Ctrl Pts',(-0.810556943749999,18.5229166676226,1.40392580900275));
#9409=CARTESIAN_POINT('Ctrl Pts',(-1.6211138875,18.4645833342893,0.935950539335167));
#9410=CARTESIAN_POINT('Ctrl Pts',(-1.6211138875,18.4062500009559,0.));
#9411=CARTESIAN_POINT('Ctrl Pts',(-1.6211138875,18.3479166676226,-0.935950539335166));
#9412=CARTESIAN_POINT('Ctrl Pts',(-0.81055694375,18.2895833342893,-1.40392580900275));
#9413=CARTESIAN_POINT('Ctrl Pts',(-1.14620883215705E-16,18.2312500009559,
-1.87190107867033));
#9414=CARTESIAN_POINT('Ctrl Pts',(0.81055694375,18.1729166676226,-1.40392580900275));
#9415=CARTESIAN_POINT('Ctrl Pts',(1.6211138875,18.1145833342893,-0.935950539335166));
#9416=CARTESIAN_POINT('Ctrl Pts',(1.6211138875,18.0562500009559,-1.9852919333802E-16));
#9417=CARTESIAN_POINT('Ctrl Pts',(1.6211138875,17.9979166676226,0.935950539335165));
#9418=CARTESIAN_POINT('Ctrl Pts',(0.810556943750001,17.9395833342893,1.40392580900275));
#9419=CARTESIAN_POINT('Ctrl Pts',(3.43862649647115E-16,17.8812500009559,
1.87190107867033));
#9420=CARTESIAN_POINT('Ctrl Pts',(-0.810556943749999,17.8229166676226,1.40392580900275));
#9421=CARTESIAN_POINT('Ctrl Pts',(-1.6211138875,17.7645833342893,0.935950539335167));
#9422=CARTESIAN_POINT('Ctrl Pts',(-1.6211138875,17.7062500009559,0.));
#9423=CARTESIAN_POINT('Ctrl Pts',(-1.6211138875,17.6479166676226,-0.935950539335166));
#9424=CARTESIAN_POINT('Ctrl Pts',(-0.81055694375,17.5895833342893,-1.40392580900275));
#9425=CARTESIAN_POINT('Ctrl Pts',(-1.14620883215705E-16,17.5312500009559,
-1.87190107867033));
#9426=CARTESIAN_POINT('Ctrl Pts',(0.81055694375,17.4729166676226,-1.40392580900275));
#9427=CARTESIAN_POINT('Ctrl Pts',(1.6211138875,17.4145833342893,-0.935950539335166));
#9428=CARTESIAN_POINT('Ctrl Pts',(1.6211138875,17.3562500009559,-1.9852919333802E-16));
#9429=CARTESIAN_POINT('Ctrl Pts',(1.6211138875,17.2979166676226,0.935950539335165));
#9430=CARTESIAN_POINT('Ctrl Pts',(0.810556943750001,17.2395833342893,1.40392580900275));
#9431=CARTESIAN_POINT('Ctrl Pts',(3.43862649647115E-16,17.1812500009559,
1.87190107867033));
#9432=CARTESIAN_POINT('Ctrl Pts',(-0.810556943749999,17.1229166676226,1.40392580900275));
#9433=CARTESIAN_POINT('Ctrl Pts',(-1.6211138875,17.0645833342893,0.935950539335167));
#9434=CARTESIAN_POINT('Ctrl Pts',(-1.6211138875,17.0062500009559,0.));
#9435=CARTESIAN_POINT('Ctrl Pts',(-1.6211138875,16.9479166676226,-0.935950539335166));
#9436=CARTESIAN_POINT('Ctrl Pts',(-0.81055694375,16.8895833342893,-1.40392580900275));
#9437=CARTESIAN_POINT('Ctrl Pts',(-1.14620883215705E-16,16.8312500009559,
-1.87190107867033));
#9438=CARTESIAN_POINT('Ctrl Pts',(0.81055694375,16.7729166676226,-1.40392580900275));
#9439=CARTESIAN_POINT('Ctrl Pts',(1.6211138875,16.7145833342893,-0.935950539335166));
#9440=CARTESIAN_POINT('Ctrl Pts',(1.6211138875,16.6562500009559,-1.9852919333802E-16));
#9441=CARTESIAN_POINT('Ctrl Pts',(1.6211138875,16.5979166676226,0.935950539335165));
#9442=CARTESIAN_POINT('Ctrl Pts',(0.810556943750001,16.5395833342893,1.40392580900275));
#9443=CARTESIAN_POINT('Ctrl Pts',(3.43862649647115E-16,16.4812500009559,
1.87190107867033));
#9444=CARTESIAN_POINT('Ctrl Pts',(-0.810556943749999,16.4229166676226,1.40392580900275));
#9445=CARTESIAN_POINT('Ctrl Pts',(-1.6211138875,16.3645833342893,0.935950539335167));
#9446=CARTESIAN_POINT('Ctrl Pts',(-1.6211138875,16.3062500009559,0.));
#9447=CARTESIAN_POINT('Ctrl Pts',(-1.6211138875,16.2479166676226,-0.935950539335166));
#9448=CARTESIAN_POINT('Ctrl Pts',(-0.81055694375,16.1895833342893,-1.40392580900275));
#9449=CARTESIAN_POINT('Ctrl Pts',(-1.14620883215705E-16,16.1312500009559,
-1.87190107867033));
#9450=CARTESIAN_POINT('Ctrl Pts',(0.81055694375,16.0729166676226,-1.40392580900275));
#9451=CARTESIAN_POINT('Ctrl Pts',(1.6211138875,16.0145833342893,-0.935950539335166));
#9452=CARTESIAN_POINT('Ctrl Pts',(1.6211138875,15.9562500009559,-1.9852919333802E-16));
#9453=CARTESIAN_POINT('Ctrl Pts',(1.6211138875,15.8979166676226,0.935950539335165));
#9454=CARTESIAN_POINT('Ctrl Pts',(0.810556943750001,15.8395833342893,1.40392580900275));
#9455=CARTESIAN_POINT('Ctrl Pts',(3.43862649647115E-16,15.7812500009559,
1.87190107867033));
#9456=CARTESIAN_POINT('Ctrl Pts',(-0.810556943749999,15.7229166676226,1.40392580900275));
#9457=CARTESIAN_POINT('Ctrl Pts',(-1.6211138875,15.6645833342893,0.935950539335167));
#9458=CARTESIAN_POINT('Ctrl Pts',(-1.6211138875,15.6062500009559,0.));
#9459=CARTESIAN_POINT('Ctrl Pts',(-1.6211138875,15.5479166676226,-0.935950539335166));
#9460=CARTESIAN_POINT('Ctrl Pts',(-0.81055694375,15.4895833342893,-1.40392580900275));
#9461=CARTESIAN_POINT('Ctrl Pts',(-1.14620883215705E-16,15.4312500009559,
-1.87190107867033));
#9462=CARTESIAN_POINT('Ctrl Pts',(0.81055694375,15.3729166676226,-1.40392580900275));
#9463=CARTESIAN_POINT('Ctrl Pts',(1.6211138875,15.3145833342893,-0.935950539335166));
#9464=CARTESIAN_POINT('Ctrl Pts',(1.6211138875,15.2562500009559,-1.9852919333802E-16));
#9465=CARTESIAN_POINT('Ctrl Pts',(1.6211138875,15.1979166676226,0.935950539335165));
#9466=CARTESIAN_POINT('Ctrl Pts',(0.810556943750001,15.1395833342893,1.40392580900275));
#9467=CARTESIAN_POINT('Ctrl Pts',(3.43862649647115E-16,15.0812500009559,
1.87190107867033));
#9468=CARTESIAN_POINT('Ctrl Pts',(-0.810556943749999,15.0229166676226,1.40392580900275));
#9469=CARTESIAN_POINT('Ctrl Pts',(-1.6211138875,14.9645833342893,0.935950539335167));
#9470=CARTESIAN_POINT('Ctrl Pts',(-1.6211138875,14.9062500009559,0.));
#9471=CARTESIAN_POINT('Ctrl Pts',(-1.6211138875,14.8479166676226,-0.935950539335166));
#9472=CARTESIAN_POINT('Ctrl Pts',(-0.81055694375,14.7895833342893,-1.40392580900275));
#9473=CARTESIAN_POINT('Ctrl Pts',(-1.14620883215705E-16,14.7312500009559,
-1.87190107867033));
#9474=CARTESIAN_POINT('Ctrl Pts',(0.81055694375,14.6729166676226,-1.40392580900275));
#9475=CARTESIAN_POINT('Ctrl Pts',(1.6211138875,14.6145833342893,-0.935950539335166));
#9476=CARTESIAN_POINT('Ctrl Pts',(1.6211138875,14.5562500009559,-1.9852919333802E-16));
#9477=CARTESIAN_POINT('Ctrl Pts',(1.6211138875,14.4979166676226,0.935950539335165));
#9478=CARTESIAN_POINT('Ctrl Pts',(0.810556943750001,14.4395833342893,1.40392580900275));
#9479=CARTESIAN_POINT('Ctrl Pts',(3.43862649647115E-16,14.3812500009559,
1.87190107867033));
#9480=CARTESIAN_POINT('Ctrl Pts',(-0.810556943749999,14.3229166676226,1.40392580900275));
#9481=CARTESIAN_POINT('Ctrl Pts',(-1.6211138875,14.2645833342893,0.935950539335167));
#9482=CARTESIAN_POINT('Ctrl Pts',(-1.6211138875,14.2062500009559,0.));
#9483=CARTESIAN_POINT('Ctrl Pts',(-1.6211138875,14.1479166676226,-0.935950539335166));
#9484=CARTESIAN_POINT('Ctrl Pts',(-0.81055694375,14.0895833342893,-1.40392580900275));
#9485=CARTESIAN_POINT('Ctrl Pts',(-1.14620883215705E-16,14.0312500009559,
-1.87190107867033));
#9486=CARTESIAN_POINT('Ctrl Pts',(0.81055694375,13.9729166676226,-1.40392580900275));
#9487=CARTESIAN_POINT('Ctrl Pts',(1.6211138875,13.9145833342893,-0.935950539335166));
#9488=CARTESIAN_POINT('Ctrl Pts',(1.6211138875,13.8562500009559,-1.9852919333802E-16));
#9489=CARTESIAN_POINT('Ctrl Pts',(1.6211138875,13.7979166676226,0.935950539335165));
#9490=CARTESIAN_POINT('Ctrl Pts',(0.810556943750001,13.7395833342893,1.40392580900275));
#9491=CARTESIAN_POINT('Ctrl Pts',(3.43862649647115E-16,13.6812500009559,
1.87190107867033));
#9492=CARTESIAN_POINT('Ctrl Pts',(-0.810556943749999,13.6229166676226,1.40392580900275));
#9493=CARTESIAN_POINT('Ctrl Pts',(-1.6211138875,13.5645833342893,0.935950539335167));
#9494=CARTESIAN_POINT('Ctrl Pts',(-1.6211138875,13.5062500009559,0.));
#9495=CARTESIAN_POINT('Ctrl Pts',(-1.6211138875,13.4479166676226,-0.935950539335166));
#9496=CARTESIAN_POINT('Ctrl Pts',(-0.81055694375,13.3895833342893,-1.40392580900275));
#9497=CARTESIAN_POINT('Ctrl Pts',(-1.14620883215705E-16,13.3312500009559,
-1.87190107867033));
#9498=CARTESIAN_POINT('Ctrl Pts',(0.81055694375,13.2729166676226,-1.40392580900275));
#9499=CARTESIAN_POINT('Ctrl Pts',(1.6211138875,13.2145833342893,-0.935950539335166));
#9500=CARTESIAN_POINT('Ctrl Pts',(1.6211138875,13.1562500009559,-1.9852919333802E-16));
#9501=CARTESIAN_POINT('Ctrl Pts',(1.6211138875,13.0979166676226,0.935950539335165));
#9502=CARTESIAN_POINT('Ctrl Pts',(0.810556943750001,13.0395833342893,1.40392580900275));
#9503=CARTESIAN_POINT('Ctrl Pts',(3.43862649647115E-16,12.9812500009559,
1.87190107867033));
#9504=CARTESIAN_POINT('Ctrl Pts',(-0.810556943749999,12.9229166676226,1.40392580900275));
#9505=CARTESIAN_POINT('Ctrl Pts',(-1.6211138875,12.8645833342893,0.935950539335167));
#9506=CARTESIAN_POINT('Ctrl Pts',(-1.6211138875,12.8062500009559,0.));
#9507=CARTESIAN_POINT('Ctrl Pts',(-1.6211138875,12.7479166676226,-0.935950539335166));
#9508=CARTESIAN_POINT('Ctrl Pts',(-0.81055694375,12.6895833342893,-1.40392580900275));
#9509=CARTESIAN_POINT('Ctrl Pts',(-1.14620883215705E-16,12.6312500009559,
-1.87190107867033));
#9510=CARTESIAN_POINT('Ctrl Pts',(0.81055694375,12.5729166676226,-1.40392580900275));
#9511=CARTESIAN_POINT('Ctrl Pts',(1.6211138875,12.5145833342893,-0.935950539335166));
#9512=CARTESIAN_POINT('Ctrl Pts',(1.6211138875,12.4562500009559,-1.9852919333802E-16));
#9513=CARTESIAN_POINT('Ctrl Pts',(1.6211138875,12.3979166676226,0.935950539335165));
#9514=CARTESIAN_POINT('Ctrl Pts',(0.810556943750001,12.3395833342893,1.40392580900275));
#9515=CARTESIAN_POINT('Ctrl Pts',(3.43862649647115E-16,12.2812500009559,
1.87190107867033));
#9516=CARTESIAN_POINT('Ctrl Pts',(-0.810556943749999,12.2229166676226,1.40392580900275));
#9517=CARTESIAN_POINT('Ctrl Pts',(-1.6211138875,12.1645833342893,0.935950539335167));
#9518=CARTESIAN_POINT('Ctrl Pts',(-1.6211138875,12.1062500009559,0.));
#9519=CARTESIAN_POINT('Ctrl Pts',(-1.6211138875,12.0479166676226,-0.935950539335166));
#9520=CARTESIAN_POINT('Ctrl Pts',(-0.81055694375,11.9895833342893,-1.40392580900275));
#9521=CARTESIAN_POINT('Ctrl Pts',(-1.14620883215705E-16,11.9312500009559,
-1.87190107867033));
#9522=CARTESIAN_POINT('Ctrl Pts',(0.81055694375,11.8729166676226,-1.40392580900275));
#9523=CARTESIAN_POINT('Ctrl Pts',(1.6211138875,11.8145833342893,-0.935950539335166));
#9524=CARTESIAN_POINT('Ctrl Pts',(1.6211138875,11.7562500009559,-1.9852919333802E-16));
#9525=CARTESIAN_POINT('Ctrl Pts',(1.6211138875,11.6979166676226,0.935950539335165));
#9526=CARTESIAN_POINT('Ctrl Pts',(0.810556943750001,11.6395833342893,1.40392580900275));
#9527=CARTESIAN_POINT('Ctrl Pts',(3.43862649647115E-16,11.5812500009559,
1.87190107867033));
#9528=CARTESIAN_POINT('Ctrl Pts',(-0.810556943749999,11.5229166676226,1.40392580900275));
#9529=CARTESIAN_POINT('Ctrl Pts',(-1.6211138875,11.4645833342893,0.935950539335167));
#9530=CARTESIAN_POINT('Ctrl Pts',(-1.6211138875,11.4062500009559,0.));
#9531=CARTESIAN_POINT('Ctrl Pts',(-1.6211138875,11.3479166676226,-0.935950539335166));
#9532=CARTESIAN_POINT('Ctrl Pts',(-0.81055694375,11.2895833342893,-1.40392580900275));
#9533=CARTESIAN_POINT('Ctrl Pts',(-1.14620883215705E-16,11.2312500009559,
-1.87190107867033));
#9534=CARTESIAN_POINT('Ctrl Pts',(0.81055694375,11.1729166676226,-1.40392580900275));
#9535=CARTESIAN_POINT('Ctrl Pts',(1.6211138875,11.1145833342893,-0.935950539335166));
#9536=CARTESIAN_POINT('Ctrl Pts',(1.6211138875,11.0562500009559,-1.9852919333802E-16));
#9537=CARTESIAN_POINT('Ctrl Pts',(1.6211138875,10.9979166676226,0.935950539335165));
#9538=CARTESIAN_POINT('Ctrl Pts',(0.810556943750001,10.9395833342893,1.40392580900275));
#9539=CARTESIAN_POINT('Ctrl Pts',(3.43862649647115E-16,10.8812500009559,
1.87190107867033));
#9540=CARTESIAN_POINT('Ctrl Pts',(-0.810556943749999,10.8229166676226,1.40392580900275));
#9541=CARTESIAN_POINT('Ctrl Pts',(-1.6211138875,10.7645833342893,0.935950539335167));
#9542=CARTESIAN_POINT('Ctrl Pts',(-1.6211138875,10.7062500009559,0.));
#9543=CARTESIAN_POINT('Ctrl Pts',(-1.6211138875,10.6479166676226,-0.935950539335166));
#9544=CARTESIAN_POINT('Ctrl Pts',(-0.81055694375,10.5895833342893,-1.40392580900275));
#9545=CARTESIAN_POINT('Ctrl Pts',(-1.14620883215705E-16,10.5312500009559,
-1.87190107867033));
#9546=CARTESIAN_POINT('Ctrl Pts',(0.81055694375,10.4729166676226,-1.40392580900275));
#9547=CARTESIAN_POINT('Ctrl Pts',(1.6211138875,10.4145833342893,-0.935950539335166));
#9548=CARTESIAN_POINT('Ctrl Pts',(1.6211138875,10.3562500009559,-1.9852919333802E-16));
#9549=CARTESIAN_POINT('Ctrl Pts',(1.6211138875,10.2979166676226,0.935950539335165));
#9550=CARTESIAN_POINT('Ctrl Pts',(0.810556943750001,10.2395833342893,1.40392580900275));
#9551=CARTESIAN_POINT('Ctrl Pts',(3.43862649647115E-16,10.1812500009559,
1.87190107867033));
#9552=CARTESIAN_POINT('Ctrl Pts',(-0.810556943749999,10.1229166676226,1.40392580900275));
#9553=CARTESIAN_POINT('Ctrl Pts',(-1.6211138875,10.0645833342893,0.935950539335167));
#9554=CARTESIAN_POINT('Ctrl Pts',(-1.6211138875,10.0062500009559,0.));
#9555=CARTESIAN_POINT('Ctrl Pts',(-1.6211138875,9.94791666762259,-0.935950539335166));
#9556=CARTESIAN_POINT('Ctrl Pts',(-0.81055694375,9.88958333428926,-1.40392580900275));
#9557=CARTESIAN_POINT('Ctrl Pts',(-1.14620883215705E-16,9.83125000095593,
-1.87190107867033));
#9558=CARTESIAN_POINT('Ctrl Pts',(0.81055694375,9.7729166676226,-1.40392580900275));
#9559=CARTESIAN_POINT('Ctrl Pts',(1.6211138875,9.71458333428926,-0.935950539335166));
#9560=CARTESIAN_POINT('Ctrl Pts',(1.6211138875,9.65625000095593,-1.9852919333802E-16));
#9561=CARTESIAN_POINT('Ctrl Pts',(1.6211138875,9.59791666762259,0.935950539335165));
#9562=CARTESIAN_POINT('Ctrl Pts',(0.810556943750001,9.53958333428926,1.40392580900275));
#9563=CARTESIAN_POINT('Ctrl Pts',(3.43862649647115E-16,9.48125000095593,
1.87190107867033));
#9564=CARTESIAN_POINT('Ctrl Pts',(-0.810556943749999,9.42291666762259,1.40392580900275));
#9565=CARTESIAN_POINT('Ctrl Pts',(-1.6211138875,9.36458333428926,0.935950539335167));
#9566=CARTESIAN_POINT('Ctrl Pts',(-1.6211138875,9.30625000095593,0.));
#9567=CARTESIAN_POINT('Ctrl Pts',(-1.6211138875,9.24791666762259,-0.935950539335166));
#9568=CARTESIAN_POINT('Ctrl Pts',(-0.81055694375,9.18958333428926,-1.40392580900275));
#9569=CARTESIAN_POINT('Ctrl Pts',(-1.14620883215705E-16,9.13125000095592,
-1.87190107867033));
#9570=CARTESIAN_POINT('Ctrl Pts',(0.81055694375,9.0729166676226,-1.40392580900275));
#9571=CARTESIAN_POINT('Ctrl Pts',(1.6211138875,9.01458333428926,-0.935950539335166));
#9572=CARTESIAN_POINT('Ctrl Pts',(1.6211138875,8.95625000095593,-1.9852919333802E-16));
#9573=CARTESIAN_POINT('Ctrl Pts',(1.6211138875,8.89791666762259,0.935950539335165));
#9574=CARTESIAN_POINT('Ctrl Pts',(0.810556943750001,8.83958333428926,1.40392580900275));
#9575=CARTESIAN_POINT('Ctrl Pts',(3.43862649647115E-16,8.78125000095592,
1.87190107867033));
#9576=CARTESIAN_POINT('Ctrl Pts',(-0.810556943749999,8.72291666762259,1.40392580900275));
#9577=CARTESIAN_POINT('Ctrl Pts',(-1.6211138875,8.66458333428927,0.935950539335167));
#9578=CARTESIAN_POINT('Ctrl Pts',(-1.6211138875,8.60625000095593,0.));
#9579=CARTESIAN_POINT('Ctrl Pts',(-1.6211138875,8.5479166676226,-0.935950539335166));
#9580=CARTESIAN_POINT('Ctrl Pts',(-0.81055694375,8.48958333428926,-1.40392580900275));
#9581=CARTESIAN_POINT('Ctrl Pts',(-1.14620883215705E-16,8.43125000095593,
-1.87190107867033));
#9582=CARTESIAN_POINT('Ctrl Pts',(0.81055694375,8.37291666762259,-1.40392580900275));
#9583=CARTESIAN_POINT('Ctrl Pts',(1.6211138875,8.31458333428926,-0.935950539335166));
#9584=CARTESIAN_POINT('Ctrl Pts',(1.6211138875,8.25625000095592,-1.9852919333802E-16));
#9585=CARTESIAN_POINT('Ctrl Pts',(1.6211138875,8.1979166676226,0.935950539335165));
#9586=CARTESIAN_POINT('Ctrl Pts',(0.810556943750001,8.13958333428925,1.40392580900275));
#9587=CARTESIAN_POINT('Ctrl Pts',(3.43862649647115E-16,8.08125000095593,
1.87190107867033));
#9588=CARTESIAN_POINT('Ctrl Pts',(-0.810556943749999,8.02291666762259,1.40392580900275));
#9589=CARTESIAN_POINT('Ctrl Pts',(-1.6211138875,7.96458333428926,0.935950539335167));
#9590=CARTESIAN_POINT('Ctrl Pts',(-1.6211138875,7.90625000095593,0.));
#9591=CARTESIAN_POINT('Ctrl Pts',(-1.6211138875,7.84791666762259,-0.935950539335166));
#9592=CARTESIAN_POINT('Ctrl Pts',(-0.81055694375,7.78958333428927,-1.40392580900275));
#9593=CARTESIAN_POINT('Ctrl Pts',(-1.14620883215705E-16,7.73125000095592,
-1.87190107867033));
#9594=CARTESIAN_POINT('Ctrl Pts',(0.81055694375,7.6729166676226,-1.40392580900275));
#9595=CARTESIAN_POINT('Ctrl Pts',(1.6211138875,7.61458333428926,-0.935950539335166));
#9596=CARTESIAN_POINT('Ctrl Pts',(1.6211138875,7.55625000095593,-1.9852919333802E-16));
#9597=CARTESIAN_POINT('Ctrl Pts',(1.6211138875,7.49791666762259,0.935950539335165));
#9598=CARTESIAN_POINT('Ctrl Pts',(0.810556943750001,7.43958333428926,1.40392580900275));
#9599=CARTESIAN_POINT('Ctrl Pts',(3.43862649647115E-16,7.38125000095592,
1.87190107867033));
#9600=CARTESIAN_POINT('Ctrl Pts',(-0.810556943749999,7.3229166676226,1.40392580900275));
#9601=CARTESIAN_POINT('Ctrl Pts',(-1.6211138875,7.26458333428925,0.935950539335167));
#9602=CARTESIAN_POINT('Ctrl Pts',(-1.6211138875,7.20625000095593,0.));
#9603=CARTESIAN_POINT('Ctrl Pts',(-1.6211138875,7.1479166676226,-0.935950539335166));
#9604=CARTESIAN_POINT('Ctrl Pts',(-0.81055694375,7.08958333428926,-1.40392580900275));
#9605=CARTESIAN_POINT('Ctrl Pts',(-1.14620883215705E-16,7.03125000095593,
-1.87190107867033));
#9606=CARTESIAN_POINT('Ctrl Pts',(0.81055694375,6.97291666762259,-1.40392580900275));
#9607=CARTESIAN_POINT('Ctrl Pts',(1.6211138875,6.91458333428927,-0.935950539335166));
#9608=CARTESIAN_POINT('Ctrl Pts',(1.6211138875,6.85625000095592,-1.9852919333802E-16));
#9609=CARTESIAN_POINT('Ctrl Pts',(1.6211138875,6.7979166676226,0.935950539335165));
#9610=CARTESIAN_POINT('Ctrl Pts',(0.810556943750001,6.73958333428926,1.40392580900275));
#9611=CARTESIAN_POINT('Ctrl Pts',(3.43862649647115E-16,6.68125000095593,
1.87190107867033));
#9612=CARTESIAN_POINT('Ctrl Pts',(-0.810556943749999,6.62291666762259,1.40392580900275));
#9613=CARTESIAN_POINT('Ctrl Pts',(-1.6211138875,6.56458333428926,0.935950539335167));
#9614=CARTESIAN_POINT('Ctrl Pts',(-1.6211138875,6.50625000095592,0.));
#9615=CARTESIAN_POINT('Ctrl Pts',(-1.6211138875,6.44791666762259,-0.935950539335166));
#9616=CARTESIAN_POINT('Ctrl Pts',(-0.81055694375,6.38958333428925,-1.40392580900275));
#9617=CARTESIAN_POINT('Ctrl Pts',(-1.14620883215705E-16,6.33125000095593,
-1.87190107867033));
#9618=CARTESIAN_POINT('Ctrl Pts',(0.81055694375,6.2729166676226,-1.40392580900275));
#9619=CARTESIAN_POINT('Ctrl Pts',(1.6211138875,6.21458333428926,-0.935950539335166));
#9620=CARTESIAN_POINT('Ctrl Pts',(1.6211138875,6.15625000095593,-1.9852919333802E-16));
#9621=CARTESIAN_POINT('Ctrl Pts',(1.6211138875,6.09791666762259,0.935950539335165));
#9622=CARTESIAN_POINT('Ctrl Pts',(0.810556943750001,6.03958333428927,1.40392580900275));
#9623=CARTESIAN_POINT('Ctrl Pts',(3.43862649647115E-16,5.98125000095592,
1.87190107867033));
#9624=CARTESIAN_POINT('Ctrl Pts',(-0.810556943749999,5.9229166676226,1.40392580900275));
#9625=CARTESIAN_POINT('Ctrl Pts',(-1.6211138875,5.86458333428926,0.935950539335167));
#9626=CARTESIAN_POINT('Ctrl Pts',(-1.6211138875,5.80625000095593,0.));
#9627=CARTESIAN_POINT('Ctrl Pts',(-1.6211138875,5.74791666762259,-0.935950539335166));
#9628=CARTESIAN_POINT('Ctrl Pts',(-0.81055694375,5.68958333428926,-1.40392580900275));
#9629=CARTESIAN_POINT('Ctrl Pts',(-1.14620883215705E-16,5.63125000095592,
-1.87190107867033));
#9630=CARTESIAN_POINT('Ctrl Pts',(0.81055694375,5.57291666762259,-1.40392580900275));
#9631=CARTESIAN_POINT('Ctrl Pts',(1.6211138875,5.51458333428927,-0.935950539335166));
#9632=CARTESIAN_POINT('Ctrl Pts',(1.6211138875,5.45625000095593,-1.9852919333802E-16));
#9633=CARTESIAN_POINT('Ctrl Pts',(1.6211138875,5.3979166676226,0.935950539335165));
#9634=CARTESIAN_POINT('Ctrl Pts',(0.810556943750001,5.33958333428926,1.40392580900275));
#9635=CARTESIAN_POINT('Ctrl Pts',(3.43862649647115E-16,5.28125000095593,
1.87190107867033));
#9636=CARTESIAN_POINT('Ctrl Pts',(-0.810556943749999,5.22291666762259,1.40392580900275));
#9637=CARTESIAN_POINT('Ctrl Pts',(-1.6211138875,5.16458333428926,0.935950539335167));
#9638=CARTESIAN_POINT('Ctrl Pts',(-1.6211138875,5.10625000095592,0.));
#9639=CARTESIAN_POINT('Ctrl Pts',(-1.6211138875,5.0479166676226,-0.935950539335166));
#9640=CARTESIAN_POINT('Ctrl Pts',(-0.81055694375,4.98958333428925,-1.40392580900275));
#9641=CARTESIAN_POINT('Ctrl Pts',(-1.14620883215705E-16,4.93125000095593,
-1.87190107867033));
#9642=CARTESIAN_POINT('Ctrl Pts',(0.81055694375,4.87291666762259,-1.40392580900275));
#9643=CARTESIAN_POINT('Ctrl Pts',(1.6211138875,4.81458333428926,-0.935950539335166));
#9644=CARTESIAN_POINT('Ctrl Pts',(1.6211138875,4.75625000095593,-1.9852919333802E-16));
#9645=CARTESIAN_POINT('Ctrl Pts',(1.6211138875,4.69791666762259,0.935950539335165));
#9646=CARTESIAN_POINT('Ctrl Pts',(0.810556943750001,4.63958333428927,1.40392580900275));
#9647=CARTESIAN_POINT('Ctrl Pts',(3.43862649647115E-16,4.58125000095593,
1.87190107867033));
#9648=CARTESIAN_POINT('Ctrl Pts',(-0.810556943749999,4.5229166676226,1.40392580900275));
#9649=CARTESIAN_POINT('Ctrl Pts',(-1.6211138875,4.46458333428926,0.935950539335167));
#9650=CARTESIAN_POINT('Ctrl Pts',(-1.6211138875,4.40625000095593,0.));
#9651=CARTESIAN_POINT('Ctrl Pts',(-1.6211138875,4.34791666762259,-0.935950539335166));
#9652=CARTESIAN_POINT('Ctrl Pts',(-0.81055694375,4.28958333428926,-1.40392580900275));
#9653=CARTESIAN_POINT('Ctrl Pts',(-1.14620883215705E-16,4.23125000095592,
-1.87190107867033));
#9654=CARTESIAN_POINT('Ctrl Pts',(0.81055694375,4.17291666762259,-1.40392580900275));
#9655=CARTESIAN_POINT('Ctrl Pts',(1.6211138875,4.11458333428925,-0.935950539335166));
#9656=CARTESIAN_POINT('Ctrl Pts',(1.6211138875,4.05625000095593,-1.9852919333802E-16));
#9657=CARTESIAN_POINT('Ctrl Pts',(1.6211138875,3.9979166676226,0.935950539335165));
#9658=CARTESIAN_POINT('Ctrl Pts',(0.810556943750001,3.93958333428926,1.40392580900275));
#9659=CARTESIAN_POINT('Ctrl Pts',(3.43862649647115E-16,3.88125000095593,
1.87190107867033));
#9660=CARTESIAN_POINT('Ctrl Pts',(-0.810556943749999,3.82291666762259,1.40392580900275));
#9661=CARTESIAN_POINT('Ctrl Pts',(-1.6211138875,3.76458333428927,0.935950539335167));
#9662=CARTESIAN_POINT('Ctrl Pts',(-1.6211138875,3.70625000095592,0.));
#9663=CARTESIAN_POINT('Ctrl Pts',(-1.6211138875,3.6479166676226,-0.935950539335166));
#9664=CARTESIAN_POINT('Ctrl Pts',(-0.81055694375,3.58958333428926,-1.40392580900275));
#9665=CARTESIAN_POINT('Ctrl Pts',(-1.14620883215705E-16,3.53125000095593,
-1.87190107867033));
#9666=CARTESIAN_POINT('Ctrl Pts',(0.81055694375,3.47291666762259,-1.40392580900275));
#9667=CARTESIAN_POINT('Ctrl Pts',(1.6211138875,3.41458333428926,-0.935950539335166));
#9668=CARTESIAN_POINT('Ctrl Pts',(1.6211138875,3.35625000095592,-1.9852919333802E-16));
#9669=CARTESIAN_POINT('Ctrl Pts',(1.6211138875,3.29791666762259,0.935950539335165));
#9670=CARTESIAN_POINT('Ctrl Pts',(0.810556943750001,3.23958333428925,1.40392580900275));
#9671=CARTESIAN_POINT('Ctrl Pts',(3.43862649647115E-16,3.18125000095593,
1.87190107867033));
#9672=CARTESIAN_POINT('Ctrl Pts',(-0.810556943749999,3.1229166676226,1.40392580900275));
#9673=CARTESIAN_POINT('Ctrl Pts',(-1.6211138875,3.06458333428926,0.935950539335167));
#9674=CARTESIAN_POINT('Ctrl Pts',(-1.6211138875,3.00625000095593,0.));
#9675=CARTESIAN_POINT('Ctrl Pts',(-1.6211138875,2.94791666762259,-0.935950539335166));
#9676=CARTESIAN_POINT('Ctrl Pts',(-0.81055694375,2.88958333428926,-1.40392580900275));
#9677=CARTESIAN_POINT('Ctrl Pts',(-1.14620883215705E-16,2.83125000095592,
-1.87190107867033));
#9678=CARTESIAN_POINT('Ctrl Pts',(0.81055694375,2.7729166676226,-1.40392580900275));
#9679=CARTESIAN_POINT('Ctrl Pts',(1.6211138875,2.71458333428926,-0.935950539335166));
#9680=CARTESIAN_POINT('Ctrl Pts',(1.6211138875,2.65625000095593,-1.9852919333802E-16));
#9681=CARTESIAN_POINT('Ctrl Pts',(1.6211138875,2.59791666762259,0.935950539335165));
#9682=CARTESIAN_POINT('Ctrl Pts',(0.810556943750001,2.53958333428926,1.40392580900275));
#9683=CARTESIAN_POINT('Ctrl Pts',(3.43862649647115E-16,2.48125000095592,
1.87190107867033));
#9684=CARTESIAN_POINT('Ctrl Pts',(-0.810556943749999,2.42291666762259,1.40392580900275));
#9685=CARTESIAN_POINT('Ctrl Pts',(-1.6211138875,2.36458333428927,0.935950539335167));
#9686=CARTESIAN_POINT('Ctrl Pts',(-1.6211138875,2.30625000095593,0.));
#9687=CARTESIAN_POINT('Ctrl Pts',(-1.6211138875,2.2479166676226,-0.935950539335166));
#9688=CARTESIAN_POINT('Ctrl Pts',(-0.81055694375,2.18958333428926,-1.40392580900275));
#9689=CARTESIAN_POINT('Ctrl Pts',(-1.14620883215705E-16,2.13125000095593,
-1.87190107867033));
#9690=CARTESIAN_POINT('Ctrl Pts',(0.81055694375,2.07291666762259,-1.40392580900275));
#9691=CARTESIAN_POINT('Ctrl Pts',(1.6211138875,2.01458333428926,-0.935950539335166));
#9692=CARTESIAN_POINT('Ctrl Pts',(1.6211138875,1.95625000095592,-1.9852919333802E-16));
#9693=CARTESIAN_POINT('Ctrl Pts',(1.6211138875,1.8979166676226,0.935950539335165));
#9694=CARTESIAN_POINT('Ctrl Pts',(0.810556943750001,1.83958333428925,1.40392580900275));
#9695=CARTESIAN_POINT('Ctrl Pts',(3.43862649647115E-16,1.78125000095593,
1.87190107867033));
#9696=CARTESIAN_POINT('Ctrl Pts',(-0.810556943749999,1.72291666762259,1.40392580900275));
#9697=CARTESIAN_POINT('Ctrl Pts',(-1.6211138875,1.66458333428926,0.935950539335167));
#9698=CARTESIAN_POINT('Ctrl Pts',(-1.6211138875,1.60625000095593,0.));
#9699=CARTESIAN_POINT('Ctrl Pts',(-1.6211138875,1.54791666762259,-0.935950539335166));
#9700=CARTESIAN_POINT('Ctrl Pts',(-0.81055694375,1.48958333428927,-1.40392580900275));
#9701=CARTESIAN_POINT('Ctrl Pts',(-1.14620883215705E-16,1.43125000095592,
-1.87190107867033));
#9702=CARTESIAN_POINT('Ctrl Pts',(0.81055694375,1.3729166676226,-1.40392580900275));
#9703=CARTESIAN_POINT('Ctrl Pts',(1.6211138875,1.31458333428926,-0.935950539335166));
#9704=CARTESIAN_POINT('Ctrl Pts',(1.6211138875,1.25625000095593,-1.9852919333802E-16));
#9705=CARTESIAN_POINT('Ctrl Pts',(1.6211138875,1.19791666762259,0.935950539335165));
#9706=CARTESIAN_POINT('Ctrl Pts',(0.810556943750001,1.13958333428926,1.40392580900275));
#9707=CARTESIAN_POINT('Ctrl Pts',(3.43862649647115E-16,1.08125000095592,
1.87190107867033));
#9708=CARTESIAN_POINT('Ctrl Pts',(-0.810556943749999,1.02291666762259,1.40392580900275));
#9709=CARTESIAN_POINT('Ctrl Pts',(-1.6211138875,0.964583334289254,0.935950539335167));
#9710=CARTESIAN_POINT('Ctrl Pts',(-1.6211138875,0.906250000955927,0.));
#9711=CARTESIAN_POINT('Ctrl Pts',(-1.6211138875,0.8479166676226,-0.935950539335166));
#9712=CARTESIAN_POINT('Ctrl Pts',(-0.81055694375,0.789583334289259,-1.40392580900275));
#9713=CARTESIAN_POINT('Ctrl Pts',(-1.14620883215705E-16,0.731250000955933,
-1.87190107867033));
#9714=CARTESIAN_POINT('Ctrl Pts',(0.81055694375,0.672916667622592,-1.40392580900275));
#9715=CARTESIAN_POINT('Ctrl Pts',(1.6211138875,0.614583334289265,-0.935950539335166));
#9716=CARTESIAN_POINT('Ctrl Pts',(1.6211138875,0.556250000955924,-1.9852919333802E-16));
#9717=CARTESIAN_POINT('Ctrl Pts',(1.6211138875,0.497916667622597,0.935950539335165));
#9718=CARTESIAN_POINT('Ctrl Pts',(0.810556943750001,0.439583334289256,1.40392580900275));
#9719=CARTESIAN_POINT('Ctrl Pts',(3.43862649647115E-16,0.381250000955929,
1.87190107867033));
#9720=CARTESIAN_POINT('Ctrl Pts',(-0.810556943749999,0.322916667622589,
1.40392580900275));
#9721=CARTESIAN_POINT('Ctrl Pts',(-1.6211138875,0.264583334289262,0.935950539335167));
#9722=CARTESIAN_POINT('Ctrl Pts',(-1.6211138875,0.206250000955921,0.));
#9723=CARTESIAN_POINT('Ctrl Pts',(-1.6211138875,0.147916667622594,-0.935950539335166));
#9724=CARTESIAN_POINT('Ctrl Pts',(-0.81055694375,0.0895833342892532,-1.40392580900275));
#9725=CARTESIAN_POINT('Ctrl Pts',(-1.14620883215705E-16,0.0312500009559263,
-1.87190107867033));
#9726=CARTESIAN_POINT('Ctrl Pts',(0.81055694375,-0.0270833323774006,-1.40392580900275));
#9727=CARTESIAN_POINT('Ctrl Pts',(1.6211138875,-0.0854166657107414,-0.935950539335166));
#9728=CARTESIAN_POINT('Ctrl Pts',(1.6211138875,-0.143749999044068,-1.9852919333802E-16));
#9729=CARTESIAN_POINT('Ctrl Pts',(1.6211138875,-0.202083332377409,0.935950539335165));
#9730=CARTESIAN_POINT('Ctrl Pts',(0.810556943750001,-0.260416665710736,
1.40392580900275));
#9731=CARTESIAN_POINT('Ctrl Pts',(3.43862649647115E-16,-0.318749999044077,
1.87190107867033));
#9732=CARTESIAN_POINT('Ctrl Pts',(-0.810556943749999,-0.377083332377404,
1.40392580900275));
#9733=CARTESIAN_POINT('Ctrl Pts',(-1.6211138875,-0.435416665710744,0.935950539335167));
#9734=CARTESIAN_POINT('Ctrl Pts',(-1.6211138875,-0.493749999044071,0.));
#9735=CARTESIAN_POINT('Ctrl Pts',(-1.6211138875,-0.552083332377412,-0.935950539335166));
#9736=CARTESIAN_POINT('Ctrl Pts',(-0.81055694375,-0.610416665710739,-1.40392580900275));
#9737=CARTESIAN_POINT('Ctrl Pts',(-1.14620883215705E-16,-0.66874999904408,
-1.87190107867033));
#9738=CARTESIAN_POINT('Ctrl Pts',(0.81055694375,-0.727083332377407,-1.40392580900275));
#9739=CARTESIAN_POINT('Ctrl Pts',(1.6211138875,-0.785416665710734,-0.935950539335166));
#9740=CARTESIAN_POINT('Ctrl Pts',(1.6211138875,-0.843749999044074,-1.9852919333802E-16));
#9741=CARTESIAN_POINT('Ctrl Pts',(1.6211138875,-0.902083332377402,0.935950539335165));
#9742=CARTESIAN_POINT('Ctrl Pts',(0.810556943750001,-0.960416665710742,
1.40392580900275));
#9743=CARTESIAN_POINT('Ctrl Pts',(3.43862649647115E-16,-1.01874999904407,
1.87190107867033));
#9744=CARTESIAN_POINT('Ctrl Pts',(-0.810556943749999,-1.07708333237741,
1.40392580900275));
#9745=CARTESIAN_POINT('Ctrl Pts',(-1.6211138875,-1.13541666571074,0.935950539335167));
#9746=CARTESIAN_POINT('Ctrl Pts',(-1.6211138875,-1.19374999904408,0.));
#9747=CARTESIAN_POINT('Ctrl Pts',(-1.6211138875,-1.2520833323774,-0.935950539335166));
#9748=CARTESIAN_POINT('Ctrl Pts',(-0.81055694375,-1.31041666571075,-1.40392580900275));
#9749=CARTESIAN_POINT('Ctrl Pts',(-1.14620883215705E-16,-1.36874999904407,
-1.87190107867033));
#9750=CARTESIAN_POINT('Ctrl Pts',(0.81055694375,-1.42708333237741,-1.40392580900275));
#9751=CARTESIAN_POINT('Ctrl Pts',(1.6211138875,-1.48541666571074,-0.935950539335166));
#9752=CARTESIAN_POINT('Ctrl Pts',(1.6211138875,-1.54374999904407,-1.9852919333802E-16));
#9753=CARTESIAN_POINT('Ctrl Pts',(1.6211138875,-1.60208333237741,0.935950539335165));
#9754=CARTESIAN_POINT('Ctrl Pts',(0.810556943750001,-1.66041666571073,1.40392580900275));
#9755=CARTESIAN_POINT('Ctrl Pts',(3.43862649647115E-16,-1.71874999904408,
1.87190107867033));
#9756=CARTESIAN_POINT('Ctrl Pts',(-0.810556943749999,-1.7770833323774,1.40392580900275));
#9757=CARTESIAN_POINT('Ctrl Pts',(-1.6211138875,-1.83541666571074,0.935950539335167));
#9758=CARTESIAN_POINT('Ctrl Pts',(-1.6211138875,-1.89374999904407,0.));
#9759=CARTESIAN_POINT('Ctrl Pts',(-1.6211138875,-1.95208333237741,-0.935950539335166));
#9760=CARTESIAN_POINT('Ctrl Pts',(-0.81055694375,-2.01041666571074,-1.40392580900275));
#9761=CARTESIAN_POINT('Ctrl Pts',(-1.14620883215705E-16,-2.06874999904408,
-1.87190107867033));
#9762=CARTESIAN_POINT('Ctrl Pts',(0.81055694375,-2.12708333237741,-1.40392580900275));
#9763=CARTESIAN_POINT('Ctrl Pts',(1.6211138875,-2.18541666571075,-0.935950539335166));
#9764=CARTESIAN_POINT('Ctrl Pts',(1.6211138875,-2.24374999904407,-1.9852919333802E-16));
#9765=CARTESIAN_POINT('Ctrl Pts',(1.6211138875,-2.3020833323774,0.935950539335165));
#9766=CARTESIAN_POINT('Ctrl Pts',(0.810556943750001,-2.36041666571074,1.40392580900275));
#9767=CARTESIAN_POINT('Ctrl Pts',(0.598929625666448,-2.37564684414964,1.52610889806617));
#9768=CARTESIAN_POINT('Ctrl Pts',(0.360688737133008,-2.39279232081431,1.5804790005409));
#9769=CARTESIAN_POINT('Ctrl Pts',(1.48613470695839,9.52000000000001,-1.33843019915343));
#9770=CARTESIAN_POINT('Ctrl Pts',(1.57630516101018,9.52000000000001,-1.2160238520719));
#9771=CARTESIAN_POINT('Ctrl Pts',(1.64972854045747,9.52000000000002,-1.08718013570266));
#9772=CARTESIAN_POINT('Ctrl Pts',(1.76662380592186,9.52000000000001,-0.814456482417219));
#9773=CARTESIAN_POINT('Ctrl Pts',(1.80998962761493,9.52000000000002,-0.669151004255831));
#9774=CARTESIAN_POINT('Ctrl Pts',(1.88756293094029,9.52000000000002,-0.231172020581771));
#9775=CARTESIAN_POINT('Ctrl Pts',(1.87351731814856,9.52000000000001,0.075154658113733));
#9776=CARTESIAN_POINT('Ctrl Pts',(1.74098688976458,9.52,0.499507026686462));
#9777=CARTESIAN_POINT('Ctrl Pts',(1.67755793546182,9.52,0.637636609961961));
#9778=CARTESIAN_POINT('Ctrl Pts',(1.52046925826298,9.51999999999999,0.888986033250457));
#9779=CARTESIAN_POINT('Ctrl Pts',(1.42490873390712,9.52000000000001,1.005753839455));
#9780=CARTESIAN_POINT('Ctrl Pts',(1.20787534958114,9.52000000000001,1.2103878868076));
#9781=CARTESIAN_POINT('Ctrl Pts',(1.08796092139376,9.52000000000001,1.29758441757011));
#9782=CARTESIAN_POINT('Ctrl Pts',(0.825073157518373,9.52000000000001,1.44138701387347));
#9783=CARTESIAN_POINT('Ctrl Pts',(0.68525065841953,9.52000000000001,1.49601523748159));
#9784=CARTESIAN_POINT('Ctrl Pts',(0.538440894222362,9.51999996467551,1.52908195976357));
#9785=CARTESIAN_POINT('Origin',(0.,0.,0.));
#9786=CARTESIAN_POINT('Origin',(0.,9.52000000000001,0.));
#9787=CARTESIAN_POINT('Origin',(0.,12.,0.));
#9788=CARTESIAN_POINT('',(-9.71064220297663E-16,12.,1.61658075373095));
#9789=CARTESIAN_POINT('',(-1.4,12.,0.808290376865476));
#9790=CARTESIAN_POINT('',(-1.325,12.,0.851591647054698));
#9791=CARTESIAN_POINT('',(-1.4,12.,-0.808290376865476));
#9792=CARTESIAN_POINT('',(-1.4,12.,-0.721687836487033));
#9793=CARTESIAN_POINT('',(1.9499918173238E-16,12.,-1.61658075373095));
#9794=CARTESIAN_POINT('',(-0.0749999999999998,12.,-1.57327948354173));
#9795=CARTESIAN_POINT('',(1.4,12.,-0.808290376865477));
#9796=CARTESIAN_POINT('',(1.325,12.,-0.851591647054698));
#9797=CARTESIAN_POINT('',(1.4,12.,0.808290376865476));
#9798=CARTESIAN_POINT('',(1.4,12.,0.721687836487033));
#9799=CARTESIAN_POINT('',(0.0749999999999994,12.,1.57327948354173));
#9800=CARTESIAN_POINT('Origin',(1.25,10.5,-0.721687836487033));
#9801=CARTESIAN_POINT('',(1.24999999999999,10.5,-0.721687836487047));
#9802=CARTESIAN_POINT('',(1.25,11.85,-0.721687836487033));
#9803=CARTESIAN_POINT('',(1.25,10.5,-0.721687836487033));
#9804=CARTESIAN_POINT('',(-1.09387392956801E-17,11.85,-1.44337567297407));
#9805=CARTESIAN_POINT('',(-5.42101086242752E-17,11.85,-1.44337567297407));
#9806=CARTESIAN_POINT('',(-1.09387392956801E-17,10.5,-1.44337567297407));
#9807=CARTESIAN_POINT('',(-1.09387392956801E-17,10.5,-1.44337567297407));
#9808=CARTESIAN_POINT('',(1.25,10.5,-0.721687836487033));
#9809=CARTESIAN_POINT('Origin',(1.25,10.5,0.721687836487033));
#9810=CARTESIAN_POINT('',(1.25,10.5,0.721687836487033));
#9811=CARTESIAN_POINT('',(1.25,11.85,0.721687836487033));
#9812=CARTESIAN_POINT('',(1.25,10.5,0.721687836487033));
#9813=CARTESIAN_POINT('',(1.25,11.85,-0.721687836487033));
#9814=CARTESIAN_POINT('',(1.25,10.5,0.721687836487033));
#9815=CARTESIAN_POINT('Origin',(-3.42958796722498E-16,10.5,1.44337567297406));
#9816=CARTESIAN_POINT('',(1.00899771935539E-14,10.5,1.44337567297406));
#9817=CARTESIAN_POINT('',(-3.42958796722498E-16,11.85,1.44337567297406));
#9818=CARTESIAN_POINT('',(-3.42958796722498E-16,10.5,1.44337567297406));
#9819=CARTESIAN_POINT('',(1.25,11.85,0.721687836487033));
#9820=CARTESIAN_POINT('',(-3.42958796722498E-16,10.5,1.44337567297406));
#9821=CARTESIAN_POINT('Origin',(-1.25,10.5,0.721687836487032));
#9822=CARTESIAN_POINT('',(-1.25,10.5,0.721687836487038));
#9823=CARTESIAN_POINT('',(-1.25,11.85,0.721687836487032));
#9824=CARTESIAN_POINT('',(-1.25,10.5,0.721687836487032));
#9825=CARTESIAN_POINT('',(-3.3881317890172E-16,11.85,1.44337567297406));
#9826=CARTESIAN_POINT('',(-1.25,10.5,0.721687836487032));
#9827=CARTESIAN_POINT('Origin',(-1.25,10.5,-0.721687836487033));
#9828=CARTESIAN_POINT('',(-1.25,10.5,-0.721687836487029));
#9829=CARTESIAN_POINT('',(-1.25,11.85,-0.721687836487033));
#9830=CARTESIAN_POINT('',(-1.25,10.5,-0.721687836487033));
#9831=CARTESIAN_POINT('',(-1.25,11.85,0.721687836487032));
#9832=CARTESIAN_POINT('',(-1.25,10.5,-0.721687836487033));
#9833=CARTESIAN_POINT('Origin',(-1.09387392956801E-17,10.5,-1.44337567297407));
#9834=CARTESIAN_POINT('',(-1.25,11.85,-0.721687836487033));
#9835=CARTESIAN_POINT('',(-1.09387392956801E-17,10.5,-1.44337567297407));
#9836=CARTESIAN_POINT('Origin',(1.25,11.85,0.721687836487033));
#9837=CARTESIAN_POINT('',(0.892857142857145,11.4928571428571,0.515491311776453));
#9838=CARTESIAN_POINT('',(0.892857142857144,11.4928571428571,-0.515491311776453));
#9839=CARTESIAN_POINT('Origin',(1.25,11.85,-0.721687836487033));
#9840=CARTESIAN_POINT('',(-4.33680868994202E-16,11.4928571428572,-1.03098262355291));
#9841=CARTESIAN_POINT('Origin',(-3.42958796722498E-16,11.85,1.44337567297406));
#9842=CARTESIAN_POINT('',(1.0842021724855E-15,11.4928571428572,1.03098262355291));
#9843=CARTESIAN_POINT('Origin',(-1.09387392956801E-17,11.85,-1.44337567297407));
#9844=CARTESIAN_POINT('',(-1.25,11.85,-0.721687836487033));
#9845=CARTESIAN_POINT('Origin',(-1.25,11.85,0.721687836487032));
#9846=CARTESIAN_POINT('',(-0.892857142857144,11.4928571428571,0.515491311776451));
#9847=CARTESIAN_POINT('Origin',(-1.25,11.85,-0.721687836487033));
#9848=CARTESIAN_POINT('Origin',(1.24999999999999,10.5,-0.721687836487047));
#9849=CARTESIAN_POINT('',(1.3661829762134E-15,10.3,-1.04337567297406));
#9850=CARTESIAN_POINT('',(2.38524477946811E-15,10.2113248654052,-0.866025403784446));
#9851=CARTESIAN_POINT('',(0.903589838486216,10.3,-0.521687836487043));
#9852=CARTESIAN_POINT('',(0.451794919243109,10.3,-0.782531754730552));
#9853=CARTESIAN_POINT('',(0.749999999999994,10.2113248654052,-0.43301270189223));
#9854=CARTESIAN_POINT('Origin',(1.25000000000001,10.5,0.721687836487021));
#9855=CARTESIAN_POINT('',(0.903589838486227,10.3,0.521687836487022));
#9856=CARTESIAN_POINT('',(0.903589838486221,10.3,-9.50233343939879E-15));
#9857=CARTESIAN_POINT('',(0.750000000000001,10.2113248654052,0.433012701892211));
#9858=CARTESIAN_POINT('Origin',(1.00899771935539E-14,10.5,1.44337567297406));
#9859=CARTESIAN_POINT('',(7.27313732092168E-15,10.3,1.04337567297406));
#9860=CARTESIAN_POINT('',(0.451794919243117,10.3,0.782531754730542));
#9861=CARTESIAN_POINT('',(6.28837260041593E-15,10.2113248654052,0.866025403784435));
#9862=CARTESIAN_POINT('Origin',(-1.25,10.5,0.721687836487038));
#9863=CARTESIAN_POINT('',(-0.90358983848622,10.3,0.521687836487035));
#9864=CARTESIAN_POINT('',(-0.451794919243106,10.3,0.782531754730548));
#9865=CARTESIAN_POINT('',(-0.749999999999995,10.2113248654052,0.433012701892221));
#9866=CARTESIAN_POINT('Origin',(-1.25,10.5,-0.721687836487029));
#9867=CARTESIAN_POINT('',(-0.903589838486223,10.3,-0.521687836487029));
#9868=CARTESIAN_POINT('',(-0.903589838486221,10.3,2.98644765238248E-15));
#9869=CARTESIAN_POINT('',(-0.749999999999998,10.2113248654052,-0.433012701892216));
#9870=CARTESIAN_POINT('Origin',(-1.09387392956801E-17,10.5,-1.44337567297407));
#9871=CARTESIAN_POINT('',(-0.451794919243112,10.3,-0.782531754730545));
#9872=CARTESIAN_POINT('Origin',(0.,10.3,0.));
#9893=UNCERTAINTY_MEASURE_WITH_UNIT(LENGTH_MEASURE(0.01),#9904,
'DISTANCE_ACCURACY_VALUE',
'Maximum model space distance between geometric entities at asserted c
onnectivities');
#9894=UNCERTAINTY_MEASURE_WITH_UNIT(LENGTH_MEASURE(0.01),#9904,
'DISTANCE_ACCURACY_VALUE',
'Maximum model space distance between geometric entities at asserted c
onnectivities');
#9902=(
GEOMETRIC_REPRESENTATION_CONTEXT(3)
GLOBAL_UNCERTAINTY_ASSIGNED_CONTEXT((#9893))
GLOBAL_UNIT_ASSIGNED_CONTEXT((#9904,#9906,#9907))
REPRESENTATION_CONTEXT('','3D')
);
#9903=(
GEOMETRIC_REPRESENTATION_CONTEXT(3)
GLOBAL_UNCERTAINTY_ASSIGNED_CONTEXT((#9894))
GLOBAL_UNIT_ASSIGNED_CONTEXT((#9904,#9906,#9907))
REPRESENTATION_CONTEXT('','3D')
);
#9904=(
LENGTH_UNIT()
NAMED_UNIT(*)
SI_UNIT(.MILLI.,.METRE.)
);
#9906=(
NAMED_UNIT(*)
PLANE_ANGLE_UNIT()
SI_UNIT($,.RADIAN.)
);
#9907=(
NAMED_UNIT(*)
SI_UNIT($,.STERADIAN.)
SOLID_ANGLE_UNIT()
);
#9915=SHAPE_DEFINITION_REPRESENTATION(#9923,#9944);
#9923=PRODUCT_DEFINITION_SHAPE('',$,#9953);
#9944=SHAPE_REPRESENTATION('',(#2234),#9902);
#9945=PRODUCT_DEFINITION_CONTEXT('part definition',#9971,'design');
#9953=PRODUCT_DEFINITION('Countersunk Screw ISO 10642 M4x12 A2',
'Countersunk Screw ISO 10642 M4x12 A2',#9961,#9945);
#9961=PRODUCT_DEFINITION_FORMATION('',$,#9980);
#9971=APPLICATION_CONTEXT(
'Core Data for Automotive Mechanical Design Process');
#9972=PRODUCT_CONTEXT('part definition',#9971,'mechanical');
#9980=PRODUCT('Countersunk Screw ISO 10642 M4x12 A2',
'Countersunk Screw ISO 10642 M4x12 A2',$,(#9972));
#9985=PRESENTATION_STYLE_ASSIGNMENT((#9990));
#9990=SURFACE_STYLE_USAGE(.BOTH.,#9995);
#9995=SURFACE_SIDE_STYLE('',(#10000));
#10000=SURFACE_STYLE_FILL_AREA(#10005);
#10005=FILL_AREA_STYLE('Opaque(31,36,43)',(#10010));
#10010=FILL_AREA_STYLE_COLOUR('Opaque(31,36,43)',#10015);
#10015=COLOUR_RGB('Opaque(31,36,43)',0.12156862745098,0.141176470588235,
0.168627450980392);
ENDSEC;
END-ISO-10303-21;
